ISO-10303-21;
HEADER;
/* Generated by software containing ST-Developer
 * from STEP Tools, Inc. (www.steptools.com) 
 */

FILE_DESCRIPTION(
/* description */ ('STEP AP214'),
/* implementation_level */ '2;1');

FILE_NAME(
/* name */ 'Eye Bolt.step',
/* time_stamp */ '2026-11-14T07:13:32-08:00',
/* author */ (''),
/* organization */ (''),
/* preprocessor_version */ 'ST-DEVELOPER v20.2',
/* originating_system */ 'Autodesk Translation Framework v15.17.0.0',
/* authorisation */ '');

FILE_SCHEMA (('AUTOMOTIVE_DESIGN { 1 0 10303 214 3 1 1 }'));
ENDSEC;

DATA;
#10=MECHANICAL_DESIGN_GEOMETRIC_PRESENTATION_REPRESENTATION('',(#1322),#32903);
#299=(
BOUNDED_SURFACE()
B_SPLINE_SURFACE(1,2,((#26568,#26569,#26570,#26571,#26572,#26573,#26574,
#26575,#26576,#26577,#26578,#26579,#26580,#26581,#26582,#26583,#26584,#26585,
#26586,#26587,#26588,#26589,#26590,#26591,#26592,#26593,#26594,#26595,#26596,
#26597,#26598,#26599,#26600,#26601,#26602,#26603,#26604,#26605,#26606,#26607,
#26608,#26609,#26610,#26611,#26612,#26613,#26614,#26615,#26616,#26617,#26618,
#26619,#26620,#26621,#26622,#26623,#26624,#26625,#26626,#26627,#26628,#26629,
#26630,#26631,#26632,#26633,#26634,#26635,#26636,#26637,#26638,#26639,#26640,
#26641,#26642,#26643,#26644,#26645,#26646,#26647,#26648,#26649,#26650,#26651,
#26652,#26653,#26654,#26655,#26656,#26657,#26658,#26659,#26660,#26661,#26662,
#26663,#26664,#26665,#26666,#26667,#26668,#26669,#26670,#26671,#26672,#26673,
#26674,#26675,#26676,#26677,#26678,#26679,#26680,#26681,#26682,#26683,#26684,
#26685,#26686,#26687,#26688,#26689,#26690,#26691,#26692,#26693,#26694,#26695,
#26696,#26697,#26698,#26699,#26700,#26701,#26702,#26703,#26704,#26705,#26706,
#26707,#26708,#26709,#26710,#26711,#26712,#26713,#26714,#26715,#26716,#26717,
#26718,#26719,#26720,#26721,#26722,#26723,#26724,#26725,#26726,#26727,#26728,
#26729,#26730,#26731,#26732,#26733,#26734,#26735,#26736,#26737,#26738,#26739,
#26740,#26741,#26742,#26743,#26744,#26745,#26746,#26747,#26748,#26749,#26750,
#26751,#26752,#26753,#26754,#26755,#26756,#26757,#26758,#26759,#26760,#26761,
#26762,#26763,#26764,#26765,#26766,#26767,#26768,#26769,#26770,#26771,#26772,
#26773,#26774,#26775,#26776,#26777,#26778,#26779,#26780,#26781,#26782,#26783,
#26784,#26785,#26786,#26787,#26788,#26789,#26790,#26791,#26792,#26793,#26794,
#26795,#26796,#26797,#26798,#26799,#26800,#26801,#26802,#26803,#26804,#26805,
#26806,#26807,#26808,#26809,#26810,#26811,#26812,#26813,#26814,#26815,#26816,
#26817,#26818,#26819,#26820,#26821,#26822,#26823,#26824,#26825,#26826,#26827,
#26828,#26829,#26830,#26831,#26832,#26833,#26834,#26835,#26836,#26837,#26838,
#26839,#26840,#26841,#26842,#26843,#26844,#26845,#26846,#26847,#26848,#26849,
#26850,#26851,#26852,#26853,#26854,#26855,#26856,#26857,#26858,#26859,#26860,
#26861,#26862,#26863,#26864,#26865,#26866,#26867,#26868,#26869,#26870,#26871,
#26872,#26873,#26874,#26875,#26876,#26877,#26878,#26879,#26880,#26881,#26882,
#26883,#26884,#26885,#26886,#26887,#26888,#26889,#26890,#26891,#26892,#26893,
#26894,#26895,#26896,#26897,#26898,#26899,#26900,#26901,#26902,#26903,#26904,
#26905,#26906,#26907,#26908,#26909,#26910,#26911,#26912,#26913,#26914,#26915,
#26916,#26917,#26918,#26919,#26920,#26921,#26922,#26923,#26924,#26925,#26926,
#26927,#26928,#26929,#26930,#26931,#26932,#26933,#26934,#26935,#26936,#26937,
#26938,#26939,#26940,#26941,#26942,#26943,#26944,#26945,#26946,#26947,#26948,
#26949,#26950,#26951,#26952,#26953,#26954,#26955,#26956,#26957,#26958,#26959,
#26960,#26961,#26962,#26963,#26964,#26965,#26966,#26967,#26968,#26969,#26970,
#26971,#26972,#26973,#26974,#26975,#26976,#26977,#26978,#26979,#26980,#26981,
#26982,#26983,#26984,#26985,#26986,#26987,#26988,#26989,#26990,#26991,#26992,
#26993,#26994,#26995,#26996,#26997,#26998,#26999,#27000,#27001,#27002,#27003,
#27004),(#27005,#27006,#27007,#27008,#27009,#27010,#27011,#27012,#27013,
#27014,#27015,#27016,#27017,#27018,#27019,#27020,#27021,#27022,#27023,#27024,
#27025,#27026,#27027,#27028,#27029,#27030,#27031,#27032,#27033,#27034,#27035,
#27036,#27037,#27038,#27039,#27040,#27041,#27042,#27043,#27044,#27045,#27046,
#27047,#27048,#27049,#27050,#27051,#27052,#27053,#27054,#27055,#27056,#27057,
#27058,#27059,#27060,#27061,#27062,#27063,#27064,#27065,#27066,#27067,#27068,
#27069,#27070,#27071,#27072,#27073,#27074,#27075,#27076,#27077,#27078,#27079,
#27080,#27081,#27082,#27083,#27084,#27085,#27086,#27087,#27088,#27089,#27090,
#27091,#27092,#27093,#27094,#27095,#27096,#27097,#27098,#27099,#27100,#27101,
#27102,#27103,#27104,#27105,#27106,#27107,#27108,#27109,#27110,#27111,#27112,
#27113,#27114,#27115,#27116,#27117,#27118,#27119,#27120,#27121,#27122,#27123,
#27124,#27125,#27126,#27127,#27128,#27129,#27130,#27131,#27132,#27133,#27134,
#27135,#27136,#27137,#27138,#27139,#27140,#27141,#27142,#27143,#27144,#27145,
#27146,#27147,#27148,#27149,#27150,#27151,#27152,#27153,#27154,#27155,#27156,
#27157,#27158,#27159,#27160,#27161,#27162,#27163,#27164,#27165,#27166,#27167,
#27168,#27169,#27170,#27171,#27172,#27173,#27174,#27175,#27176,#27177,#27178,
#27179,#27180,#27181,#27182,#27183,#27184,#27185,#27186,#27187,#27188,#27189,
#27190,#27191,#27192,#27193,#27194,#27195,#27196,#27197,#27198,#27199,#27200,
#27201,#27202,#27203,#27204,#27205,#27206,#27207,#27208,#27209,#27210,#27211,
#27212,#27213,#27214,#27215,#27216,#27217,#27218,#27219,#27220,#27221,#27222,
#27223,#27224,#27225,#27226,#27227,#27228,#27229,#27230,#27231,#27232,#27233,
#27234,#27235,#27236,#27237,#27238,#27239,#27240,#27241,#27242,#27243,#27244,
#27245,#27246,#27247,#27248,#27249,#27250,#27251,#27252,#27253,#27254,#27255,
#27256,#27257,#27258,#27259,#27260,#27261,#27262,#27263,#27264,#27265,#27266,
#27267,#27268,#27269,#27270,#27271,#27272,#27273,#27274,#27275,#27276,#27277,
#27278,#27279,#27280,#27281,#27282,#27283,#27284,#27285,#27286,#27287,#27288,
#27289,#27290,#27291,#27292,#27293,#27294,#27295,#27296,#27297,#27298,#27299,
#27300,#27301,#27302,#27303,#27304,#27305,#27306,#27307,#27308,#27309,#27310,
#27311,#27312,#27313,#27314,#27315,#27316,#27317,#27318,#27319,#27320,#27321,
#27322,#27323,#27324,#27325,#27326,#27327,#27328,#27329,#27330,#27331,#27332,
#27333,#27334,#27335,#27336,#27337,#27338,#27339,#27340,#27341,#27342,#27343,
#27344,#27345,#27346,#27347,#27348,#27349,#27350,#27351,#27352,#27353,#27354,
#27355,#27356,#27357,#27358,#27359,#27360,#27361,#27362,#27363,#27364,#27365,
#27366,#27367,#27368,#27369,#27370,#27371,#27372,#27373,#27374,#27375,#27376,
#27377,#27378,#27379,#27380,#27381,#27382,#27383,#27384,#27385,#27386,#27387,
#27388,#27389,#27390,#27391,#27392,#27393,#27394,#27395,#27396,#27397,#27398,
#27399,#27400,#27401,#27402,#27403,#27404,#27405,#27406,#27407,#27408,#27409,
#27410,#27411,#27412,#27413,#27414,#27415,#27416,#27417,#27418,#27419,#27420,
#27421,#27422,#27423,#27424,#27425,#27426,#27427,#27428,#27429,#27430,#27431,
#27432,#27433,#27434,#27435,#27436,#27437,#27438,#27439,#27440,#27441)),
 .UNSPECIFIED.,.F.,.F.,.F.)
B_SPLINE_SURFACE_WITH_KNOTS((2,2),(3,2,2,2,2,2,2,2,2,2,2,2,2,2,2,2,2,2,
2,2,2,2,2,2,2,2,2,2,2,2,2,2,2,2,2,2,2,2,2,2,2,2,2,2,2,2,2,2,2,2,2,2,2,2,
2,2,2,2,2,2,2,2,2,2,2,2,2,2,2,2,2,2,2,2,2,2,2,2,2,2,2,2,2,2,2,2,2,2,2,2,
2,2,2,2,2,2,2,2,2,2,2,2,2,2,2,2,2,2,2,2,2,2,2,2,2,2,2,2,2,2,2,2,2,2,2,2,
2,2,2,2,2,2,2,2,2,2,2,2,2,2,2,2,2,2,2,2,2,2,2,2,2,2,2,2,2,2,2,2,2,2,2,2,
2,2,2,2,2,2,2,2,2,2,2,2,2,2,2,2,2,2,2,2,2,2,2,2,2,2,2,2,2,2,2,2,2,2,2,2,
2,2,2,2,2,2,2,2,2,2,2,2,2,2,2,2,2,2,2,2,3),(0.,1.00000935051354),(0.,0.00454545454545455,
0.00909090909090909,0.0136363636363636,0.0181818181818182,0.0227272727272727,
0.0272727272727273,0.0318181818181818,0.0363636363636364,0.0409090909090909,
0.0454545454545455,0.05,0.0545454545454545,0.0590909090909091,0.0636363636363636,
0.0681818181818182,0.0727272727272727,0.0772727272727273,0.0818181818181818,
0.0863636363636364,0.0909090909090909,0.0954545454545455,0.1,0.104545454545455,
0.109090909090909,0.113636363636364,0.118181818181818,0.122727272727273,
0.127272727272727,0.131818181818182,0.136363636363636,0.140909090909091,
0.145454545454545,0.15,0.154545454545455,0.159090909090909,0.163636363636364,
0.168181818181818,0.172727272727273,0.177272727272727,0.181818181818182,
0.186363636363636,0.190909090909091,0.195454545454545,0.2,0.204545454545455,
0.209090909090909,0.213636363636364,0.218181818181818,0.222727272727273,
0.227272727272727,0.231818181818182,0.236363636363636,0.240909090909091,
0.245454545454545,0.25,0.254545454545455,0.259090909090909,0.263636363636364,
0.268181818181818,0.272727272727273,0.277272727272727,0.281818181818182,
0.286363636363636,0.290909090909091,0.295454545454545,0.3,0.304545454545455,
0.309090909090909,0.313636363636364,0.318181818181818,0.322727272727273,
0.327272727272727,0.331818181818182,0.336363636363636,0.340909090909091,
0.345454545454545,0.35,0.354545454545455,0.359090909090909,0.363636363636364,
0.368181818181818,0.372727272727273,0.377272727272727,0.381818181818182,
0.386363636363636,0.390909090909091,0.395454545454545,0.4,0.404545454545455,
0.409090909090909,0.413636363636364,0.418181818181818,0.422727272727273,
0.427272727272727,0.431818181818182,0.436363636363636,0.440909090909091,
0.445454545454545,0.45,0.454545454545455,0.459090909090909,0.463636363636364,
0.468181818181818,0.472727272727273,0.477272727272727,0.481818181818182,
0.486363636363636,0.490909090909091,0.495454545454545,0.5,0.504545454545455,
0.509090909090909,0.513636363636364,0.518181818181818,0.522727272727273,
0.527272727272727,0.531818181818182,0.536363636363636,0.540909090909091,
0.545454545454545,0.55,0.554545454545455,0.559090909090909,0.563636363636364,
0.568181818181818,0.572727272727273,0.577272727272727,0.581818181818182,
0.586363636363636,0.590909090909091,0.595454545454545,0.6,0.604545454545454,
0.609090909090909,0.613636363636364,0.618181818181818,0.622727272727273,
0.627272727272727,0.631818181818182,0.636363636363636,0.640909090909091,
0.645454545454546,0.65,0.654545454545455,0.659090909090909,0.663636363636364,
0.668181818181818,0.672727272727273,0.677272727272727,0.681818181818182,
0.686363636363636,0.690909090909091,0.695454545454545,0.7,0.704545454545455,
0.709090909090909,0.713636363636364,0.718181818181818,0.722727272727273,
0.727272727272727,0.731818181818182,0.736363636363636,0.740909090909091,
0.745454545454545,0.75,0.754545454545455,0.759090909090909,0.763636363636364,
0.768181818181818,0.772727272727273,0.777272727272727,0.781818181818182,
0.786363636363636,0.790909090909091,0.795454545454545,0.8,0.804545454545455,
0.809090909090909,0.813636363636364,0.818181818181818,0.822727272727273,
0.827272727272727,0.831818181818182,0.836363636363636,0.840909090909091,
0.845454545454545,0.85,0.854545454545454,0.859090909090909,0.863636363636364,
0.868181818181818,0.872727272727273,0.877272727272727,0.881818181818182,
0.886363636363636,0.890909090909091,0.895454545454546,0.9,0.904545454545455,
0.909090909090909,0.913636363636364,0.918181818181818,0.922727272727273,
0.927272727272727,0.931818181818182,0.936363636363636,0.940909090909091,
0.945454545454545,0.95,0.954545454545455,0.959090909090909,0.963636363636364,
0.968181818181818,0.972727272727273,0.977272727272727,0.981818181818182,
0.984250640629257,0.99409314703555),.UNSPECIFIED.)
GEOMETRIC_REPRESENTATION_ITEM()
RATIONAL_B_SPLINE_SURFACE(((1.,0.951056516295154,1.,0.951056516295154,1.,
0.951056516295154,1.,0.951056516295154,1.,0.951056516295154,1.,0.951056516295154,
1.,0.951056516295154,1.,0.951056516295154,1.,0.951056516295154,1.,0.951056516295154,
1.,0.951056516295154,1.,0.951056516295154,1.,0.951056516295154,1.,0.951056516295154,
1.,0.951056516295154,1.,0.951056516295154,1.,0.951056516295154,1.,0.951056516295154,
1.,0.951056516295154,1.,0.951056516295154,1.,0.951056516295154,1.,0.951056516295154,
1.,0.951056516295154,1.,0.951056516295154,1.,0.951056516295154,1.,0.951056516295154,
1.,0.951056516295154,1.,0.951056516295154,1.,0.951056516295154,1.,0.951056516295154,
1.,0.951056516295154,1.,0.951056516295154,1.,0.951056516295154,1.,0.951056516295154,
1.,0.951056516295154,1.,0.951056516295154,1.,0.951056516295154,1.,0.951056516295154,
1.,0.951056516295154,1.,0.951056516295154,1.,0.951056516295154,1.,0.951056516295154,
1.,0.951056516295154,1.,0.951056516295154,1.,0.951056516295154,1.,0.951056516295154,
1.,0.951056516295154,1.,0.951056516295154,1.,0.951056516295154,1.,0.951056516295154,
1.,0.951056516295154,1.,0.951056516295154,1.,0.951056516295154,1.,0.951056516295154,
1.,0.951056516295154,1.,0.951056516295154,1.,0.951056516295154,1.,0.951056516295154,
1.,0.951056516295154,1.,0.951056516295154,1.,0.951056516295154,1.,0.951056516295154,
1.,0.951056516295154,1.,0.951056516295154,1.,0.951056516295154,1.,0.951056516295154,
1.,0.951056516295154,1.,0.951056516295154,1.,0.951056516295154,1.,0.951056516295154,
1.,0.951056516295154,1.,0.951056516295154,1.,0.951056516295154,1.,0.951056516295154,
1.,0.951056516295154,1.,0.951056516295154,1.,0.951056516295154,1.,0.951056516295154,
1.,0.951056516295154,1.,0.951056516295154,1.,0.951056516295154,1.,0.951056516295154,
1.,0.951056516295154,1.,0.951056516295154,1.,0.951056516295154,1.,0.951056516295154,
1.,0.951056516295154,1.,0.951056516295154,1.,0.951056516295154,1.,0.951056516295154,
1.,0.951056516295154,1.,0.951056516295154,1.,0.951056516295154,1.,0.951056516295154,
1.,0.951056516295154,1.,0.951056516295154,1.,0.951056516295154,1.,0.951056516295154,
1.,0.951056516295154,1.,0.951056516295154,1.,0.951056516295154,1.,0.951056516295154,
1.,0.951056516295154,1.,0.951056516295154,1.,0.951056516295154,1.,0.951056516295154,
1.,0.951056516295154,1.,0.951056516295154,1.,0.951056516295154,1.,0.951056516295154,
1.,0.951056516295154,1.,0.951056516295154,1.,0.951056516295154,1.,0.951056516295154,
1.,0.951056516295154,1.,0.951056516295154,1.,0.951056516295154,1.,0.951056516295154,
1.,0.951056516295154,1.,0.951056516295154,1.,0.951056516295154,1.,0.951056516295154,
1.,0.951056516295154,1.,0.951056516295154,1.,0.951056516295154,1.,0.951056516295154,
1.,0.951056516295154,1.,0.951056516295154,1.,0.951056516295154,1.,0.951056516295154,
1.,0.951056516295154,1.,0.951056516295154,1.,0.951056516295154,1.,0.951056516295154,
1.,0.951056516295154,1.,0.951056516295154,1.,0.951056516295154,1.,0.951056516295154,
1.,0.951056516295154,1.,0.951056516295154,1.,0.951056516295154,1.,0.951056516295154,
1.,0.951056516295154,1.,0.951056516295154,1.,0.951056516295154,1.,0.951056516295154,
1.,0.951056516295154,1.,0.951056516295154,1.,0.951056516295154,1.,0.951056516295154,
1.,0.951056516295154,1.,0.951056516295154,1.,0.951056516295154,1.,0.951056516295154,
1.,0.951056516295154,1.,0.951056516295154,1.,0.951056516295154,1.,0.951056516295154,
1.,0.951056516295154,1.,0.951056516295154,1.,0.951056516295154,1.,0.951056516295154,
1.,0.951056516295154,1.,0.951056516295154,1.,0.951056516295154,1.,0.951056516295154,
1.,0.951056516295154,1.,0.951056516295154,1.,0.951056516295154,1.,0.951056516295154,
1.,0.951056516295154,1.,0.951056516295154,1.,0.951056516295154,1.,0.951056516295154,
1.,0.951056516295154,1.,0.951056516295154,1.,0.951056516295154,1.,0.951056516295154,
1.,0.951056516295154,1.,0.951056516295154,1.,0.951056516295154,1.,0.951056516295154,
1.,0.951056516295154,1.,0.951056516295154,1.,0.951056516295154,1.,0.951056516295154,
1.,0.951056516295154,1.,0.951056516295154,1.,0.951056516295154,1.,0.951056516295154,
1.,0.951056516295154,1.,0.951056516295154,1.,0.951056516295154,1.,0.951056516295154,
1.,0.951056516295154,1.,0.951056516295154,1.,0.951056516295154,1.,0.951056516295154,
1.,0.951056516295154,1.,0.951056516295154,1.,0.951056516295154,1.,0.951056516295154,
1.,0.951056516295154,1.,0.951056516295154,1.,0.951056516295154,1.,0.951056516295154,
1.,0.951056516295154,1.,0.951056516295154,1.,0.951056516295154,1.,0.951056516295154,
1.,0.951056516295154,1.,0.951056516295154,1.,0.951056516295154,1.,0.951056516295154,
1.,0.951056516295154,1.,0.951056516295154,1.,0.973808338199829,0.975649137349576,
0.975649137349576,0.975649137349576),(1.,0.951056516295154,1.,0.951056516295154,
1.,0.951056516295154,1.,0.951056516295154,1.,0.951056516295154,1.,0.951056516295154,
1.,0.951056516295154,1.,0.951056516295154,1.,0.951056516295154,1.,0.951056516295154,
1.,0.951056516295154,1.,0.951056516295154,1.,0.951056516295154,1.,0.951056516295154,
1.,0.951056516295154,1.,0.951056516295154,1.,0.951056516295154,1.,0.951056516295154,
1.,0.951056516295154,1.,0.951056516295154,1.,0.951056516295154,1.,0.951056516295154,
1.,0.951056516295154,1.,0.951056516295154,1.,0.951056516295154,1.,0.951056516295154,
1.,0.951056516295154,1.,0.951056516295154,1.,0.951056516295154,1.,0.951056516295154,
1.,0.951056516295154,1.,0.951056516295154,1.,0.951056516295154,1.,0.951056516295154,
1.,0.951056516295154,1.,0.951056516295154,1.,0.951056516295154,1.,0.951056516295154,
1.,0.951056516295154,1.,0.951056516295154,1.,0.951056516295154,1.,0.951056516295154,
1.,0.951056516295154,1.,0.951056516295154,1.,0.951056516295154,1.,0.951056516295154,
1.,0.951056516295154,1.,0.951056516295154,1.,0.951056516295154,1.,0.951056516295154,
1.,0.951056516295154,1.,0.951056516295154,1.,0.951056516295154,1.,0.951056516295154,
1.,0.951056516295154,1.,0.951056516295154,1.,0.951056516295154,1.,0.951056516295154,
1.,0.951056516295154,1.,0.951056516295154,1.,0.951056516295154,1.,0.951056516295154,
1.,0.951056516295154,1.,0.951056516295154,1.,0.951056516295154,1.,0.951056516295154,
1.,0.951056516295154,1.,0.951056516295154,1.,0.951056516295154,1.,0.951056516295154,
1.,0.951056516295154,1.,0.951056516295154,1.,0.951056516295154,1.,0.951056516295154,
1.,0.951056516295154,1.,0.951056516295154,1.,0.951056516295154,1.,0.951056516295154,
1.,0.951056516295154,1.,0.951056516295154,1.,0.951056516295154,1.,0.951056516295154,
1.,0.951056516295154,1.,0.951056516295154,1.,0.951056516295154,1.,0.951056516295154,
1.,0.951056516295154,1.,0.951056516295154,1.,0.951056516295154,1.,0.951056516295154,
1.,0.951056516295154,1.,0.951056516295154,1.,0.951056516295154,1.,0.951056516295154,
1.,0.951056516295154,1.,0.951056516295154,1.,0.951056516295154,1.,0.951056516295154,
1.,0.951056516295154,1.,0.951056516295154,1.,0.951056516295154,1.,0.951056516295154,
1.,0.951056516295154,1.,0.951056516295154,1.,0.951056516295154,1.,0.951056516295154,
1.,0.951056516295154,1.,0.951056516295154,1.,0.951056516295154,1.,0.951056516295154,
1.,0.951056516295154,1.,0.951056516295154,1.,0.951056516295154,1.,0.951056516295154,
1.,0.951056516295154,1.,0.951056516295154,1.,0.951056516295154,1.,0.951056516295154,
1.,0.951056516295154,1.,0.951056516295154,1.,0.951056516295154,1.,0.951056516295154,
1.,0.951056516295154,1.,0.951056516295154,1.,0.951056516295154,1.,0.951056516295154,
1.,0.951056516295154,1.,0.951056516295154,1.,0.951056516295154,1.,0.951056516295154,
1.,0.951056516295154,1.,0.951056516295154,1.,0.951056516295154,1.,0.951056516295154,
1.,0.951056516295154,1.,0.951056516295154,1.,0.951056516295154,1.,0.951056516295154,
1.,0.951056516295154,1.,0.951056516295154,1.,0.951056516295154,1.,0.951056516295154,
1.,0.951056516295154,1.,0.951056516295154,1.,0.951056516295154,1.,0.951056516295154,
1.,0.951056516295154,1.,0.951056516295154,1.,0.951056516295154,1.,0.951056516295154,
1.,0.951056516295154,1.,0.951056516295154,1.,0.951056516295154,1.,0.951056516295154,
1.,0.951056516295154,1.,0.951056516295154,1.,0.951056516295154,1.,0.951056516295154,
1.,0.951056516295154,1.,0.951056516295154,1.,0.951056516295154,1.,0.951056516295154,
1.,0.951056516295154,1.,0.951056516295154,1.,0.951056516295154,1.,0.951056516295154,
1.,0.951056516295154,1.,0.951056516295154,1.,0.951056516295154,1.,0.951056516295154,
1.,0.951056516295154,1.,0.951056516295154,1.,0.951056516295154,1.,0.951056516295154,
1.,0.951056516295154,1.,0.951056516295154,1.,0.951056516295154,1.,0.951056516295154,
1.,0.951056516295154,1.,0.951056516295154,1.,0.951056516295154,1.,0.951056516295154,
1.,0.951056516295154,1.,0.951056516295154,1.,0.951056516295154,1.,0.951056516295154,
1.,0.951056516295154,1.,0.951056516295154,1.,0.951056516295154,1.,0.951056516295154,
1.,0.951056516295154,1.,0.951056516295154,1.,0.951056516295154,1.,0.951056516295154,
1.,0.951056516295154,1.,0.951056516295154,1.,0.951056516295154,1.,0.951056516295154,
1.,0.951056516295154,1.,0.951056516295154,1.,0.951056516295154,1.,0.951056516295154,
1.,0.951056516295154,1.,0.951056516295154,1.,0.951056516295154,1.,0.951056516295154,
1.,0.951056516295154,1.,0.951056516295154,1.,0.951056516295154,1.,0.951056516295154,
1.,0.951056516295154,1.,0.951056516295154,1.,0.951056516295154,1.,0.951056516295154,
1.,0.951056516295154,1.,0.951056516295154,1.,0.973808338199829,0.975649137349576,
0.975649137349576,0.975649137349576)))
REPRESENTATION_ITEM('')
SURFACE()
);
#300=(
BOUNDED_SURFACE()
B_SPLINE_SURFACE(1,2,((#27453,#27454,#27455,#27456,#27457,#27458,#27459,
#27460,#27461,#27462,#27463,#27464,#27465,#27466,#27467,#27468,#27469,#27470,
#27471,#27472,#27473,#27474,#27475,#27476,#27477,#27478,#27479,#27480,#27481,
#27482,#27483,#27484,#27485,#27486,#27487,#27488,#27489,#27490,#27491,#27492,
#27493,#27494,#27495,#27496,#27497,#27498,#27499,#27500,#27501,#27502,#27503,
#27504,#27505,#27506,#27507,#27508,#27509,#27510,#27511,#27512,#27513,#27514,
#27515,#27516,#27517,#27518,#27519,#27520,#27521,#27522,#27523,#27524,#27525,
#27526,#27527,#27528,#27529,#27530,#27531,#27532,#27533,#27534,#27535,#27536,
#27537,#27538,#27539,#27540,#27541,#27542,#27543,#27544,#27545,#27546,#27547,
#27548,#27549,#27550,#27551,#27552,#27553,#27554,#27555,#27556,#27557,#27558,
#27559,#27560,#27561,#27562,#27563,#27564,#27565,#27566,#27567,#27568,#27569,
#27570,#27571,#27572,#27573,#27574,#27575,#27576,#27577,#27578,#27579,#27580,
#27581,#27582,#27583,#27584,#27585,#27586,#27587,#27588,#27589,#27590,#27591,
#27592,#27593,#27594,#27595,#27596,#27597,#27598,#27599,#27600,#27601,#27602,
#27603,#27604,#27605,#27606,#27607,#27608,#27609,#27610,#27611,#27612,#27613,
#27614,#27615,#27616,#27617,#27618,#27619,#27620,#27621,#27622,#27623,#27624,
#27625,#27626,#27627,#27628,#27629,#27630,#27631,#27632,#27633,#27634,#27635,
#27636,#27637,#27638,#27639,#27640,#27641,#27642,#27643,#27644,#27645,#27646,
#27647,#27648,#27649,#27650,#27651,#27652,#27653,#27654,#27655,#27656,#27657,
#27658,#27659,#27660,#27661,#27662,#27663,#27664,#27665,#27666,#27667,#27668,
#27669,#27670,#27671,#27672,#27673,#27674,#27675,#27676,#27677,#27678,#27679,
#27680,#27681,#27682,#27683,#27684,#27685,#27686,#27687,#27688,#27689,#27690,
#27691,#27692,#27693,#27694,#27695,#27696,#27697,#27698,#27699,#27700,#27701,
#27702,#27703,#27704,#27705,#27706,#27707,#27708,#27709,#27710,#27711,#27712,
#27713,#27714,#27715,#27716,#27717,#27718,#27719,#27720,#27721,#27722,#27723,
#27724,#27725,#27726,#27727,#27728,#27729,#27730,#27731,#27732,#27733,#27734,
#27735,#27736,#27737,#27738,#27739,#27740,#27741,#27742,#27743,#27744,#27745,
#27746,#27747,#27748,#27749,#27750,#27751,#27752,#27753,#27754,#27755,#27756,
#27757,#27758,#27759,#27760,#27761,#27762,#27763,#27764,#27765,#27766,#27767,
#27768,#27769,#27770,#27771,#27772,#27773,#27774,#27775,#27776,#27777,#27778,
#27779,#27780,#27781,#27782,#27783,#27784,#27785,#27786,#27787,#27788,#27789,
#27790,#27791,#27792,#27793,#27794,#27795,#27796,#27797,#27798,#27799,#27800,
#27801,#27802,#27803,#27804,#27805,#27806,#27807,#27808,#27809,#27810,#27811,
#27812,#27813,#27814,#27815,#27816,#27817,#27818,#27819,#27820,#27821,#27822,
#27823,#27824,#27825,#27826,#27827,#27828,#27829,#27830,#27831,#27832,#27833,
#27834,#27835,#27836,#27837,#27838,#27839,#27840,#27841,#27842,#27843,#27844,
#27845,#27846,#27847,#27848,#27849,#27850,#27851,#27852,#27853,#27854,#27855,
#27856,#27857,#27858,#27859,#27860,#27861,#27862,#27863,#27864,#27865,#27866,
#27867,#27868,#27869,#27870,#27871,#27872,#27873,#27874,#27875,#27876,#27877,
#27878,#27879,#27880,#27881,#27882,#27883,#27884,#27885,#27886,#27887),
(#27888,#27889,#27890,#27891,#27892,#27893,#27894,#27895,#27896,#27897,
#27898,#27899,#27900,#27901,#27902,#27903,#27904,#27905,#27906,#27907,#27908,
#27909,#27910,#27911,#27912,#27913,#27914,#27915,#27916,#27917,#27918,#27919,
#27920,#27921,#27922,#27923,#27924,#27925,#27926,#27927,#27928,#27929,#27930,
#27931,#27932,#27933,#27934,#27935,#27936,#27937,#27938,#27939,#27940,#27941,
#27942,#27943,#27944,#27945,#27946,#27947,#27948,#27949,#27950,#27951,#27952,
#27953,#27954,#27955,#27956,#27957,#27958,#27959,#27960,#27961,#27962,#27963,
#27964,#27965,#27966,#27967,#27968,#27969,#27970,#27971,#27972,#27973,#27974,
#27975,#27976,#27977,#27978,#27979,#27980,#27981,#27982,#27983,#27984,#27985,
#27986,#27987,#27988,#27989,#27990,#27991,#27992,#27993,#27994,#27995,#27996,
#27997,#27998,#27999,#28000,#28001,#28002,#28003,#28004,#28005,#28006,#28007,
#28008,#28009,#28010,#28011,#28012,#28013,#28014,#28015,#28016,#28017,#28018,
#28019,#28020,#28021,#28022,#28023,#28024,#28025,#28026,#28027,#28028,#28029,
#28030,#28031,#28032,#28033,#28034,#28035,#28036,#28037,#28038,#28039,#28040,
#28041,#28042,#28043,#28044,#28045,#28046,#28047,#28048,#28049,#28050,#28051,
#28052,#28053,#28054,#28055,#28056,#28057,#28058,#28059,#28060,#28061,#28062,
#28063,#28064,#28065,#28066,#28067,#28068,#28069,#28070,#28071,#28072,#28073,
#28074,#28075,#28076,#28077,#28078,#28079,#28080,#28081,#28082,#28083,#28084,
#28085,#28086,#28087,#28088,#28089,#28090,#28091,#28092,#28093,#28094,#28095,
#28096,#28097,#28098,#28099,#28100,#28101,#28102,#28103,#28104,#28105,#28106,
#28107,#28108,#28109,#28110,#28111,#28112,#28113,#28114,#28115,#28116,#28117,
#28118,#28119,#28120,#28121,#28122,#28123,#28124,#28125,#28126,#28127,#28128,
#28129,#28130,#28131,#28132,#28133,#28134,#28135,#28136,#28137,#28138,#28139,
#28140,#28141,#28142,#28143,#28144,#28145,#28146,#28147,#28148,#28149,#28150,
#28151,#28152,#28153,#28154,#28155,#28156,#28157,#28158,#28159,#28160,#28161,
#28162,#28163,#28164,#28165,#28166,#28167,#28168,#28169,#28170,#28171,#28172,
#28173,#28174,#28175,#28176,#28177,#28178,#28179,#28180,#28181,#28182,#28183,
#28184,#28185,#28186,#28187,#28188,#28189,#28190,#28191,#28192,#28193,#28194,
#28195,#28196,#28197,#28198,#28199,#28200,#28201,#28202,#28203,#28204,#28205,
#28206,#28207,#28208,#28209,#28210,#28211,#28212,#28213,#28214,#28215,#28216,
#28217,#28218,#28219,#28220,#28221,#28222,#28223,#28224,#28225,#28226,#28227,
#28228,#28229,#28230,#28231,#28232,#28233,#28234,#28235,#28236,#28237,#28238,
#28239,#28240,#28241,#28242,#28243,#28244,#28245,#28246,#28247,#28248,#28249,
#28250,#28251,#28252,#28253,#28254,#28255,#28256,#28257,#28258,#28259,#28260,
#28261,#28262,#28263,#28264,#28265,#28266,#28267,#28268,#28269,#28270,#28271,
#28272,#28273,#28274,#28275,#28276,#28277,#28278,#28279,#28280,#28281,#28282,
#28283,#28284,#28285,#28286,#28287,#28288,#28289,#28290,#28291,#28292,#28293,
#28294,#28295,#28296,#28297,#28298,#28299,#28300,#28301,#28302,#28303,#28304,
#28305,#28306,#28307,#28308,#28309,#28310,#28311,#28312,#28313,#28314,#28315,
#28316,#28317,#28318,#28319,#28320,#28321,#28322)),.UNSPECIFIED.,.F.,.F.,
 .F.)
B_SPLINE_SURFACE_WITH_KNOTS((2,2),(3,2,2,2,2,2,2,2,2,2,2,2,2,2,2,2,2,2,
2,2,2,2,2,2,2,2,2,2,2,2,2,2,2,2,2,2,2,2,2,2,2,2,2,2,2,2,2,2,2,2,2,2,2,2,
2,2,2,2,2,2,2,2,2,2,2,2,2,2,2,2,2,2,2,2,2,2,2,2,2,2,2,2,2,2,2,2,2,2,2,2,
2,2,2,2,2,2,2,2,2,2,2,2,2,2,2,2,2,2,2,2,2,2,2,2,2,2,2,2,2,2,2,2,2,2,2,2,
2,2,2,2,2,2,2,2,2,2,2,2,2,2,2,2,2,2,2,2,2,2,2,2,2,2,2,2,2,2,2,2,2,2,2,2,
2,2,2,2,2,2,2,2,2,2,2,2,2,2,2,2,2,2,2,2,2,2,2,2,2,2,2,2,2,2,2,2,2,2,2,2,
2,2,2,2,2,2,2,2,2,2,2,2,2,2,2,2,2,2,2,3),(0.,1.),(0.,0.00454545454545455,
0.00909090909090909,0.0136363636363636,0.0181818181818182,0.0227272727272727,
0.0272727272727273,0.0318181818181818,0.0363636363636364,0.0409090909090909,
0.0454545454545455,0.05,0.0545454545454545,0.0590909090909091,0.0636363636363636,
0.0681818181818182,0.0727272727272727,0.0772727272727273,0.0818181818181818,
0.0863636363636364,0.0909090909090909,0.0954545454545455,0.1,0.104545454545455,
0.109090909090909,0.113636363636364,0.118181818181818,0.122727272727273,
0.127272727272727,0.131818181818182,0.136363636363636,0.140909090909091,
0.145454545454545,0.15,0.154545454545455,0.159090909090909,0.163636363636364,
0.168181818181818,0.172727272727273,0.177272727272727,0.181818181818182,
0.186363636363636,0.190909090909091,0.195454545454545,0.2,0.204545454545455,
0.209090909090909,0.213636363636364,0.218181818181818,0.222727272727273,
0.227272727272727,0.231818181818182,0.236363636363636,0.240909090909091,
0.245454545454545,0.25,0.254545454545455,0.259090909090909,0.263636363636364,
0.268181818181818,0.272727272727273,0.277272727272727,0.281818181818182,
0.286363636363636,0.290909090909091,0.295454545454545,0.3,0.304545454545455,
0.309090909090909,0.313636363636364,0.318181818181818,0.322727272727273,
0.327272727272727,0.331818181818182,0.336363636363636,0.340909090909091,
0.345454545454545,0.35,0.354545454545455,0.359090909090909,0.363636363636364,
0.368181818181818,0.372727272727273,0.377272727272727,0.381818181818182,
0.386363636363636,0.390909090909091,0.395454545454545,0.4,0.404545454545455,
0.409090909090909,0.413636363636364,0.418181818181818,0.422727272727273,
0.427272727272727,0.431818181818182,0.436363636363636,0.440909090909091,
0.445454545454545,0.45,0.454545454545455,0.459090909090909,0.463636363636364,
0.468181818181818,0.472727272727273,0.477272727272727,0.481818181818182,
0.486363636363636,0.490909090909091,0.495454545454545,0.5,0.504545454545455,
0.509090909090909,0.513636363636364,0.518181818181818,0.522727272727273,
0.527272727272727,0.531818181818182,0.536363636363636,0.540909090909091,
0.545454545454545,0.55,0.554545454545455,0.559090909090909,0.563636363636364,
0.568181818181818,0.572727272727273,0.577272727272727,0.581818181818182,
0.586363636363636,0.590909090909091,0.595454545454545,0.6,0.604545454545454,
0.609090909090909,0.613636363636364,0.618181818181818,0.622727272727273,
0.627272727272727,0.631818181818182,0.636363636363636,0.640909090909091,
0.645454545454546,0.65,0.654545454545455,0.659090909090909,0.663636363636364,
0.668181818181818,0.672727272727273,0.677272727272727,0.681818181818182,
0.686363636363636,0.690909090909091,0.695454545454545,0.7,0.704545454545455,
0.709090909090909,0.713636363636364,0.718181818181818,0.722727272727273,
0.727272727272727,0.731818181818182,0.736363636363636,0.740909090909091,
0.745454545454545,0.75,0.754545454545455,0.759090909090909,0.763636363636364,
0.768181818181818,0.772727272727273,0.777272727272727,0.781818181818182,
0.786363636363636,0.790909090909091,0.795454545454545,0.8,0.804545454545455,
0.809090909090909,0.813636363636364,0.818181818181818,0.822727272727273,
0.827272727272727,0.831818181818182,0.836363636363636,0.840909090909091,
0.845454545454545,0.85,0.854545454545454,0.859090909090909,0.863636363636364,
0.868181818181818,0.872727272727273,0.877272727272727,0.881818181818182,
0.886363636363636,0.890909090909091,0.895454545454546,0.9,0.904545454545455,
0.909090909090909,0.913636363636364,0.918181818181818,0.922727272727273,
0.927272727272727,0.931818181818182,0.936363636363636,0.940909090909091,
0.945454545454545,0.95,0.954545454545455,0.959090909090909,0.963636363636364,
0.968181818181818,0.972727272727273,0.977272727272727,0.981818181818182,
0.984250643037892),.UNSPECIFIED.)
GEOMETRIC_REPRESENTATION_ITEM()
RATIONAL_B_SPLINE_SURFACE(((1.,0.951056516295154,1.,0.951056516295154,1.,
0.951056516295154,1.,0.951056516295154,1.,0.951056516295154,1.,0.951056516295154,
1.,0.951056516295154,1.,0.951056516295154,1.,0.951056516295154,1.,0.951056516295154,
1.,0.951056516295154,1.,0.951056516295154,1.,0.951056516295154,1.,0.951056516295154,
1.,0.951056516295154,1.,0.951056516295154,1.,0.951056516295154,1.,0.951056516295154,
1.,0.951056516295154,1.,0.951056516295154,1.,0.951056516295154,1.,0.951056516295154,
1.,0.951056516295154,1.,0.951056516295154,1.,0.951056516295154,1.,0.951056516295154,
1.,0.951056516295154,1.,0.951056516295154,1.,0.951056516295154,1.,0.951056516295154,
1.,0.951056516295154,1.,0.951056516295154,1.,0.951056516295154,1.,0.951056516295154,
1.,0.951056516295154,1.,0.951056516295154,1.,0.951056516295154,1.,0.951056516295154,
1.,0.951056516295154,1.,0.951056516295154,1.,0.951056516295154,1.,0.951056516295154,
1.,0.951056516295154,1.,0.951056516295154,1.,0.951056516295154,1.,0.951056516295154,
1.,0.951056516295154,1.,0.951056516295154,1.,0.951056516295154,1.,0.951056516295154,
1.,0.951056516295154,1.,0.951056516295154,1.,0.951056516295154,1.,0.951056516295154,
1.,0.951056516295154,1.,0.951056516295154,1.,0.951056516295154,1.,0.951056516295154,
1.,0.951056516295154,1.,0.951056516295154,1.,0.951056516295154,1.,0.951056516295154,
1.,0.951056516295154,1.,0.951056516295154,1.,0.951056516295154,1.,0.951056516295154,
1.,0.951056516295154,1.,0.951056516295154,1.,0.951056516295154,1.,0.951056516295154,
1.,0.951056516295154,1.,0.951056516295154,1.,0.951056516295154,1.,0.951056516295154,
1.,0.951056516295154,1.,0.951056516295154,1.,0.951056516295154,1.,0.951056516295154,
1.,0.951056516295154,1.,0.951056516295154,1.,0.951056516295154,1.,0.951056516295154,
1.,0.951056516295154,1.,0.951056516295154,1.,0.951056516295154,1.,0.951056516295154,
1.,0.951056516295154,1.,0.951056516295154,1.,0.951056516295154,1.,0.951056516295154,
1.,0.951056516295154,1.,0.951056516295154,1.,0.951056516295154,1.,0.951056516295154,
1.,0.951056516295154,1.,0.951056516295154,1.,0.951056516295154,1.,0.951056516295154,
1.,0.951056516295154,1.,0.951056516295154,1.,0.951056516295154,1.,0.951056516295154,
1.,0.951056516295154,1.,0.951056516295154,1.,0.951056516295154,1.,0.951056516295154,
1.,0.951056516295154,1.,0.951056516295154,1.,0.951056516295154,1.,0.951056516295154,
1.,0.951056516295154,1.,0.951056516295154,1.,0.951056516295154,1.,0.951056516295154,
1.,0.951056516295154,1.,0.951056516295154,1.,0.951056516295154,1.,0.951056516295154,
1.,0.951056516295154,1.,0.951056516295154,1.,0.951056516295154,1.,0.951056516295154,
1.,0.951056516295154,1.,0.951056516295154,1.,0.951056516295154,1.,0.951056516295154,
1.,0.951056516295154,1.,0.951056516295154,1.,0.951056516295154,1.,0.951056516295154,
1.,0.951056516295154,1.,0.951056516295154,1.,0.951056516295154,1.,0.951056516295154,
1.,0.951056516295154,1.,0.951056516295154,1.,0.951056516295154,1.,0.951056516295154,
1.,0.951056516295154,1.,0.951056516295154,1.,0.951056516295154,1.,0.951056516295154,
1.,0.951056516295154,1.,0.951056516295154,1.,0.951056516295154,1.,0.951056516295154,
1.,0.951056516295154,1.,0.951056516295154,1.,0.951056516295154,1.,0.951056516295154,
1.,0.951056516295154,1.,0.951056516295154,1.,0.951056516295154,1.,0.951056516295154,
1.,0.951056516295154,1.,0.951056516295154,1.,0.951056516295154,1.,0.951056516295154,
1.,0.951056516295154,1.,0.951056516295154,1.,0.951056516295154,1.,0.951056516295154,
1.,0.951056516295154,1.,0.951056516295154,1.,0.951056516295154,1.,0.951056516295154,
1.,0.951056516295154,1.,0.951056516295154,1.,0.951056516295154,1.,0.951056516295154,
1.,0.951056516295154,1.,0.951056516295154,1.,0.951056516295154,1.,0.951056516295154,
1.,0.951056516295154,1.,0.951056516295154,1.,0.951056516295154,1.,0.951056516295154,
1.,0.951056516295154,1.,0.951056516295154,1.,0.951056516295154,1.,0.951056516295154,
1.,0.951056516295154,1.,0.951056516295154,1.,0.951056516295154,1.,0.951056516295154,
1.,0.951056516295154,1.,0.951056516295154,1.,0.951056516295154,1.,0.951056516295154,
1.,0.951056516295154,1.,0.951056516295154,1.,0.951056516295154,1.,0.951056516295154,
1.,0.951056516295154,1.,0.951056516295154,1.,0.951056516295154,1.,0.951056516295154,
1.,0.951056516295154,1.,0.951056516295154,1.,0.951056516295154,1.,0.951056516295154,
1.,0.951056516295154,1.,0.951056516295154,1.,0.951056516295154,1.,0.951056516295154,
1.,0.951056516295154,1.,0.951056516295154,1.,0.951056516295154,1.,0.951056516295154,
1.,0.951056516295154,1.,0.951056516295154,1.,0.951056516295154,1.,0.951056516295154,
1.,0.951056516295154,1.,0.951056516295154,1.,0.973808312264696,0.975649140995143),
(1.,0.951056516295154,1.,0.951056516295154,1.,0.951056516295154,1.,0.951056516295154,
1.,0.951056516295154,1.,0.951056516295154,1.,0.951056516295154,1.,0.951056516295154,
1.,0.951056516295154,1.,0.951056516295154,1.,0.951056516295154,1.,0.951056516295154,
1.,0.951056516295154,1.,0.951056516295154,1.,0.951056516295154,1.,0.951056516295154,
1.,0.951056516295154,1.,0.951056516295154,1.,0.951056516295154,1.,0.951056516295154,
1.,0.951056516295154,1.,0.951056516295154,1.,0.951056516295154,1.,0.951056516295154,
1.,0.951056516295154,1.,0.951056516295154,1.,0.951056516295154,1.,0.951056516295154,
1.,0.951056516295154,1.,0.951056516295154,1.,0.951056516295154,1.,0.951056516295154,
1.,0.951056516295154,1.,0.951056516295154,1.,0.951056516295154,1.,0.951056516295154,
1.,0.951056516295154,1.,0.951056516295154,1.,0.951056516295154,1.,0.951056516295154,
1.,0.951056516295154,1.,0.951056516295154,1.,0.951056516295154,1.,0.951056516295154,
1.,0.951056516295154,1.,0.951056516295154,1.,0.951056516295154,1.,0.951056516295154,
1.,0.951056516295154,1.,0.951056516295154,1.,0.951056516295154,1.,0.951056516295154,
1.,0.951056516295154,1.,0.951056516295154,1.,0.951056516295154,1.,0.951056516295154,
1.,0.951056516295154,1.,0.951056516295154,1.,0.951056516295154,1.,0.951056516295154,
1.,0.951056516295154,1.,0.951056516295154,1.,0.951056516295154,1.,0.951056516295154,
1.,0.951056516295154,1.,0.951056516295154,1.,0.951056516295154,1.,0.951056516295154,
1.,0.951056516295154,1.,0.951056516295154,1.,0.951056516295154,1.,0.951056516295154,
1.,0.951056516295154,1.,0.951056516295154,1.,0.951056516295154,1.,0.951056516295154,
1.,0.951056516295154,1.,0.951056516295154,1.,0.951056516295154,1.,0.951056516295154,
1.,0.951056516295154,1.,0.951056516295154,1.,0.951056516295154,1.,0.951056516295154,
1.,0.951056516295154,1.,0.951056516295154,1.,0.951056516295154,1.,0.951056516295154,
1.,0.951056516295154,1.,0.951056516295154,1.,0.951056516295154,1.,0.951056516295154,
1.,0.951056516295154,1.,0.951056516295154,1.,0.951056516295154,1.,0.951056516295154,
1.,0.951056516295154,1.,0.951056516295154,1.,0.951056516295154,1.,0.951056516295154,
1.,0.951056516295154,1.,0.951056516295154,1.,0.951056516295154,1.,0.951056516295154,
1.,0.951056516295154,1.,0.951056516295154,1.,0.951056516295154,1.,0.951056516295154,
1.,0.951056516295154,1.,0.951056516295154,1.,0.951056516295154,1.,0.951056516295154,
1.,0.951056516295154,1.,0.951056516295154,1.,0.951056516295154,1.,0.951056516295154,
1.,0.951056516295154,1.,0.951056516295154,1.,0.951056516295154,1.,0.951056516295154,
1.,0.951056516295154,1.,0.951056516295154,1.,0.951056516295154,1.,0.951056516295154,
1.,0.951056516295154,1.,0.951056516295154,1.,0.951056516295154,1.,0.951056516295154,
1.,0.951056516295154,1.,0.951056516295154,1.,0.951056516295154,1.,0.951056516295154,
1.,0.951056516295154,1.,0.951056516295154,1.,0.951056516295154,1.,0.951056516295154,
1.,0.951056516295154,1.,0.951056516295154,1.,0.951056516295154,1.,0.951056516295154,
1.,0.951056516295154,1.,0.951056516295154,1.,0.951056516295154,1.,0.951056516295154,
1.,0.951056516295154,1.,0.951056516295154,1.,0.951056516295154,1.,0.951056516295154,
1.,0.951056516295154,1.,0.951056516295154,1.,0.951056516295154,1.,0.951056516295154,
1.,0.951056516295154,1.,0.951056516295154,1.,0.951056516295154,1.,0.951056516295154,
1.,0.951056516295154,1.,0.951056516295154,1.,0.951056516295154,1.,0.951056516295154,
1.,0.951056516295154,1.,0.951056516295154,1.,0.951056516295154,1.,0.951056516295154,
1.,0.951056516295154,1.,0.951056516295154,1.,0.951056516295154,1.,0.951056516295154,
1.,0.951056516295154,1.,0.951056516295154,1.,0.951056516295154,1.,0.951056516295154,
1.,0.951056516295154,1.,0.951056516295154,1.,0.951056516295154,1.,0.951056516295154,
1.,0.951056516295154,1.,0.951056516295154,1.,0.951056516295154,1.,0.951056516295154,
1.,0.951056516295154,1.,0.951056516295154,1.,0.951056516295154,1.,0.951056516295154,
1.,0.951056516295154,1.,0.951056516295154,1.,0.951056516295154,1.,0.951056516295154,
1.,0.951056516295154,1.,0.951056516295154,1.,0.951056516295154,1.,0.951056516295154,
1.,0.951056516295154,1.,0.951056516295154,1.,0.951056516295154,1.,0.951056516295154,
1.,0.951056516295154,1.,0.951056516295154,1.,0.951056516295154,1.,0.951056516295154,
1.,0.951056516295154,1.,0.951056516295154,1.,0.951056516295154,1.,0.951056516295154,
1.,0.951056516295154,1.,0.951056516295154,1.,0.951056516295154,1.,0.951056516295154,
1.,0.951056516295154,1.,0.951056516295154,1.,0.951056516295154,1.,0.951056516295154,
1.,0.951056516295154,1.,0.951056516295154,1.,0.951056516295154,1.,0.951056516295154,
1.,0.973808312264696,0.975649140995143)))
REPRESENTATION_ITEM('')
SURFACE()
);
#301=(
BOUNDED_SURFACE()
B_SPLINE_SURFACE(3,2,((#28323,#28324,#28325),(#28326,#28327,#28328),(#28329,
#28330,#28331),(#28332,#28333,#28334),(#28335,#28336,#28337),(#28338,#28339,
#28340),(#28341,#28342,#28343),(#28344,#28345,#28346),(#28347,#28348,#28349),
(#28350,#28351,#28352)),.UNSPECIFIED.,.F.,.F.,.F.)
B_SPLINE_SURFACE_WITH_KNOTS((4,2,2,2,4),(3,3),(0.00398013717080998,0.00543136490531493,
0.00682381476862857,0.00821626463194221,0.00960871449525586),(0.4504813546384,
1.00005877787119),.UNSPECIFIED.)
GEOMETRIC_REPRESENTATION_ITEM()
RATIONAL_B_SPLINE_SURFACE(((0.876526511260875,0.862952378099386,1.00002931931674),
(0.896639296968354,0.885276275149306,1.00002454344832),(0.914408347469022,
0.904998777035469,1.00002032411003),(0.944823095920487,0.938757189375995,
1.00001310199577),(0.957749166091975,0.953104294941835,1.00001003264421),
(0.978422485020086,0.976050347773278,1.00000512367475),(0.986354320920379,
0.984854174882576,1.00000324022583),(0.997174546550185,0.9968639286049,
1.00000067091621),(1.00000968195182,1.00001074634309,0.999999997700978),
(1.,1.,1.)))
REPRESENTATION_ITEM('')
SURFACE()
);
#302=(
BOUNDED_SURFACE()
B_SPLINE_SURFACE(3,2,((#28365,#28366,#28367),(#28368,#28369,#28370),(#28371,
#28372,#28373),(#28374,#28375,#28376),(#28377,#28378,#28379),(#28380,#28381,
#28382),(#28383,#28384,#28385),(#28386,#28387,#28388),(#28389,#28390,#28391),
(#28392,#28393,#28394),(#28395,#28396,#28397),(#28398,#28399,#28400),(#28401,
#28402,#28403),(#28404,#28405,#28406),(#28407,#28408,#28409),(#28410,#28411,
#28412),(#28413,#28414,#28415),(#28416,#28417,#28418),(#28419,#28420,#28421),
(#28422,#28423,#28424),(#28425,#28426,#28427),(#28428,#28429,#28430),(#28431,
#28432,#28433),(#28434,#28435,#28436),(#28437,#28438,#28439),(#28440,#28441,
#28442),(#28443,#28444,#28445),(#28446,#28447,#28448),(#28449,#28450,#28451),
(#28452,#28453,#28454)),.UNSPECIFIED.,.F.,.F.,.F.)
B_SPLINE_SURFACE_WITH_KNOTS((4,2,2,2,2,2,2,2,2,2,2,2,2,2,4),(3,3),(0.,0.0023928943576613,
0.00358934153649195,0.0047857887153226,0.00598223589415325,0.0071786830729839,
0.0095715774306452,0.0101698010200605,0.0107680246094759,0.0119644717883065,
0.0131609189671372,0.0143573661459678,0.0155538133247985,0.0167502605036291,
0.0191431548612904),(0.,1.),.UNSPECIFIED.)
GEOMETRIC_REPRESENTATION_ITEM()
RATIONAL_B_SPLINE_SURFACE(((1.,0.755519678577116,1.),(1.,0.767712634757759,
1.),(1.,0.780608196095567,1.),(1.,0.79934306756545,1.),(1.,0.80552470893265,
1.),(1.,0.817270248347207,1.),(1.,0.822799993283502,1.),(1.,0.832991457849502,
1.),(1.,0.837654127549585,1.),(1.,0.845923910809236,1.),(1.,0.849550572374246,
1.),(1.,0.85828554581335,1.),(1.,0.861359462352663,1.),(1.,0.86139338043001,
1.),(1.,0.861206147953501,1.),(1.,0.860450812266049,1.),(1.,0.859884337138352,
1.),(1.,0.857640585891707,1.),(1.,0.855419731623233,1.),(1.,0.849623257971125,
1.),(1.,0.846014379835457,1.),(1.,0.837715224709792,1.),(1.,0.833033055512742,
1.),(1.,0.822797218586941,1.),(1.,0.817242571682893,1.),(1.,0.805445312247108,
1.),(1.,0.799306345600238,1.),(1.,0.780606551099107,1.),(1.,0.767720440554272,
1.),(1.,0.755519678577116,1.)))
REPRESENTATION_ITEM('')
SURFACE()
);
#303=(
BOUNDED_SURFACE()
B_SPLINE_SURFACE(3,2,((#28549,#28550,#28551),(#28552,#28553,#28554),(#28555,
#28556,#28557),(#28558,#28559,#28560),(#28561,#28562,#28563),(#28564,#28565,
#28566),(#28567,#28568,#28569),(#28570,#28571,#28572),(#28573,#28574,#28575),
(#28576,#28577,#28578)),.UNSPECIFIED.,.F.,.F.,.F.)
B_SPLINE_SURFACE_WITH_KNOTS((4,2,2,2,4),(3,3),(0.00398006295905424,0.00543136490531495,
0.0068238147686286,0.00821626463194225,0.0096087144952559),(-5.88520829470716E-5,
0.549518434171745),.UNSPECIFIED.)
GEOMETRIC_REPRESENTATION_ITEM()
RATIONAL_B_SPLINE_SURFACE(((1.0000293570705,0.862949004176479,0.876523415273787),
(1.00002457487029,0.885274300596315,0.896637470909482),(1.00002034996106,
0.904997931282859,0.914407546500262),(1.00001311853906,0.938757212096139,
0.944823091258541),(1.00001004531197,0.953104312339345,0.957749162522093),
(1.00000513014418,0.976050356658273,0.978422483197019),(1.00000324431711,
0.984854180501291,0.986354319767304),(1.00000067176334,0.996863929768465,
0.997174546311578),(0.999999997698076,1.00001074633898,1.00000968195253),
(1.,1.,1.)))
REPRESENTATION_ITEM('')
SURFACE()
);
#304=(
BOUNDED_SURFACE()
B_SPLINE_SURFACE(3,2,((#28591,#28592,#28593),(#28594,#28595,#28596),(#28597,
#28598,#28599),(#28600,#28601,#28602),(#28603,#28604,#28605),(#28606,#28607,
#28608),(#28609,#28610,#28611),(#28612,#28613,#28614),(#28615,#28616,#28617),
(#28618,#28619,#28620)),.UNSPECIFIED.,.F.,.F.,.F.)
B_SPLINE_SURFACE_WITH_KNOTS((4,2,2,2,4),(3,3),(0.00398013717069273,0.00543136490531495,
0.00682381476862858,0.0082162646319422,0.00960871449525583),(0.450481354362641,
1.00005877787131),.UNSPECIFIED.)
GEOMETRIC_REPRESENTATION_ITEM()
RATIONAL_B_SPLINE_SURFACE(((0.8765265112696,0.862952378025167,1.00002931931679),
(0.896639296976939,0.885276275088599,1.00002454344837),(0.91440834747712,
0.904998776986295,1.00002032411007),(0.944823095926639,0.938757189345328,
1.0000131019958),(0.957749166096613,0.953104294918273,1.00001003264423),
(0.978422485022468,0.97605034776126,1.00000512367476),(0.986354320921773,
0.984854174874851,1.00000324022583),(0.997174546550589,0.996863928603428,
1.00000067091621),(1.00000968195173,1.00001074634299,0.999999997700978),
(1.,1.,1.)))
REPRESENTATION_ITEM('')
SURFACE()
);
#305=(
BOUNDED_SURFACE()
B_SPLINE_SURFACE(3,2,((#28633,#28634,#28635),(#28636,#28637,#28638),(#28639,
#28640,#28641),(#28642,#28643,#28644),(#28645,#28646,#28647),(#28648,#28649,
#28650),(#28651,#28652,#28653),(#28654,#28655,#28656),(#28657,#28658,#28659),
(#28660,#28661,#28662),(#28663,#28664,#28665),(#28666,#28667,#28668),(#28669,
#28670,#28671),(#28672,#28673,#28674),(#28675,#28676,#28677),(#28678,#28679,
#28680),(#28681,#28682,#28683),(#28684,#28685,#28686),(#28687,#28688,#28689),
(#28690,#28691,#28692),(#28693,#28694,#28695),(#28696,#28697,#28698),(#28699,
#28700,#28701),(#28702,#28703,#28704),(#28705,#28706,#28707),(#28708,#28709,
#28710),(#28711,#28712,#28713),(#28714,#28715,#28716),(#28717,#28718,#28719),
(#28720,#28721,#28722)),.UNSPECIFIED.,.F.,.F.,.F.)
B_SPLINE_SURFACE_WITH_KNOTS((4,2,2,2,2,2,2,2,2,2,2,2,2,2,4),(3,3),(0.,0.00239289435766131,
0.00358934153649196,0.00478578871532262,0.00598223589415327,0.00717868307298392,
0.00957157743064523,0.0101698010200606,0.0107680246094759,0.0119644717883065,
0.0131609189671372,0.0143573661459678,0.0155538133247985,0.0167502605036292,
0.0191431548612905),(0.,1.),.UNSPECIFIED.)
GEOMETRIC_REPRESENTATION_ITEM()
RATIONAL_B_SPLINE_SURFACE(((1.,0.755519678577118,1.),(1.,0.767712634757661,
1.),(1.,0.780608196095702,1.),(1.,0.799343067565385,1.),(1.,0.805524708932718,
1.),(1.,0.817270248347141,1.),(1.,0.822799993283503,1.),(1.,0.832991457849504,
1.),(1.,0.837654127549563,1.),(1.,0.845923910809259,1.),(1.,0.849550572374269,
1.),(1.,0.858285545813306,1.),(1.,0.861359462352663,1.),(1.,0.86139338043001,
1.),(1.,0.861206147953501,1.),(1.,0.860450812266049,1.),(1.,0.859884337138363,
1.),(1.,0.857640585891685,1.),(1.,0.8554197316233,1.),(1.,0.849623257971058,
1.),(1.,0.84601437983548,1.),(1.,0.837715224709771,1.),(1.,0.833033055512787,
1.),(1.,0.822797218586897,1.),(1.,0.817242571682917,1.),(1.,0.805445312247087,
1.),(1.,0.799306345600284,1.),(1.,0.780606551099021,1.),(1.,0.767720440554341,
1.),(1.,0.755519678577118,1.)))
REPRESENTATION_ITEM('')
SURFACE()
);
#306=(
BOUNDED_SURFACE()
B_SPLINE_SURFACE(3,2,((#28817,#28818,#28819),(#28820,#28821,#28822),(#28823,
#28824,#28825),(#28826,#28827,#28828),(#28829,#28830,#28831),(#28832,#28833,
#28834),(#28835,#28836,#28837),(#28838,#28839,#28840),(#28841,#28842,#28843),
(#28844,#28845,#28846)),.UNSPECIFIED.,.F.,.F.,.F.)
B_SPLINE_SURFACE_WITH_KNOTS((4,2,2,2,4),(3,3),(0.00398006295938679,0.00543136490531494,
0.00682381476862857,0.0082162646319422,0.00960871449525583),(-5.88520826145246E-5,
0.549518433842917),.UNSPECIFIED.)
GEOMETRIC_REPRESENTATION_ITEM()
RATIONAL_B_SPLINE_SURFACE(((1.00002935707033,0.862949004273862,0.876523415271378),
(1.00002457487015,0.885274300673986,0.896637470903998),(1.00002034996095,
0.904997931343717,0.914407546492603),(1.00001311853899,0.938757212132757,
0.944823091251248),(1.00001004531191,0.953104312367488,0.957749162516602),
(1.00000513014415,0.976050356672542,0.978422483194122),(1.00000324431709,
0.984854180510462,0.986354319765605),(1.00000067176334,0.996863929770251,
0.997174546311125),(0.999999997698075,1.00001074633906,1.00000968195261),
(1.,1.,1.)))
REPRESENTATION_ITEM('')
SURFACE()
);
#307=(
BOUNDED_SURFACE()
B_SPLINE_SURFACE(3,2,((#28859,#28860,#28861),(#28862,#28863,#28864),(#28865,
#28866,#28867),(#28868,#28869,#28870),(#28871,#28872,#28873),(#28874,#28875,
#28876),(#28877,#28878,#28879),(#28880,#28881,#28882),(#28883,#28884,#28885),
(#28886,#28887,#28888),(#28889,#28890,#28891),(#28892,#28893,#28894),(#28895,
#28896,#28897),(#28898,#28899,#28900),(#28901,#28902,#28903),(#28904,#28905,
#28906)),.UNSPECIFIED.,.F.,.F.,.F.)
B_SPLINE_SURFACE_WITH_KNOTS((4,2,2,2,2,2,2,4),(3,3),(-0.000112562685732122,
0.000183317511890047,0.000366635023783252,0.000733270047569662,0.00109990507135607,
0.00146654009514248,0.0021998101427153,0.00293308019028812),(0.,1.00011256268573),
 .UNSPECIFIED.)
GEOMETRIC_REPRESENTATION_ITEM()
RATIONAL_B_SPLINE_SURFACE(((1.,0.888568848431313,1.00002508597939),(1.,
0.914720098615804,1.00001919866948),(1.,0.926614357760784,1.00001652096997),
(1.,0.941497644191807,1.00001317036458),(1.,0.945991617994044,1.00001215865706),
(1.,0.957827766219728,1.00000949403979),(1.,0.963503346961192,1.00000821632257),
(1.,0.973100607067783,1.00000605573583),(1.,0.976922506379337,1.00000519532932),
(1.,0.983418125950154,1.00000373300055),(1.,0.986078267870898,1.00000313413512),
(1.,0.992789809396114,1.00000162319684),(1.,0.995607448637691,1.00000098887476),
(1.,0.99922902552814,1.00000017356591),(1.,0.999994157715377,1.00000000131525),
(1.,1.,1.)))
REPRESENTATION_ITEM('')
SURFACE()
);
#308=(
BOUNDED_SURFACE()
B_SPLINE_SURFACE(3,2,((#28908,#28909,#28910),(#28911,#28912,#28913),(#28914,
#28915,#28916),(#28917,#28918,#28919),(#28920,#28921,#28922),(#28923,#28924,
#28925)),.UNSPECIFIED.,.F.,.F.,.F.)
B_SPLINE_SURFACE_WITH_KNOTS((4,2,4),(3,3),(-2.51534904016637E-17,0.00233940766482981,
0.00467881532965964),(0.,1.),.UNSPECIFIED.)
GEOMETRIC_REPRESENTATION_ITEM()
RATIONAL_B_SPLINE_SURFACE(((1.,0.707106781186545,1.),(1.,0.737898683933714,
1.),(1.,0.772355112026995,1.),(1.,0.844136160947679,1.),(1.,0.88073843286887,
1.),(1.,0.912870929175271,1.)))
REPRESENTATION_ITEM('')
SURFACE()
);
#309=(
BOUNDED_SURFACE()
B_SPLINE_SURFACE(3,2,((#28926,#28927,#28928),(#28929,#28930,#28931),(#28932,
#28933,#28934),(#28935,#28936,#28937),(#28938,#28939,#28940),(#28941,#28942,
#28943),(#28944,#28945,#28946),(#28947,#28948,#28949)),.UNSPECIFIED.,.F.,
 .F.,.F.)
B_SPLINE_SURFACE_WITH_KNOTS((4,2,2,4),(3,3),(-6.98226199080665E-17,0.00233568752491197,
0.00350353128736798,0.004671375049824),(0.,1.),.UNSPECIFIED.)
GEOMETRIC_REPRESENTATION_ITEM()
RATIONAL_B_SPLINE_SURFACE(((1.,0.912870929175276,1.),(1.,0.880766500224452,
1.),(1.,0.84428481138994,1.),(1.,0.7909171071033,1.),(1.,0.773315924547783,
1.),(1.,0.739103003635572,1.),(1.,0.722569869246584,1.),(1.,0.707106781186588,
1.)))
REPRESENTATION_ITEM('')
SURFACE()
);
#310=(
BOUNDED_SURFACE()
B_SPLINE_SURFACE(3,2,((#28951,#28952,#28953),(#28954,#28955,#28956),(#28957,
#28958,#28959),(#28960,#28961,#28962),(#28963,#28964,#28965),(#28966,#28967,
#28968),(#28969,#28970,#28971),(#28972,#28973,#28974),(#28975,#28976,#28977),
(#28978,#28979,#28980),(#28981,#28982,#28983),(#28984,#28985,#28986),(#28987,
#28988,#28989),(#28990,#28991,#28992),(#28993,#28994,#28995),(#28996,#28997,
#28998)),.UNSPECIFIED.,.F.,.F.,.F.)
B_SPLINE_SURFACE_WITH_KNOTS((4,2,2,2,2,2,2,4),(3,3),(-1.60420989719343E-5,
0.000718638734763963,0.00145331956849986,0.00182065998536781,0.00218800040223576,
0.0025553408191037,0.00273901102753768,0.00303146126452106),(0.,1.00010878002855),
 .UNSPECIFIED.)
GEOMETRIC_REPRESENTATION_ITEM()
RATIONAL_B_SPLINE_SURFACE(((1.,1.,1.),(1.,0.999993811318941,1.00000000134641),
(1.,0.999229107803248,1.00000016771535),(1.,0.995637462429539,1.00000094911392),
(1.,0.992845445901653,1.0000015565452),(1.,0.986217024917209,1.00000299862485),
(1.,0.983595353986027,1.00000356899572),(1.,0.977148768484335,1.00000497151523),
(1.,0.973342745657784,1.00000579955378),(1.,0.963689034415866,1.00000789981575),
(1.,0.957941368212052,1.00000915027833),(1.,0.946018892185112,1.0000117441329),
(1.,0.941495863696682,1.00001272816323),(1.,0.92668492389742,1.00001595043214),
(1.,0.914960830141336,1.00001850112665),(1.,0.889823099708682,1.00002397009272)))
REPRESENTATION_ITEM('')
SURFACE()
);
#311=(
BOUNDED_SURFACE()
B_SPLINE_SURFACE(3,2,((#28999,#29000,#29001),(#29002,#29003,#29004),(#29005,
#29006,#29007),(#29008,#29009,#29010),(#29011,#29012,#29013),(#29014,#29015,
#29016),(#29017,#29018,#29019),(#29020,#29021,#29022),(#29023,#29024,#29025),
(#29026,#29027,#29028),(#29029,#29030,#29031),(#29032,#29033,#29034),(#29035,
#29036,#29037),(#29038,#29039,#29040),(#29041,#29042,#29043),(#29044,#29045,
#29046)),.UNSPECIFIED.,.F.,.F.,.F.)
B_SPLINE_SURFACE_WITH_KNOTS((4,2,2,2,2,2,2,4),(3,3),(-1.60420989715478E-5,
0.000723179017757225,0.001462400134486,0.00183201069285038,0.00220162125121477,
0.00257123180957916,0.00275603708876135,0.00304759539405443),(0.,1.00010675302611),
 .UNSPECIFIED.)
GEOMETRIC_REPRESENTATION_ITEM()
RATIONAL_B_SPLINE_SURFACE(((1.,1.,1.),(1.,0.999993484045624,1.0000000013912),
(1.,0.999229603748512,1.00000016448426),(1.,0.995614556488104,1.00000093631873),
(1.,0.992787523332635,1.00000153990742),(1.,0.986117874326191,1.00000296391785),
(1.,0.983484316794167,1.00000352619832),(1.,0.977034241545352,1.00000490332842),
(1.,0.973235033264553,1.00000571448239),(1.,0.963662174424421,1.00000775834569),
(1.,0.957994029080871,1.00000896852902),(1.,0.946081971657189,1.00001151182537),
(1.,0.941528775727103,1.00001248396026),(1.,0.92674259996446,1.00001564089828),
(1.,0.915116673686062,1.0000181231039),(1.,0.890638328972987,1.00002334937864)))
REPRESENTATION_ITEM('')
SURFACE()
);
#312=(
BOUNDED_SURFACE()
B_SPLINE_SURFACE(3,2,((#29048,#29049,#29050),(#29051,#29052,#29053),(#29054,
#29055,#29056),(#29057,#29058,#29059),(#29060,#29061,#29062),(#29063,#29064,
#29065),(#29066,#29067,#29068),(#29069,#29070,#29071)),.UNSPECIFIED.,.F.,
 .F.,.F.)
B_SPLINE_SURFACE_WITH_KNOTS((4,2,2,4),(3,3),(9.30245463992563E-17,0.00233568752491339,
0.00350353128737004,0.00467137504982669),(0.,1.),.UNSPECIFIED.)
GEOMETRIC_REPRESENTATION_ITEM()
RATIONAL_B_SPLINE_SURFACE(((1.,0.912870929175271,1.),(1.,0.880766500224456,
1.),(1.,0.84428481138985,1.),(1.,0.790917107103246,1.),(1.,0.773315924547701,
1.),(1.,0.739103003635471,1.),(1.,0.722569869246403,1.),(1.,0.707106781186576,
1.)))
REPRESENTATION_ITEM('')
SURFACE()
);
#313=(
BOUNDED_SURFACE()
B_SPLINE_SURFACE(3,2,((#29072,#29073,#29074),(#29075,#29076,#29077),(#29078,
#29079,#29080),(#29081,#29082,#29083),(#29084,#29085,#29086),(#29087,#29088,
#29089)),.UNSPECIFIED.,.F.,.F.,.F.)
B_SPLINE_SURFACE_WITH_KNOTS((4,2,4),(3,3),(4.33680868994202E-17,0.00233940766482989,
0.00467881532965973),(0.,1.),.UNSPECIFIED.)
GEOMETRIC_REPRESENTATION_ITEM()
RATIONAL_B_SPLINE_SURFACE(((1.,0.707106781186544,1.),(1.,0.737898683933686,
1.),(1.,0.772355112027042,1.),(1.,0.844136160947639,1.),(1.,0.880738432868901,
1.),(1.,0.912870929175275,1.)))
REPRESENTATION_ITEM('')
SURFACE()
);
#314=(
BOUNDED_SURFACE()
B_SPLINE_SURFACE(3,2,((#29091,#29092,#29093),(#29094,#29095,#29096),(#29097,
#29098,#29099),(#29100,#29101,#29102),(#29103,#29104,#29105),(#29106,#29107,
#29108),(#29109,#29110,#29111),(#29112,#29113,#29114),(#29115,#29116,#29117),
(#29118,#29119,#29120),(#29121,#29122,#29123),(#29124,#29125,#29126),(#29127,
#29128,#29129),(#29130,#29131,#29132),(#29133,#29134,#29135),(#29136,#29137,
#29138)),.UNSPECIFIED.,.F.,.F.,.F.)
B_SPLINE_SURFACE_WITH_KNOTS((4,2,2,2,2,2,2,4),(3,3),(-0.000112562684352504,
0.000183317511890177,0.000366635023783385,0.000733270047569803,0.00109990507135622,
0.00146654009514264,0.00219981014271547,0.00293308019028831),(0.,1.00011256268435),
 .UNSPECIFIED.)
GEOMETRIC_REPRESENTATION_ITEM()
RATIONAL_B_SPLINE_SURFACE(((1.,0.888568848797213,1.000025085979),(1.,0.914720098726859,
1.00001919866922),(1.,0.926614357803736,1.00001652096976),(1.,0.941497644191894,
1.00001317036442),(1.,0.945991617994114,1.00001215865691),(1.,0.957827766219802,
1.00000949403968),(1.,0.963503346961249,1.00000821632247),(1.,0.973100607067813,
1.00000605573575),(1.,0.976922506379361,1.00000519532926),(1.,0.983418125950182,
1.00000373300051),(1.,0.986078267870914,1.00000313413508),(1.,0.992789809396121,
1.00000162319682),(1.,0.995607448637693,1.00000098887474),(1.,0.999229025528137,
1.00000017356591),(1.,0.999994157715368,1.00000000131525),(1.,1.,1.)))
REPRESENTATION_ITEM('')
SURFACE()
);
#317=B_SPLINE_CURVE_WITH_KNOTS('',3,(#24065,#24066,#24067,#24068,#24069,
#24070,#24071,#24072,#24073,#24074,#24075,#24076,#24077,#24078,#24079,#24080,
#24081,#24082,#24083,#24084,#24085,#24086,#24087,#24088,#24089,#24090,#24091,
#24092,#24093,#24094,#24095,#24096,#24097,#24098,#24099,#24100),
 .UNSPECIFIED.,.F.,.F.,(4,2,2,2,2,2,2,2,2,2,2,2,2,2,2,2,2,4),(-7.02983716919818,
-6.91061727983595,-6.60184957613577,-6.29209349508421,-5.97672564685978,
-5.6693427861326,-5.35705323733312,-5.04620132033749,-4.73820324576839,
-4.4231606033521,-4.11494256505677,-3.80457129106106,-3.49054974125412,
-3.18321904871051,-2.87024417000407,-2.56027854485072,-2.25179476733888,
-2.02069964322786),.UNSPECIFIED.);
#318=B_SPLINE_CURVE_WITH_KNOTS('',3,(#24104,#24105,#24106,#24107,#24108,
#24109,#24110,#24111,#24112,#24113,#24114,#24115,#24116,#24117,#24118,#24119,
#24120,#24121,#24122,#24123,#24124,#24125,#24126,#24127,#24128,#24129,#24130,
#24131,#24132,#24133,#24134,#24135,#24136,#24137,#24138,#24139,#24140,#24141,
#24142,#24143,#24144,#24145,#24146,#24147,#24148,#24149),.UNSPECIFIED.,
 .F.,.F.,(4,3,3,3,3,3,3,3,3,3,3,3,3,3,3,4),(-1.78276958404949E-5,0.00048760205222048,
0.000990696883911432,0.0011620783262953,0.00159313838411329,0.00201847260827172,
0.0023419843484311,0.00264615772116661,0.0029489264191348,0.0032509318938781,
0.0035218903705669,0.00402412376628078,0.0041118433816348,0.00435917421442693,
0.00460747003987267,0.00470179639270271),.UNSPECIFIED.);
#319=B_SPLINE_CURVE_WITH_KNOTS('',3,(#24151,#24152,#24153,#24154,#24155,
#24156,#24157,#24158,#24159,#24160,#24161,#24162,#24163,#24164,#24165,#24166,
#24167,#24168,#24169,#24170,#24171,#24172,#24173,#24174,#24175,#24176,#24177,
#24178,#24179,#24180,#24181,#24182,#24183,#24184,#24185,#24186,#24187,#24188,
#24189,#24190,#24191,#24192,#24193,#24194,#24195,#24196,#24197,#24198,#24199,
#24200,#24201,#24202,#24203,#24204,#24205,#24206,#24207,#24208,#24209,#24210,
#24211,#24212,#24213,#24214,#24215,#24216,#24217,#24218,#24219,#24220,#24221,
#24222,#24223,#24224,#24225,#24226,#24227,#24228,#24229,#24230,#24231,#24232,
#24233,#24234,#24235,#24236,#24237,#24238,#24239,#24240,#24241,#24242,#24243,
#24244,#24245,#24246,#24247,#24248,#24249,#24250,#24251,#24252,#24253,#24254,
#24255,#24256,#24257,#24258,#24259,#24260,#24261,#24262,#24263,#24264,#24265),
 .UNSPECIFIED.,.F.,.F.,(4,3,3,3,3,3,3,3,3,3,3,3,3,3,3,3,3,3,3,3,3,3,3,3,
3,3,3,3,3,3,3,3,3,3,3,3,3,3,4),(0.,0.000835280056435426,0.00169563992176735,
0.00202900517965703,0.00203670118809256,0.00273967946803035,0.00304350776948554,
0.00305586812971479,0.00382326558602126,0.00405801035931406,0.00407363242773161,
0.00488802506566889,0.00507251294914258,0.00508876089012826,0.00571265222895443,
0.0060870155389711,0.00610043813452581,0.00739805770417624,0.00811602071862814,
0.00811729674236745,0.00862041865727346,0.00912389078901127,0.00913052330845666,
0.0101329818752895,0.0101450258982852,0.0107937367146334,0.0111445911494065,
0.0111595284881137,0.0119661634642224,0.0121594862552067,0.0121740310779422,
0.0129702064619354,0.0131770532806838,0.0139835466547703,0.0141959022300147,
0.0142030362575992,0.0150627300415056,0.0158961801336698,0.0162320414372563),
 .UNSPECIFIED.);
#320=B_SPLINE_CURVE_WITH_KNOTS('',3,(#24267,#24268,#24269,#24270,#24271,
#24272,#24273,#24274,#24275,#24276,#24277,#24278,#24279,#24280,#24281,#24282,
#24283,#24284,#24285,#24286,#24287,#24288,#24289,#24290,#24291,#24292,#24293,
#24294,#24295,#24296,#24297,#24298,#24299,#24300,#24301,#24302,#24303,#24304,
#24305,#24306,#24307,#24308,#24309,#24310,#24311,#24312,#24313,#24314,#24315,
#24316,#24317,#24318),.UNSPECIFIED.,.F.,.F.,(4,3,3,3,3,3,3,3,3,3,3,3,3,
3,3,3,3,4),(0.,0.000250783426701624,0.000500478773643964,0.000595498928445555,
0.0011024723631392,0.00119099785689111,0.00149585681270147,0.00180098314939396,
0.00210806480762694,0.00238199571378222,0.00281024881469782,0.00324458797215041,
0.00357299357067334,0.00391657307822326,0.00416849249911889,0.00443812719701021,
0.0047084871246697,0.00476399142756445),.UNSPECIFIED.);
#321=B_SPLINE_CURVE_WITH_KNOTS('',3,(#24320,#24321,#24322,#24323,#24324,
#24325,#24326,#24327,#24328,#24329,#24330,#24331,#24332,#24333,#24334,#24335,
#24336,#24337,#24338,#24339,#24340,#24341,#24342,#24343,#24344,#24345,#24346,
#24347,#24348,#24349,#24350,#24351,#24352,#24353,#24354,#24355,#24356,#24357,
#24358,#24359,#24360,#24361,#24362,#24363,#24364,#24365),.UNSPECIFIED.,
 .F.,.F.,(4,3,3,3,3,3,3,3,3,3,3,3,3,3,3,4),(-1.78276958405635E-5,0.000487602051909098,
0.000990696883295357,0.00116207832629524,0.00159313838411058,0.00201847260826763,
0.00234198434843103,0.0026461577211663,0.0029489264191348,0.00325093189387818,
0.00352189037056683,0.00402412376627937,0.00411184338163473,0.00435917421442732,
0.00460747003987296,0.00470179639270263),.UNSPECIFIED.);
#322=B_SPLINE_CURVE_WITH_KNOTS('',3,(#24367,#24368,#24369,#24370,#24371,
#24372,#24373,#24374,#24375,#24376,#24377,#24378,#24379,#24380,#24381,#24382,
#24383,#24384,#24385,#24386,#24387,#24388,#24389,#24390,#24391,#24392,#24393,
#24394,#24395,#24396,#24397,#24398,#24399,#24400,#24401,#24402,#24403,#24404,
#24405,#24406,#24407,#24408,#24409,#24410,#24411,#24412,#24413,#24414,#24415,
#24416,#24417,#24418,#24419,#24420,#24421,#24422,#24423,#24424,#24425,#24426,
#24427,#24428,#24429,#24430,#24431,#24432,#24433,#24434,#24435,#24436,#24437,
#24438,#24439,#24440,#24441,#24442,#24443,#24444,#24445,#24446,#24447,#24448,
#24449,#24450,#24451,#24452,#24453,#24454,#24455,#24456,#24457,#24458,#24459,
#24460,#24461,#24462,#24463,#24464,#24465,#24466,#24467,#24468,#24469,#24470,
#24471,#24472,#24473,#24474,#24475,#24476,#24477,#24478,#24479,#24480,#24481),
 .UNSPECIFIED.,.F.,.F.,(4,3,3,3,3,3,3,3,3,3,3,3,3,3,3,3,3,3,3,3,3,3,3,3,
3,3,3,3,3,3,3,3,3,3,3,3,3,3,4),(0.,0.000835280057182376,0.00169563992374365,
0.00202900517965707,0.00203670118809262,0.00273967946780872,0.0030435077694856,
0.00305586812971486,0.00382326558623257,0.00405801035931413,0.00407363242773168,
0.00488802506543847,0.00507251294914266,0.00508876089012833,0.00571265222913317,
0.0060870155389712,0.00610043813452591,0.00739805770647065,0.00811602071862826,
0.00811729674236754,0.00862041865727386,0.00912389078901138,0.00913052330845679,
0.0101329818752897,0.0101450258982853,0.0107937367140956,0.0111445911494066,
0.0111595284881138,0.0119661634632636,0.0121594862552069,0.0121740310779424,
0.0129702064615506,0.0131770532806835,0.0139835466544668,0.0141959022300149,
0.0142030362575994,0.015062730039064,0.0158961801294878,0.0162320414372565),
 .UNSPECIFIED.);
#323=B_SPLINE_CURVE_WITH_KNOTS('',3,(#24482,#24483,#24484,#24485,#24486,
#24487,#24488,#24489,#24490,#24491,#24492,#24493,#24494,#24495,#24496,#24497,
#24498,#24499,#24500,#24501,#24502,#24503,#24504,#24505,#24506,#24507,#24508,
#24509,#24510,#24511,#24512,#24513,#24514,#24515,#24516,#24517,#24518,#24519,
#24520,#24521,#24522,#24523,#24524,#24525,#24526,#24527,#24528,#24529,#24530,
#24531,#24532,#24533),.UNSPECIFIED.,.F.,.F.,(4,3,3,3,3,3,3,3,3,3,3,3,3,
3,3,3,3,4),(0.,0.000250783426701639,0.000500478773643702,0.00059549892844555,
0.00110247236313969,0.0011909978568911,0.00149585681270176,0.00180098314939464,
0.00210806480762769,0.0023819957137822,0.00281024881469934,0.00324458797215156,
0.0035729935706733,0.00391657307822337,0.00416849249911885,0.00443812719701222,
0.00470848712467381,0.00476399142756435),.UNSPECIFIED.);
#324=B_SPLINE_CURVE_WITH_KNOTS('',3,(#24535,#24536,#24537,#24538,#24539,
#24540,#24541,#24542,#24543,#24544,#24545,#24546,#24547,#24548,#24549,#24550,
#24551,#24552),.UNSPECIFIED.,.F.,.F.,(4,2,2,2,2,2,2,2,4),(-2.02069964322786,
-1.93602870456447,-1.62817717542802,-1.31711717061402,-1.00426032153936,
-0.696786756318718,-0.383063120605535,-0.192742107424168,-1.68481669504672E-7),
 .UNSPECIFIED.);
#325=B_SPLINE_CURVE_WITH_KNOTS('',3,(#24555,#24556,#24557,#24558,#24559,
#24560,#24561,#24562,#24563,#24564,#24565,#24566,#24567,#24568,#24569,#24570,
#24571,#24572,#24573,#24574,#24575,#24576,#24577,#24578,#24579,#24580,#24581,
#24582),.UNSPECIFIED.,.F.,.F.,(4,2,2,2,2,2,2,2,2,2,2,2,2,4),(-102.474089688378,
-102.46654374275,-102.459658842978,-102.445888796445,-102.418354743121,
-102.363366857814,-102.25415351107,-102.036501710124,-101.720905207923,
-101.412622763323,-101.103211103582,-100.790411499237,-100.483417818375,
-100.455361666765),.UNSPECIFIED.);
#326=B_SPLINE_CURVE_WITH_KNOTS('',3,(#24587,#24588,#24589,#24590,#24591,
#24592,#24593,#24594,#24595,#24596,#24597,#24598,#24599,#24600,#24601,#24602,
#24603,#24604,#24605,#24606,#24607,#24608,#24609,#24610,#24611,#24612,#24613,
#24614,#24615,#24616,#24617,#24618,#24619,#24620,#24621,#24622),
 .UNSPECIFIED.,.F.,.F.,(4,2,2,2,2,2,2,2,2,2,2,2,2,2,2,2,2,4),(-12.038757850411,
-11.8853163131962,-11.5753600418793,-11.2669746154469,-10.9513198822466,
-10.6435111532232,-10.3325590764039,-10.0196946327693,-9.71229683067363,
-9.39868523199586,-9.08943048477653,-8.78038464839336,-8.46395120910075,
-8.15632710992796,-7.8446364669664,-7.53273261566686,-7.22501792738819,
-7.02983716919818),.UNSPECIFIED.);
#327=B_SPLINE_CURVE_WITH_KNOTS('',3,(#24623,#24624,#24625,#24626,#24627,
#24628,#24629,#24630,#24631,#24632,#24633,#24634,#24635,#24636,#24637,#24638,
#24639,#24640,#24641,#24642,#24643,#24644,#24645,#24646,#24647,#24648,#24649,
#24650,#24651,#24652,#24653,#24654,#24655,#24656,#24657,#24658),
 .UNSPECIFIED.,.F.,.F.,(4,2,2,2,2,2,2,2,2,2,2,2,2,2,2,2,2,4),(-100.455361666765,
-100.170076029009,-99.8598933647241,-99.552143383566,-99.2372865599758,
-98.9295390353325,-98.6192902679461,-98.3071935852368,-98.0001977363163,
-97.6855532606439,-97.3760059671289,-97.0677518385104,-96.7535593223314,
-96.4461472340099,-96.134886301849,-95.8234121302857,-95.5162222726446,
-95.4519283393931),.UNSPECIFIED.);
#328=B_SPLINE_CURVE_WITH_KNOTS('',3,(#24663,#24664,#24665,#24666,#24667,
#24668,#24669,#24670,#24671,#24672,#24673,#24674,#24675,#24676,#24677,#24678,
#24679,#24680,#24681,#24682,#24683,#24684,#24685,#24686,#24687,#24688,#24689,
#24690,#24691,#24692,#24693,#24694,#24695,#24696,#24697,#24698),
 .UNSPECIFIED.,.F.,.F.,(4,2,2,2,2,2,2,2,2,2,2,2,2,2,2,2,2,4),(-17.0471773480641,
-16.858831398655,-16.5469160471412,-16.2392734228736,-15.9249731659921,
-15.6162249090113,-15.3065668667821,-14.9911686850119,-14.6838364190402,
-14.3716502905428,-14.060796004546,-13.7528833607647,-13.437947332658,-13.1297597759444,
-12.8194921961025,-12.5054502022621,-12.1981827248202,-12.038757850411),
 .UNSPECIFIED.);
#329=B_SPLINE_CURVE_WITH_KNOTS('',3,(#24699,#24700,#24701,#24702,#24703,
#24704,#24705,#24706,#24707,#24708,#24709,#24710,#24711,#24712,#24713,#24714,
#24715,#24716,#24717,#24718,#24719,#24720,#24721,#24722,#24723,#24724,#24725,
#24726,#24727,#24728,#24729,#24730,#24731,#24732,#24733,#24734),
 .UNSPECIFIED.,.F.,.F.,(4,2,2,2,2,2,2,2,2,2,2,2,2,2,2,2,2,4),(-95.4519283393931,
-95.2001303583947,-94.8911288140346,-94.5822053411759,-94.2685786867721,
-93.9612985535358,-93.6488915867085,-93.3379369392675,-93.030377939059,
-92.7147134772413,-92.4063569027996,-92.0967869846843,-91.7839183337999,
-91.4768183345611,-91.1632878409301,-90.85303324059,-90.5451455491716,-90.4465923804445),
 .UNSPECIFIED.);
#330=B_SPLINE_CURVE_WITH_KNOTS('',3,(#24739,#24740,#24741,#24742,#24743,
#24744,#24745,#24746,#24747,#24748,#24749,#24750,#24751,#24752,#24753,#24754,
#24755,#24756,#24757,#24758,#24759,#24760,#24761,#24762,#24763,#24764,#24765,
#24766,#24767,#24768,#24769,#24770,#24771,#24772,#24773,#24774),
 .UNSPECIFIED.,.F.,.F.,(4,2,2,2,2,2,2,2,2,2,2,2,2,2,2,2,2,4),(-22.0548538324586,
-21.832827853436,-21.5187457875705,-21.2115252632328,-20.8987529717923,
-20.5887876674696,-20.2804855806856,-19.9649278030172,-19.6571448681826,
-19.3462865382462,-19.0333952627533,-18.7260574772503,-18.4125437773414,
-18.1032938823081,-17.7943433300796,-17.4780103234481,-17.170425145641,
-17.0471773480641),.UNSPECIFIED.);
#331=B_SPLINE_CURVE_WITH_KNOTS('',3,(#24775,#24776,#24777,#24778,#24779,
#24780,#24781,#24782,#24783,#24784,#24785,#24786,#24787,#24788,#24789,#24790,
#24791,#24792,#24793,#24794,#24795,#24796,#24797,#24798,#24799,#24800,#24801,
#24802,#24803,#24804,#24805,#24806,#24807,#24808,#24809,#24810),
 .UNSPECIFIED.,.F.,.F.,(4,2,2,2,2,2,2,2,2,2,2,2,2,2,2,2,2,4),(-90.4465923804445,
-90.2302170891205,-89.9223838493343,-89.6119648299085,-89.299795102601,
-88.9926809815866,-88.6778369847466,-88.3682131269476,-88.0598102421047,
-87.7455409623599,-87.4380307810344,-87.1265897630268,-86.8150371043751,
-86.5077175775081,-86.1914185238541,-85.8823344459644,-85.573252838895,
-85.4407846201475),.UNSPECIFIED.);
#332=B_SPLINE_CURVE_WITH_KNOTS('',3,(#24815,#24816,#24817,#24818,#24819,
#24820,#24821,#24822,#24823,#24824,#24825,#24826,#24827,#24828,#24829,#24830,
#24831,#24832,#24833,#24834,#24835,#24836,#24837,#24838,#24839,#24840,#24841,
#24842,#24843,#24844,#24845,#24846,#24847,#24848,#24849,#24850),
 .UNSPECIFIED.,.F.,.F.,(4,2,2,2,2,2,2,2,2,2,2,2,2,2,2,2,2,4),(-27.0628130182279,
-26.8069778864524,-26.490730231184,-26.1831669347654,-25.8716551853357,
-25.559709422747,-25.2521228733781,-24.9379080994133,-24.6291615235746,
-24.3195868347493,-24.0041384835497,-23.6968401183334,-23.3847428143161,
-23.0738674443347,-22.7660247078664,-22.4511806787902,-22.1430061561745,
-22.0548538324586),.UNSPECIFIED.);
#333=B_SPLINE_CURVE_WITH_KNOTS('',3,(#24851,#24852,#24853,#24854,#24855,
#24856,#24857,#24858,#24859,#24860,#24861,#24862,#24863,#24864,#24865,#24866,
#24867,#24868,#24869,#24870,#24871,#24872,#24873,#24874,#24875,#24876,#24877,
#24878,#24879,#24880,#24881,#24882,#24883,#24884,#24885,#24886),
 .UNSPECIFIED.,.F.,.F.,(4,2,2,2,2,2,2,2,2,2,2,2,2,2,2,2,2,4),(-85.4407846201475,
-85.2595428973909,-84.9521525010805,-84.639558343424,-84.3285184262725,
-84.0208197185399,-83.705070310243,-83.3966229683412,-83.0868823718611,
-82.7739279078785,-82.4667066598592,-82.1529764130471,-81.8426333927081,
-81.5345946694503,-81.2195777462055,-80.911642722096,-80.601041703004,-80.4335177250807),
 .UNSPECIFIED.);
#334=B_SPLINE_CURVE_WITH_KNOTS('',3,(#24891,#24892,#24893,#24894,#24895,
#24896,#24897,#24898,#24899,#24900,#24901,#24902,#24903,#24904,#24905,#24906,
#24907,#24908,#24909,#24910,#24911,#24912,#24913,#24914,#24915,#24916,#24917,
#24918,#24919,#24920,#24921,#24922,#24923,#24924,#24925,#24926),
 .UNSPECIFIED.,.F.,.F.,(4,2,2,2,2,2,2,2,2,2,2,2,2,2,2,2,2,4),(-32.0696198736087,
-31.7781082037164,-31.4633407311828,-31.1551614995253,-30.8450572548339,
-30.5309155756559,-30.2237251951323,-29.9110318438284,-29.6010389747784,
-29.2928044075254,-28.9773283521885,-28.6695537841855,-28.3587741699972,
-28.0458367711374,-27.7385425892498,-27.4251117737632,-27.1158485377647,
-27.0628130182279),.UNSPECIFIED.);
#335=B_SPLINE_CURVE_WITH_KNOTS('',3,(#24927,#24928,#24929,#24930,#24931,
#24932,#24933,#24934,#24935,#24936,#24937,#24938,#24939,#24940,#24941,#24942,
#24943,#24944,#24945,#24946,#24947,#24948,#24949,#24950,#24951,#24952,#24953,
#24954,#24955,#24956,#24957,#24958,#24959,#24960,#24961,#24962),
 .UNSPECIFIED.,.F.,.F.,(4,2,2,2,2,2,2,2,2,2,2,2,2,2,2,2,2,4),(-80.4335177250807,
-80.2887823377538,-79.9815356448999,-79.6664817246118,-79.3567650240283,
-79.0482006811451,-78.7338380395159,-78.4262143499005,-78.1145820896486,
-77.8029345943652,-77.4954717391251,-77.1790776601926,-76.8700744291997,
-76.5610545946566,-76.2474854347615,-75.9402037447504,-75.627644696357,
-75.4263375761454),.UNSPECIFIED.);
#336=B_SPLINE_CURVE_WITH_KNOTS('',3,(#24967,#24968,#24969,#24970,#24971,
#24972,#24973,#24974,#24975,#24976,#24977,#24978,#24979,#24980,#24981,#24982,
#24983,#24984,#24985,#24986,#24987,#24988,#24989,#24990,#24991,#24992,#24993,
#24994,#24995,#24996,#24997,#24998,#24999,#25000,#25001,#25002,#25003,#25004),
 .UNSPECIFIED.,.F.,.F.,(4,2,2,2,2,2,2,2,2,2,2,2,2,2,2,2,2,2,4),(-37.0769841873551,
-37.0575083077529,-36.7502407984738,-36.4368770759001,-36.1275822274484,
-35.8187752969543,-35.5025971161927,-35.1950383117034,-34.88359289563,-34.5715978566608,
-34.2640507816734,-33.9499057927643,-33.6411429317627,-33.331636141935,
-33.0161179680958,-32.7088363625265,-32.3968124814779,-32.0858972713141,
-32.0696198736087),.UNSPECIFIED.);
#337=B_SPLINE_CURVE_WITH_KNOTS('',3,(#25005,#25006,#25007,#25008,#25009,
#25010,#25011,#25012,#25013,#25014,#25015,#25016,#25017,#25018,#25019,#25020,
#25021,#25022,#25023,#25024,#25025,#25026,#25027,#25028,#25029,#25030,#25031,
#25032,#25033,#25034,#25035,#25036,#25037,#25038,#25039,#25040),
 .UNSPECIFIED.,.F.,.F.,(4,2,2,2,2,2,2,2,2,2,2,2,2,2,2,2,2,4),(-75.4263375761454,
-75.3167416267388,-75.0091222628059,-74.693513377888,-74.3851950606098,
-74.0755041712474,-73.7626873451246,-73.4555636200335,-73.1418568101527,
-72.831646908359,-72.5236764420255,-72.208795912533,-71.9009784300672,-71.5904164789951,
-71.2782903385179,-70.9711298391533,-70.6560902661978,-70.4207058556691),
 .UNSPECIFIED.);
#338=B_SPLINE_CURVE_WITH_KNOTS('',3,(#25045,#25046,#25047,#25048,#25049,
#25050,#25051,#25052,#25053,#25054,#25055,#25056,#25057,#25058,#25059,#25060,
#25061,#25062,#25063,#25064,#25065,#25066,#25067,#25068,#25069,#25070,#25071,
#25072,#25073,#25074,#25075,#25076,#25077,#25078,#25079,#25080),
 .UNSPECIFIED.,.F.,.F.,(4,2,2,2,2,2,2,2,2,2,2,2,2,2,2,2,2,4),(-42.0835650080859,
-42.0276024561896,-41.7203201695277,-41.4083535901313,-41.0973799381269,
-40.7896277028518,-40.4749206008968,-40.1667187871955,-39.8566726623258,
-39.5424521318403,-39.2352746747194,-38.922644324604,-38.6126054028072,
-38.3044218286954,-37.98901148703,-37.6812276180551,-37.37051094087,-37.0769841873551),
 .UNSPECIFIED.);
#339=B_SPLINE_CURVE_WITH_KNOTS('',3,(#25081,#25082,#25083,#25084,#25085,
#25086,#25087,#25088,#25089,#25090,#25091,#25092,#25093,#25094,#25095,#25096,
#25097,#25098,#25099,#25100,#25101,#25102,#25103,#25104,#25105,#25106,#25107,
#25108,#25109,#25110,#25111,#25112,#25113,#25114,#25115,#25116),
 .UNSPECIFIED.,.F.,.F.,(4,2,2,2,2,2,2,2,2,2,2,2,2,2,2,2,2,4),(-70.4207058556691,
-70.3465017244344,-70.0379956331957,-69.7237639236243,-69.416245783058,
-69.1046441997098,-68.7931241987137,-68.4857369618575,-68.1694742193023,
-67.8605977832699,-67.5516229712482,-67.2381825248866,-66.9309955834494,
-66.6184531943587,-66.3076748184943,-66.0001191746988,-65.684638545429,
-65.4152002552604),.UNSPECIFIED.);
#340=B_SPLINE_CURVE_WITH_KNOTS('',3,(#25121,#25122,#25123,#25124,#25125,
#25126,#25127,#25128,#25129,#25130,#25131,#25132,#25133,#25134,#25135,#25136,
#25137,#25138,#25139,#25140,#25141,#25142,#25143,#25144,#25145,#25146,#25147,
#25148,#25149,#25150,#25151,#25152,#25153,#25154,#25155,#25156),
 .UNSPECIFIED.,.F.,.F.,(4,2,2,2,2,2,2,2,2,2,2,2,2,2,2,2,2,4),(-47.0910467575489,
-47.0004773013202,-46.692666388461,-46.3819962211513,-46.0689096299662,
-45.7616514853505,-45.4483383831922,-45.138993755588,-44.8302336827447,
-44.514108399339,-44.206536503736,-43.8951410858116,-43.5830781495772,-43.2755534665247,
-42.9614618670812,-42.6526647270027,-42.3432097035513,-42.0835650080859),
 .UNSPECIFIED.);
#341=B_SPLINE_CURVE_WITH_KNOTS('',3,(#25157,#25158,#25159,#25160,#25161,
#25162,#25163,#25164,#25165,#25166,#25167,#25168,#25169,#25170,#25171,#25172,
#25173,#25174,#25175,#25176,#25177,#25178,#25179,#25180,#25181,#25182,#25183,
#25184,#25185,#25186,#25187,#25188,#25189,#25190,#25191,#25192),
 .UNSPECIFIED.,.F.,.F.,(4,2,2,2,2,2,2,2,2,2,2,2,2,2,2,2,2,4),(-65.4152002552604,
-65.376436341034,-65.0667777641196,-64.7540863074667,-64.4470455058427,
-64.1333431058225,-63.8232539322029,-63.5153355089084,-63.200578841122,
-62.8928653273433,-62.5823245298298,-62.2703190625795,-61.9632295532419,
-61.6481849043275,-61.3387118184057,-61.0302472735284,-60.7161336210183,
-60.4108627972263),.UNSPECIFIED.);
#342=B_SPLINE_CURVE_WITH_KNOTS('',3,(#25197,#25198,#25199,#25200,#25201,
#25202,#25203,#25204,#25205,#25206,#25207,#25208,#25209,#25210,#25211,#25212,
#25213,#25214,#25215,#25216,#25217,#25218,#25219,#25220,#25221,#25222,#25223,
#25224,#25225,#25226,#25227,#25228,#25229,#25230,#25231,#25232),
 .UNSPECIFIED.,.F.,.F.,(4,2,2,2,2,2,2,2,2,2,2,2,2,2,2,2,2,4),(-52.0980129685988,
-51.9730797155729,-51.6642304507307,-51.3548104950973,-51.0390955345897,
-50.7317949854421,-50.4198689750653,-50.108818627249,-49.8010859273223,
-49.4864223734463,-49.1781801469801,-48.8681755897101,-48.5538574830228,
-48.2466754690557,-47.9340915292134,-47.6239883003567,-47.3158386130918,
-47.0910467575489),.UNSPECIFIED.);
#343=B_SPLINE_CURVE_WITH_KNOTS('',3,(#25233,#25234,#25235,#25236,#25237,
#25238,#25239,#25240,#25241,#25242,#25243,#25244,#25245,#25246,#25247,#25248,
#25249,#25250,#25251,#25252,#25253,#25254,#25255,#25256,#25257,#25258,#25259,
#25260,#25261,#25262,#25263,#25264,#25265,#25266,#25267,#25268,#25269,#25270),
 .UNSPECIFIED.,.F.,.F.,(4,2,2,2,2,2,2,2,2,2,2,2,2,2,2,2,2,2,4),(-60.4108627972263,
-60.4087068158386,-60.0971176296951,-59.7857122133521,-59.4783848698016,
-59.1622404359523,-58.8534775234458,-58.5445303791034,-58.2312056492169,
-57.9240986618394,-57.6115540159792,-57.300887267302,-56.9933790350214,
-56.6780134555657,-56.3699135075542,-56.0602693186155,-55.7476900387188,
-55.4407167803585,-55.4071129852565),.UNSPECIFIED.);
#344=B_SPLINE_CURVE_WITH_KNOTS('',3,(#25275,#25276,#25277,#25278,#25279,
#25280,#25281,#25282,#25283,#25284,#25285,#25286,#25287,#25288,#25289,#25290,
#25291,#25292,#25293,#25294,#25295,#25296,#25297,#25298,#25299,#25300,#25301,
#25302,#25303,#25304,#25305,#25306,#25307,#25308,#25309,#25310),
 .UNSPECIFIED.,.F.,.F.,(4,2,2,2,2,2,2,2,2,2,2,2,2,2,2,2,2,4),(-57.1054920760842,
-56.9437704025751,-56.6365568449243,-56.322735716271,-56.0124454172078,
-55.7043761272089,-55.3937355145563,-55.0805468237212,-54.7732805137774,
-54.4600009967079,-54.1505887093072,-53.8418580853489,-53.5257685396563,
-53.2181659400515,-52.9068036303523,-52.5946546131302,-52.2871349042509,
-52.0980129685988),.UNSPECIFIED.);
#345=B_SPLINE_CURVE_WITH_KNOTS('',3,(#25311,#25312,#25313,#25314,#25315,
#25316,#25317,#25318,#25319,#25320,#25321,#25322,#25323,#25324,#25325,#25326,
#25327,#25328,#25329,#25330,#25331,#25332,#25333,#25334,#25335,#25336,#25337,
#25338,#25339,#25340,#25341,#25342,#25343,#25344,#25345,#25346),
 .UNSPECIFIED.,.F.,.F.,(4,2,2,2,2,2,2,2,2,2,2,2,2,2,2,2,2,4),(-55.4071129852565,
-55.1269993808329,-54.8170176401417,-54.5091344278048,-54.194488160584,
-53.8868641521749,-53.5763261395185,-53.2644278801274,-52.9573934420036,
-52.6423239878026,-52.3329527642613,-52.0245125101988,-51.7105031272677,
-51.4031526194724,-51.0958326655231,-50.7819027279722,-50.4733999003014,
-50.4034127968505),.UNSPECIFIED.);
#346=B_SPLINE_CURVE_WITH_KNOTS('',3,(#25351,#25352,#25353,#25354,#25355,
#25356,#25357,#25358,#25359,#25360,#25361,#25362,#25363,#25364,#25365,#25366,
#25367,#25368,#25369,#25370,#25371,#25372,#25373,#25374,#25375,#25376,#25377,
#25378,#25379,#25380,#25381,#25382,#25383,#25384,#25385,#25386),
 .UNSPECIFIED.,.F.,.F.,(4,2,2,2,2,2,2,2,2,2,2,2,2,2,2,2,2,4),(-62.1136210401049,
-61.9163387340731,-61.6086313703946,-61.2968929557857,-60.9851664195768,
-60.6776115528275,-60.3611377639058,-60.0520563158807,-59.7429353108473,
-59.4292867469164,-59.1219184839582,-58.8092489948486,-58.4982663785463,
-58.1905516047176,-57.8748624413629,-57.5664631706967,-57.2566672869653,
-57.1054920760842),.UNSPECIFIED.);
#347=B_SPLINE_CURVE_WITH_KNOTS('',3,(#25387,#25388,#25389,#25390,#25391,
#25392,#25393,#25394,#25395,#25396,#25397,#25398,#25399,#25400,#25401,#25402,
#25403,#25404,#25405,#25406,#25407,#25408,#25409,#25410,#25411,#25412,#25413,
#25414,#25415,#25416,#25417,#25418,#25419,#25420,#25421,#25422),
 .UNSPECIFIED.,.F.,.F.,(4,2,2,2,2,2,2,2,2,2,2,2,2,2,2,2,2,4),(-50.4034127968505,
-50.164105472623,-49.8488834773958,-49.5418417861919,-49.230029139742,-48.9193892122316,
-48.6118193294818,-48.297263519743,-47.9893372298427,-47.6794422899663,
-47.3655898524267,-47.058631647327,-46.7461468985924,-46.4364215495851,
-46.1283985834444,-45.8131317920273,-45.5056023522412,-45.4002962379396),
 .UNSPECIFIED.);
#348=B_SPLINE_CURVE_WITH_KNOTS('',3,(#25427,#25428,#25429,#25430,#25431,
#25432,#25433,#25434,#25435,#25436,#25437,#25438,#25439,#25440,#25441,#25442,
#25443,#25444,#25445,#25446,#25447,#25448,#25449,#25450,#25451,#25452,#25453,
#25454,#25455,#25456,#25457,#25458,#25459,#25460,#25461,#25462),
 .UNSPECIFIED.,.F.,.F.,(4,2,2,2,2,2,2,2,2,2,2,2,2,2,2,2,2,4),(-67.1222250534393,
-66.8889859665686,-66.5804612178844,-66.2706205210999,-65.9575893611776,
-65.6502823358052,-65.3364431537315,-65.0260231367163,-64.7178901318218,
-64.4027954105073,-64.0947799572192,-63.7840755293362,-63.4717384956288,
-63.1644028402809,-62.8492369333942,-62.5394420846956,-62.2307804551113,
-62.1136210401049),.UNSPECIFIED.);
#349=B_SPLINE_CURVE_WITH_KNOTS('',3,(#25463,#25464,#25465,#25466,#25467,
#25468,#25469,#25470,#25471,#25472,#25473,#25474,#25475,#25476,#25477,#25478,
#25479,#25480,#25481,#25482,#25483,#25484,#25485,#25486,#25487,#25488,#25489,
#25490,#25491,#25492,#25493,#25494,#25495,#25496,#25497,#25498),
 .UNSPECIFIED.,.F.,.F.,(4,2,2,2,2,2,2,2,2,2,2,2,2,2,2,2,2,4),(-45.4002962379396,
-45.1950299093757,-44.8823730677161,-44.5753034279609,-44.2620795406819,
-43.9530750929825,-43.644409446872,-43.3283695899486,-43.0210435048463,
-42.7097376296218,-42.398062628467,-42.0906936991598,-41.7766849905124,
-41.4681881765344,-41.1588170036172,-40.8436536045709,-40.5365853475107,
-40.3961502328463),.UNSPECIFIED.);
#350=B_SPLINE_CURVE_WITH_KNOTS('',3,(#25503,#25504,#25505,#25506,#25507,
#25508,#25509,#25510,#25511,#25512,#25513,#25514,#25515,#25516,#25517,#25518,
#25519,#25520,#25521,#25522,#25523,#25524,#25525,#25526,#25527,#25528,#25529,
#25530,#25531,#25532,#25533,#25534,#25535,#25536,#25537,#25538),
 .UNSPECIFIED.,.F.,.F.,(4,2,2,2,2,2,2,2,2,2,2,2,2,2,2,2,2,4),(-72.1302573428804,
-71.8631304122031,-71.5534330563933,-71.2449364392317,-70.9305928217517,
-70.6230033389037,-70.3114592540741,-69.9998322224352,-69.6924245282241,
-69.3760139851406,-69.0668548000318,-68.7576767210128,-68.443890679124,
-68.1364175726176,-67.8237181807294,-67.5126020479389,-67.2048122935097,
-67.1222250534393),.UNSPECIFIED.);
#351=B_SPLINE_CURVE_WITH_KNOTS('',3,(#25539,#25540,#25541,#25542,#25543,
#25544,#25545,#25546,#25547,#25548,#25549,#25550,#25551,#25552,#25553,#25554,
#25555,#25556,#25557,#25558,#25559,#25560,#25561,#25562,#25563,#25564,#25565,
#25566,#25567,#25568,#25569,#25570,#25571,#25572,#25573,#25574),
 .UNSPECIFIED.,.F.,.F.,(4,2,2,2,2,2,2,2,2,2,2,2,2,2,2,2,2,4),(-40.3961502328463,
-40.2246904616579,-39.9140796544823,-39.606446806267,-39.2918055999392,
-38.9838738720454,-38.6738961625095,-38.3600921718419,-38.053094203686,
-37.7405218252869,-37.4308134458335,-37.1227139008544,-36.8073566670787,
-36.4998088910576,-36.1891491286477,-35.8765273825777,-35.5694047444726,
-35.3924138450891),.UNSPECIFIED.);
#352=B_SPLINE_CURVE_WITH_KNOTS('',3,(#25579,#25580,#25581,#25582,#25583,
#25584,#25585,#25586,#25587,#25588,#25589,#25590,#25591,#25592,#25593,#25594,
#25595,#25596,#25597,#25598,#25599,#25600,#25601,#25602,#25603,#25604,#25605,
#25606,#25607,#25608,#25609,#25610,#25611,#25612,#25613,#25614),
 .UNSPECIFIED.,.F.,.F.,(4,2,2,2,2,2,2,2,2,2,2,2,2,2,2,2,2,4),(-77.1366478717291,
-76.8355230676794,-76.5244969661853,-76.2168508494848,-75.9011143340131,
-75.5926850995749,-75.2830185434786,-74.9700779966474,-74.6628964476979,
-74.3492600632362,-74.0389331812871,-73.7309549479999,-73.4159535036981,
-73.1080444062249,-72.7975252397004,-72.4852825886811,-72.178083541516,
-72.1302573428804),.UNSPECIFIED.);
#353=B_SPLINE_CURVE_WITH_KNOTS('',3,(#25615,#25616,#25617,#25618,#25619,
#25620,#25621,#25622,#25623,#25624,#25625,#25626,#25627,#25628,#25629,#25630,
#25631,#25632,#25633,#25634,#25635,#25636,#25637,#25638,#25639,#25640,#25641,
#25642,#25643,#25644,#25645,#25646,#25647,#25648,#25649,#25650),
 .UNSPECIFIED.,.F.,.F.,(4,2,2,2,2,2,2,2,2,2,2,2,2,2,2,2,2,4),(-35.3924138450891,
-35.2560893785116,-34.9470878667756,-34.6383335093246,-34.3221996684171,
-34.014841951678,-33.7034455514833,-33.3917901474578,-33.0843559896569,
-32.7702532653614,-32.461744606947,-32.1522816756052,-31.8371571040235,
-31.5300453916212,-31.2180533276116,-30.9074528993813,-30.5997412551407,
-30.3874064632604),.UNSPECIFIED.);
#354=B_SPLINE_CURVE_WITH_KNOTS('',3,(#25655,#25656,#25657,#25658,#25659,
#25660,#25661,#25662,#25663,#25664,#25665,#25666,#25667,#25668,#25669,#25670,
#25671,#25672,#25673,#25674,#25675,#25676,#25677,#25678,#25679,#25680,#25681,
#25682,#25683,#25684,#25685,#25686,#25687,#25688,#25689,#25690,#25691,#25692),
 .UNSPECIFIED.,.F.,.F.,(4,2,2,2,2,2,2,2,2,2,2,2,2,2,2,2,2,2,4),(-82.1419590834687,
-82.1176007910994,-81.8072554425438,-81.4950907524697,-81.1880142579156,
-80.873263839072,-80.5636478744585,-80.2553038443901,-79.9410419117584,
-79.633555116795,-79.3221945146972,-79.0106508199037,-78.703376894399,-78.387176536406,
-78.0781046361535,-77.7690883629183,-77.4553904456565,-77.1480320043487,
-77.1366478717291),.UNSPECIFIED.);
#355=B_SPLINE_CURVE_WITH_KNOTS('',3,(#25693,#25694,#25695,#25696,#25697,
#25698,#25699,#25700,#25701,#25702,#25703,#25704,#25705,#25706,#25707,#25708,
#25709,#25710,#25711,#25712,#25713,#25714,#25715,#25716,#25717,#25718,#25719,
#25720,#25721,#25722,#25723,#25724,#25725,#25726,#25727,#25728),
 .UNSPECIFIED.,.F.,.F.,(4,2,2,2,2,2,2,2,2,2,2,2,2,2,2,2,2,4),(-30.3874064632604,
-30.2849996850917,-29.9770449392946,-29.6669697019036,-29.3531945565624,
-29.0461403261237,-28.7334656171847,-28.4237557504156,-28.1155642693923,
-27.800101850319,-27.4925185322491,-27.1817568932496,-26.8691509574993,
-26.5619592729381,-26.2485379032423,-25.9395212737839,-25.6306633294113,
-25.3825818071783),.UNSPECIFIED.);
#356=B_SPLINE_CURVE_WITH_KNOTS('',3,(#25733,#25734,#25735,#25736,#25737,
#25738,#25739,#25740,#25741,#25742,#25743,#25744,#25745,#25746,#25747,#25748,
#25749,#25750,#25751,#25752,#25753,#25754,#25755,#25756,#25757,#25758,#25759,
#25760,#25761,#25762,#25763,#25764,#25765,#25766,#25767,#25768),
 .UNSPECIFIED.,.F.,.F.,(4,2,2,2,2,2,2,2,2,2,2,2,2,2,2,2,2,4),(-87.1467179399563,
-87.08588220081,-86.7770149001574,-86.4633883814524,-86.156129319966,-85.8437993712712,
-85.5328468320979,-85.2253306548538,-84.909667125882,-84.6013169568405,
-84.2918124156487,-83.9789458786145,-83.6718751054293,-83.3584307994978,
-83.0481807364898,-82.7403442197742,-82.425419395495,-82.1419590834687),
 .UNSPECIFIED.);
#357=B_SPLINE_CURVE_WITH_KNOTS('',3,(#25769,#25770,#25771,#25772,#25773,
#25774,#25775,#25776,#25777,#25778,#25779,#25780,#25781,#25782,#25783,#25784,
#25785,#25786,#25787,#25788,#25789,#25790,#25791,#25792,#25793,#25794,#25795,
#25796,#25797,#25798,#25799,#25800,#25801,#25802,#25803,#25804),
 .UNSPECIFIED.,.F.,.F.,(4,2,2,2,2,2,2,2,2,2,2,2,2,2,2,2,2,4),(-25.3825818071783,
-25.3144209224753,-25.0070148119768,-24.695513470675,-24.3838588306673,
-24.0763438668322,-23.7621327140135,-23.4535946485024,-23.1440257555464,
-22.8289201864819,-22.5217486530133,-22.2096453156183,-21.8990366757631,
-21.5912311755097,-21.2763751382008,-20.9683801793135,-20.6581934941524,
-20.3765334205341),.UNSPECIFIED.);
#358=B_SPLINE_CURVE_WITH_KNOTS('',3,(#25809,#25810,#25811,#25812,#25813,
#25814,#25815,#25816,#25817,#25818,#25819,#25820,#25821,#25822,#25823,#25824,
#25825,#25826,#25827,#25828,#25829,#25830,#25831,#25832,#25833,#25834,#25835,
#25836,#25837,#25838,#25839,#25840,#25841,#25842,#25843,#25844),
 .UNSPECIFIED.,.F.,.F.,(4,2,2,2,2,2,2,2,2,2,2,2,2,2,2,2,2,4),(-92.1499753716227,
-92.0541924144739,-91.7464836512906,-91.4316182443593,-91.123873592165,
-90.8136895664306,-90.5015858623512,-90.1946170421438,-89.8800580960553,
-89.5705068478487,-89.2623020321016,-88.9481047839233,-88.6407047453379,
-88.3295157048067,-88.0180385885635,-87.7108841615196,-87.3948832438076,
-87.1467179399563),.UNSPECIFIED.);
#359=B_SPLINE_CURVE_WITH_KNOTS('',3,(#25845,#25846,#25847,#25848,#25849,
#25850,#25851,#25852,#25853,#25854,#25855,#25856,#25857,#25858,#25859,#25860,
#25861,#25862,#25863,#25864,#25865,#25866,#25867,#25868,#25869,#25870,#25871,
#25872,#25873,#25874,#25875,#25876,#25877,#25878,#25879,#25880,#25881,#25882),
 .UNSPECIFIED.,.F.,.F.,(4,2,2,2,2,2,2,2,2,2,2,2,2,2,2,2,2,2,4),(-20.3765334205341,
-20.3444276288399,-20.0373012529877,-19.7245103792346,-19.4147808169846,
-19.1064828976576,-18.7909014347054,-18.4832658461886,-18.1723886302269,
-17.859779364247,-17.5525032859371,-17.2389622676149,-16.929912818555,-16.6209373331314,
-16.3045726743746,-15.9971019731104,-15.6854821421927,-15.373809691922,
-15.3702501983023),.UNSPECIFIED.);
#360=B_SPLINE_CURVE_WITH_KNOTS('',3,(#25887,#25888,#25889,#25890,#25891,
#25892,#25893,#25894,#25895,#25896,#25897,#25898,#25899,#25900,#25901,#25902,
#25903,#25904,#25905,#25906,#25907,#25908,#25909,#25910,#25911,#25912,#25913,
#25914,#25915,#25916,#25917,#25918,#25919,#25920,#25921,#25922),
 .UNSPECIFIED.,.F.,.F.,(4,2,2,2,2,2,2,2,2,2,2,2,2,2,2,2,2,4),(-97.1531123408846,
-97.0224344199092,-96.7153844107451,-96.3995709672319,-96.0906238614074,
-95.7818917441421,-95.468319396795,-95.1611437241807,-94.848980193566,-94.5380842326777,
-94.230683440607,-93.9150755558694,-93.6067873912186,-93.2974317275935,
-92.9846220740555,-92.6776466084498,-92.3643825150026,-92.1499753716227),
 .UNSPECIFIED.);
#361=B_SPLINE_CURVE_WITH_KNOTS('',3,(#25923,#25924,#25925,#25926,#25927,
#25928,#25929,#25930,#25931,#25932,#25933,#25934,#25935,#25936,#25937,#25938,
#25939,#25940,#25941,#25942,#25943,#25944,#25945,#25946,#25947,#25948,#25949,
#25950,#25951,#25952,#25953,#25954,#25955,#25956,#25957,#25958),
 .UNSPECIFIED.,.F.,.F.,(4,2,2,2,2,2,2,2,2,2,2,2,2,2,2,2,2,4),(-15.3702501983023,
-15.0661991157021,-14.7518660086767,-14.4432814244333,-14.1335932317505,
-13.8184870007477,-13.5112399241302,-13.199012110835,-12.8883770031141,
-12.5804634365136,-12.2654797384413,-11.9574278997467,-11.6471167320135,
-11.3333408258675,-11.0261271421597,-10.713207177595,-10.4034401316373,
-10.3632048196668),.UNSPECIFIED.);
#362=B_SPLINE_CURVE_WITH_KNOTS('',3,(#25963,#25964,#25965,#25966,#25967,
#25968,#25969,#25970,#25971,#25972,#25973,#25974,#25975,#25976,#25977,#25978,
#25979,#25980,#25981,#25982,#25983,#25984,#25985,#25986,#25987,#25988,#25989,
#25990,#25991,#25992,#25993,#25994,#25995,#25996,#25997,#25998),
 .UNSPECIFIED.,.F.,.F.,(4,2,2,2,2,2,2,2,2,2,2,2,2,2,2,2,2,4),(-102.154690645213,
-101.987556999368,-101.680660695609,-101.367563783602,-101.057416380731,
-100.749820529465,-100.434996927783,-100.127309127348,-99.8172728811381,
-99.5052127675913,-99.1983359936896,-98.8839560771392,-98.5744524240466,
-98.2663725330835,-97.9522225174849,-97.6448926661825,-97.3338621803013,
-97.1531123408846),.UNSPECIFIED.);
#363=B_SPLINE_CURVE_WITH_KNOTS('',3,(#25999,#26000,#26001,#26002,#26003,
#26004,#26005,#26006,#26007,#26008,#26009,#26010,#26011,#26012,#26013,#26014,
#26015,#26016,#26017,#26018,#26019,#26020,#26021,#26022,#26023,#26024,#26025,
#26026,#26027,#26028,#26029,#26030,#26031,#26032,#26033,#26034),
 .UNSPECIFIED.,.F.,.F.,(4,2,2,2,2,2,2,2,2,2,2,2,2,2,2,2,2,4),(-10.3632048196668,
-10.0950221884295,-9.77930874677035,-9.47160476592912,-9.16059916985077,
-8.84796777245071,-8.54059274199171,-8.22691934660563,-7.91781988331396,
-7.6087138693961,-7.29221420374721,-6.98466339271854,-6.67291242750295,
-6.36120402867725,-6.05348387685949,-5.73901621000068,-5.43036858402126,
-5.35481643806797),.UNSPECIFIED.);
#364=B_SPLINE_CURVE_WITH_KNOTS('',3,(#26041,#26042,#26043,#26044,#26045,
#26046,#26047,#26048,#26049,#26050,#26051,#26052,#26053,#26054,#26055,#26056,
#26057,#26058,#26059,#26060,#26061,#26062,#26063,#26064,#26065,#26066,#26067,
#26068,#26069,#26070,#26071,#26072,#26073,#26074),.UNSPECIFIED.,.F.,.F.,
(4,2,2,2,2,2,2,2,2,2,2,2,2,2,2,2,4),(-106.874476063165,-106.604105121065,
-106.335692503319,-106.024296620534,-105.717335282747,-105.401696172039,
-105.092785792685,-104.784174219368,-104.470638521187,-104.163529711546,
-103.851518994257,-103.540662313851,-103.233361625802,-102.917791732759,
-102.609548098789,-102.300327250781,-102.154690645213),.UNSPECIFIED.);
#365=B_SPLINE_CURVE_WITH_KNOTS('',3,(#26075,#26076,#26077,#26078,#26079,
#26080,#26081,#26082,#26083,#26084,#26085,#26086,#26087,#26088,#26089,#26090,
#26091,#26092,#26093,#26094,#26095,#26096,#26097,#26098,#26099,#26100,#26101,
#26102,#26103,#26104,#26105,#26106,#26107,#26108,#26109,#26110),
 .UNSPECIFIED.,.F.,.F.,(4,2,2,2,2,2,2,2,2,2,2,2,2,2,2,2,2,4),(-5.35481643806797,
-5.12054865168396,-4.80542245821637,-4.49808485837619,-4.18572028641412,
-3.87504095581268,-3.56700601646214,-3.25188239828953,-2.94375766551306,
-2.63330989072761,-2.31950505958809,-2.01218970805026,-1.69912865491474,
-1.38930690941913,-1.08075630985562,-0.764898895970032,-0.457111115329854,
-0.346239220973872),.UNSPECIFIED.);
#366=B_SPLINE_CURVE_WITH_KNOTS('',3,(#26136,#26137,#26138,#26139,#26140,
#26141,#26142,#26143,#26144,#26145,#26146,#26147,#26148,#26149,#26150,#26151,
#26152,#26153,#26154,#26155,#26156,#26157,#26158,#26159,#26160,#26161,#26162,
#26163,#26164,#26165,#26166,#26167,#26168,#26169,#26170,#26171,#26172,#26173,
#26174,#26175,#26176,#26177,#26178,#26179,#26180,#26181,#26182,#26183,#26184,
#26185,#26186,#26187,#26188,#26189,#26190,#26191,#26192,#26193,#26194,#26195,
#26196,#26197,#26198,#26199,#26200,#26201,#26202),.UNSPECIFIED.,.F.,.F.,
(4,3,3,3,3,3,3,3,3,3,3,3,3,3,3,3,3,3,3,3,3,3,4),(0.0041660518496644,0.00459976416699748,
0.00546021591375608,0.0057750006243275,0.00639487133587175,0.00675437997785038,
0.00695961430893405,0.00757842774990045,0.00804854404194467,0.0081494048247967,
0.00869562607399181,0.00874625427688977,0.00920849047335839,0.00934270810603896,
0.00934406861977701,0.0106292804107923,0.0117265310038454,0.0119310362342275,
0.0125368230564803,0.0129107735164763,0.0132252002983218,0.0140854315246815,
0.0145193643624109),.UNSPECIFIED.);
#367=B_SPLINE_CURVE_WITH_KNOTS('',3,(#26203,#26204,#26205,#26206,#26207,
#26208,#26209,#26210,#26211,#26212,#26213,#26214,#26215,#26216,#26217,#26218,
#26219,#26220,#26221,#26222,#26223,#26224,#26225,#26226,#26227,#26228,#26229,
#26230,#26231,#26232,#26233,#26234,#26235,#26236,#26237,#26238,#26239,#26240,
#26241,#26242,#26243,#26244,#26245,#26246,#26247,#26248,#26249,#26250,#26251,
#26252,#26253,#26254,#26255,#26256,#26257,#26258,#26259,#26260,#26261,#26262,
#26263,#26264,#26265,#26266,#26267,#26268,#26269),.UNSPECIFIED.,.F.,.F.,
(4,3,3,3,3,3,3,3,3,3,3,3,3,3,3,3,3,3,3,3,3,3,4),(0.0041660518496669,0.0045997641669973,
0.00546021591375601,0.00577500062432757,0.00639487133588581,0.00675437997785032,
0.0069596143089341,0.00757842774983116,0.00804854404194462,0.00814940482479665,
0.00869562607399177,0.00874625427688975,0.00920849047333203,0.00934270810603892,
0.00934406861977701,0.0106292804114527,0.0117265310038455,0.0119310362342275,
0.0125368230564929,0.0129107735164765,0.0132252002983218,0.0140854315246816,
0.0145193643624118),.UNSPECIFIED.);
#368=B_SPLINE_CURVE_WITH_KNOTS('',3,(#26271,#26272,#26273,#26274,#26275,
#26276,#26277,#26278,#26279,#26280,#26281,#26282,#26283,#26284),
 .UNSPECIFIED.,.F.,.F.,(4,2,2,2,2,2,4),(-1.62358010524267,-1.32771579098637,
-1.0654737946073,-0.587083880817408,-0.264803320204801,-0.13597564184897,
0.),.UNSPECIFIED.);
#369=B_SPLINE_CURVE_WITH_KNOTS('',3,(#26288,#26289,#26290,#26291,#26292,
#26293,#26294,#26295,#26296,#26297,#26298,#26299,#26300,#26301,#26302,#26303,
#26304,#26305),.UNSPECIFIED.,.F.,.F.,(4,2,2,2,2,2,2,2,4),(-3.97757183645169,
-3.73001710320254,-3.47073400331661,-3.19180345145064,-2.83616150801241,
-2.51533726294721,-2.3691450825456,-2.0816506234592,-1.94059934416272),
 .UNSPECIFIED.);
#370=B_SPLINE_CURVE_WITH_KNOTS('',3,(#26309,#26310,#26311,#26312,#26313,
#26314,#26315,#26316,#26317,#26318,#26319,#26320,#26321,#26322,#26323,#26324,
#26325,#26326),.UNSPECIFIED.,.F.,.F.,(4,2,2,2,2,2,2,2,4),(-1.94059934416272,
-1.80303531466732,-1.51989931485796,-1.21685973325026,-0.90441123218411,
-0.606202781914648,-0.343816058000839,-0.168665484648542,0.),
 .UNSPECIFIED.);
#371=B_SPLINE_CURVE_WITH_KNOTS('',3,(#26328,#26329,#26330,#26331,#26332,
#26333),.UNSPECIFIED.,.F.,.F.,(4,2,4),(-0.346239220973872,-0.227029016346038,
-9.99999999473644E-7),.UNSPECIFIED.);
#372=B_SPLINE_CURVE_WITH_KNOTS('',3,(#26336,#26337,#26338,#26339,#26340,
#26341,#26342,#26343,#26344,#26345,#26346,#26347,#26348,#26349,#26350,#26351),
 .UNSPECIFIED.,.F.,.F.,(4,3,3,3,3,4),(0.,0.000451322032191559,0.000929732914751349,
0.00118344017626207,0.00236688035252415,0.0047337607050483),
 .UNSPECIFIED.);
#373=B_SPLINE_CURVE_WITH_KNOTS('',3,(#26352,#26353,#26354,#26355,#26356,
#26357,#26358,#26359,#26360,#26361,#26362,#26363,#26364,#26365,#26366,#26367,
#26368,#26369,#26370,#26371,#26372,#26373,#26374,#26375,#26376,#26377,#26378,
#26379,#26380,#26381,#26382,#26383,#26384,#26385,#26386,#26387,#26388,#26389,
#26390,#26391),.UNSPECIFIED.,.F.,.F.,(4,3,3,3,3,3,3,3,3,3,3,3,3,4),(0.,
0.000185189249441203,0.000368062392512153,0.000370402020091198,0.000660760771445963,
0.000736124785024307,0.000740751361344412,0.00110965157437254,0.00147224957004861,
0.00147684472482692,0.00187750418039922,0.00220912636931071,0.00266911044484345,
0.0029444991400972),.UNSPECIFIED.);
#374=B_SPLINE_CURVE_WITH_KNOTS('',3,(#26393,#26394,#26395,#26396,#26397,
#26398,#26399,#26400,#26401,#26402,#26403,#26404,#26405,#26406,#26407,#26408,
#26409,#26410,#26411,#26412,#26413,#26414,#26415,#26416,#26417,#26418,#26419,
#26420,#26421,#26422,#26423,#26424,#26425,#26426,#26427,#26428,#26429,#26430,
#26431,#26432,#26433,#26434,#26435),.UNSPECIFIED.,.F.,.F.,(4,3,3,3,3,3,
3,3,3,3,3,3,3,3,4),(-1.60764784209641E-5,0.000499411850648658,0.000723635622661751,
0.000723642899130192,0.00103927233191355,0.0013403986652088,0.0014632911881516,
0.00146336227668135,0.0018331686514735,0.00220304610996557,0.0022030816542325,
0.00257292357087475,0.00257294134300808,0.00275788190338485,0.00294280103178366),
 .UNSPECIFIED.);
#375=B_SPLINE_CURVE_WITH_KNOTS('',3,(#26436,#26437,#26438,#26439,#26440,
#26441,#26442,#26443,#26444,#26445,#26446,#26447,#26448),.UNSPECIFIED.,
 .F.,.F.,(4,3,3,3,4),(0.,0.00234949256753247,0.00326816604257249,0.00408172543590533,
0.00469898513506494),.UNSPECIFIED.);
#376=B_SPLINE_CURVE_WITH_KNOTS('',3,(#26451,#26452,#26453,#26454,#26455,
#26456,#26457,#26458,#26459,#26460,#26461,#26462,#26463,#26464,#26465,#26466),
 .UNSPECIFIED.,.F.,.F.,(4,3,3,3,3,4),(0.,0.000451322031352851,0.000929732913567863,
0.00118344017626208,0.00236688035252417,0.00473376070504833),
 .UNSPECIFIED.);
#377=B_SPLINE_CURVE_WITH_KNOTS('',3,(#26467,#26468,#26469,#26470,#26471,
#26472,#26473,#26474,#26475,#26476,#26477,#26478,#26479,#26480,#26481,#26482,
#26483,#26484,#26485,#26486,#26487,#26488,#26489,#26490,#26491,#26492,#26493,
#26494,#26495,#26496,#26497,#26498,#26499,#26500,#26501,#26502,#26503),
 .UNSPECIFIED.,.F.,.F.,(4,3,3,3,3,3,3,3,3,3,3,3,4),(0.,0.000186086495974917,
0.000372163572863526,0.000372184889337349,0.000744327145727053,0.000744369778660529,
0.00111655466602905,0.0014886542914541,0.00148873955732231,0.00223298143718115,
0.00223309919665271,0.00286524466138102,0.00297730858290821),
 .UNSPECIFIED.);
#378=B_SPLINE_CURVE_WITH_KNOTS('',3,(#26505,#26506,#26507,#26508,#26509,
#26510,#26511,#26512,#26513,#26514,#26515,#26516,#26517,#26518,#26519,#26520,
#26521,#26522,#26523,#26524,#26525,#26526,#26527,#26528,#26529,#26530,#26531,
#26532,#26533,#26534,#26535,#26536,#26537,#26538,#26539,#26540,#26541,#26542,
#26543,#26544,#26545,#26546,#26547),.UNSPECIFIED.,.F.,.F.,(4,3,3,3,3,3,
3,3,3,3,3,3,3,3,4),(-1.60764784223026E-5,0.000499412098106437,0.000723635622661197,
0.000723642899128064,0.00103927233247834,0.00134039866621365,0.00146329118815029,
0.00146336227667843,0.00183316865147226,0.00220304610996427,0.0022030816542288,
0.00257292357087343,0.00257294134300398,0.00275788190338312,0.00294280103177916),
 .UNSPECIFIED.);
#379=B_SPLINE_CURVE_WITH_KNOTS('',3,(#26548,#26549,#26550,#26551,#26552,
#26553,#26554,#26555,#26556,#26557,#26558,#26559,#26560),.UNSPECIFIED.,
 .F.,.F.,(4,3,3,3,4),(0.,0.002349492567534,0.00326816604266149,0.00408172543673988,
0.004698985135068),.UNSPECIFIED.);
#380=B_SPLINE_CURVE_WITH_KNOTS('',3,(#28354,#28355,#28356,#28357,#28358,
#28359,#28360,#28361,#28362,#28363),.UNSPECIFIED.,.F.,.F.,(4,2,2,2,4),(-1.97874132814648E-5,
0.00222205868858777,0.00278252021405508,0.00334298173952239,0.004463904790457),
 .UNSPECIFIED.);
#381=B_SPLINE_CURVE_WITH_KNOTS('',3,(#28455,#28456,#28457,#28458,#28459,
#28460,#28461,#28462,#28463,#28464,#28465,#28466,#28467,#28468,#28469,#28470,
#28471,#28472,#28473,#28474,#28475,#28476,#28477,#28478,#28479,#28480,#28481,
#28482,#28483,#28484,#28485,#28486,#28487,#28488,#28489,#28490,#28491,#28492,
#28493,#28494,#28495,#28496,#28497,#28498,#28499,#28500,#28501,#28502,#28503),
 .UNSPECIFIED.,.F.,.F.,(4,3,3,3,3,3,3,3,3,3,3,3,3,3,3,3,4),(0.,0.000379018093662348,
0.000744171494405515,0.00108379438629942,0.00140978955393366,0.00173094370171073,
0.00202840150890502,0.0020520978494878,0.00232114678039188,0.00262671080521888,
0.00291522316429607,0.00307814677423169,0.00327435230353986,0.00350085469361757,
0.00372101287058707,0.0039314003020558,0.00410419569897559),
 .UNSPECIFIED.);
#382=B_SPLINE_CURVE_WITH_KNOTS('',3,(#28505,#28506,#28507,#28508,#28509,
#28510,#28511,#28512,#28513,#28514,#28515,#28516,#28517,#28518,#28519,#28520,
#28521,#28522,#28523,#28524,#28525,#28526,#28527,#28528,#28529,#28530,#28531,
#28532,#28533,#28534,#28535,#28536,#28537,#28538,#28539,#28540,#28541,#28542,
#28543,#28544,#28545,#28546,#28547),.UNSPECIFIED.,.F.,.F.,(4,3,3,3,3,3,
3,3,3,3,3,3,3,3,4),(0.,0.000237141843545166,0.00048768786178728,0.000757439823406238,
0.0010271917850252,0.00130827499283397,0.00160260588705221,0.0017756125446872,
0.00205438357005039,0.002361793104946,0.00268278078634015,0.00301878732570562,
0.00337857137823455,0.00376136364485667,0.00410876714010079),
 .UNSPECIFIED.);
#383=B_SPLINE_CURVE_WITH_KNOTS('',3,(#28579,#28580,#28581,#28582,#28583,
#28584,#28585,#28586,#28587,#28588,#28589,#28590),.UNSPECIFIED.,.F.,.F.,
(4,2,2,2,2,4),(9.92648521184955E-17,0.00111453019999537,0.00167179529999301,
0.00222906039999065,0.00334359059998592,0.0044581207999812),
 .UNSPECIFIED.);
#384=B_SPLINE_CURVE_WITH_KNOTS('',3,(#28622,#28623,#28624,#28625,#28626,
#28627,#28628,#28629,#28630,#28631),.UNSPECIFIED.,.F.,.F.,(4,2,2,2,4),(-1.97874132811905E-5,
0.00222205868858802,0.00278252021405532,0.00334298173952263,0.00446390479045723),
 .UNSPECIFIED.);
#385=B_SPLINE_CURVE_WITH_KNOTS('',3,(#28723,#28724,#28725,#28726,#28727,
#28728,#28729,#28730,#28731,#28732,#28733,#28734,#28735,#28736,#28737,#28738,
#28739,#28740,#28741,#28742,#28743,#28744,#28745,#28746,#28747,#28748,#28749,
#28750,#28751,#28752,#28753,#28754,#28755,#28756,#28757,#28758,#28759,#28760,
#28761,#28762,#28763,#28764,#28765,#28766,#28767,#28768,#28769,#28770,#28771),
 .UNSPECIFIED.,.F.,.F.,(4,3,3,3,3,3,3,3,3,3,3,3,3,3,3,3,4),(0.,0.000379018092565528,
0.00074417149243569,0.00108379438364185,0.00140978955067594,0.00173094370008185,
0.0020284015067481,0.00205209784948776,0.0023211467803934,0.00262671080542169,
0.00291522316466974,0.00307814677423164,0.00327435230354241,0.00350085469357018,
0.00372101287049888,0.00393140030193836,0.00410419569897552),
 .UNSPECIFIED.);
#386=B_SPLINE_CURVE_WITH_KNOTS('',3,(#28773,#28774,#28775,#28776,#28777,
#28778,#28779,#28780,#28781,#28782,#28783,#28784,#28785,#28786,#28787,#28788,
#28789,#28790,#28791,#28792,#28793,#28794,#28795,#28796,#28797,#28798,#28799,
#28800,#28801,#28802,#28803,#28804,#28805,#28806,#28807,#28808,#28809,#28810,
#28811,#28812,#28813,#28814,#28815),.UNSPECIFIED.,.F.,.F.,(4,3,3,3,3,3,
3,3,3,3,3,3,3,3,4),(0.,0.000237141844569432,0.000487687864522147,0.000757439824773671,
0.00102719178502519,0.00130827499701704,0.00160260589471355,0.00177561254466418,
0.00205438357005039,0.00236179310188202,0.00268278077972904,0.00301878731501841,
0.00337857136277177,0.00376136362374476,0.00410876714010078),
 .UNSPECIFIED.);
#387=B_SPLINE_CURVE_WITH_KNOTS('',3,(#28847,#28848,#28849,#28850,#28851,
#28852,#28853,#28854,#28855,#28856,#28857,#28858),.UNSPECIFIED.,.F.,.F.,
(4,2,2,2,2,4),(9.56971647899676E-17,0.00111453019999533,0.00167179529999294,
0.00222906039999056,0.00334359059998579,0.00445812079998102),
 .UNSPECIFIED.);
#456=(
BOUNDED_CURVE()
B_SPLINE_CURVE(2,(#23076,#23077,#23078,#23079,#23080,#23081,#23082,#23083,
#23084,#23085,#23086),.UNSPECIFIED.,.F.,.F.)
B_SPLINE_CURVE_WITH_KNOTS((3,2,2,2,2,3),(0.00349366271704399,0.00454545454545455,
0.00909090909090909,0.0136363636363636,0.0181818181818182,0.0227272727272727),
 .UNSPECIFIED.)
CURVE()
GEOMETRIC_REPRESENTATION_ITEM()
RATIONAL_B_SPLINE_CURVE((0.982590712260093,0.988674761632765,1.,0.951056516295154,
1.,0.951056516295154,1.,0.951056516295154,1.,0.951056516295154,1.))
REPRESENTATION_ITEM('')
);
#457=(
BOUNDED_CURVE()
B_SPLINE_CURVE(2,(#23089,#23090,#23091,#23092,#23093),.UNSPECIFIED.,.F.,
 .F.)
B_SPLINE_CURVE_WITH_KNOTS((3,2,3),(0.0151375700072014,0.0184727520515342,
0.0230909400644179),.UNSPECIFIED.)
CURVE()
GEOMETRIC_REPRESENTATION_ITEM()
RATIONAL_B_SPLINE_CURVE((0.980360524940442,0.964653793309387,1.,0.951056516295154,
1.))
REPRESENTATION_ITEM('')
);
#458=(
BOUNDED_CURVE()
B_SPLINE_CURVE(2,(#23098,#23099,#23100,#23101,#23102,#23103,#23104,#23105,
#23106,#23107,#23108,#23109,#23110,#23111,#23112,#23113,#23114,#23115,#23116,
#23117,#23118),.UNSPECIFIED.,.F.,.F.)
B_SPLINE_CURVE_WITH_KNOTS((3,2,2,2,2,2,2,2,2,2,3),(0.0227272727272727,0.0272727272727273,
0.0318181818181818,0.0363636363636364,0.0409090909090909,0.0454545454545455,
0.05,0.0545454545454545,0.0590909090909091,0.0636363636363636,0.0681818181818182),
 .UNSPECIFIED.)
CURVE()
GEOMETRIC_REPRESENTATION_ITEM()
RATIONAL_B_SPLINE_CURVE((1.,0.951056516295154,1.,0.951056516295154,1.,0.951056516295154,
1.,0.951056516295154,1.,0.951056516295154,1.,0.951056516295154,1.,0.951056516295154,
1.,0.951056516295154,1.,0.951056516295154,1.,0.951056516295154,1.))
REPRESENTATION_ITEM('')
);
#459=(
BOUNDED_CURVE()
B_SPLINE_CURVE(2,(#23119,#23120,#23121,#23122,#23123,#23124,#23125,#23126,
#23127,#23128,#23129,#23130,#23131,#23132,#23133,#23134,#23135,#23136,#23137,
#23138,#23139),.UNSPECIFIED.,.F.,.F.)
B_SPLINE_CURVE_WITH_KNOTS((3,2,2,2,2,2,2,2,2,2,3),(0.0230909400644179,0.0277091280773016,
0.0323273160901852,0.0369455041030689,0.0415636921159526,0.0461818801288363,
0.05080006814172,0.0554182561546037,0.0600364441674874,0.0646546321803711,
0.0692728201932548),.UNSPECIFIED.)
CURVE()
GEOMETRIC_REPRESENTATION_ITEM()
RATIONAL_B_SPLINE_CURVE((1.,0.951056516295154,1.,0.951056516295154,1.,0.951056516295154,
1.,0.951056516295154,1.,0.951056516295154,1.,0.951056516295154,1.,0.951056516295154,
1.,0.951056516295154,1.,0.951056516295154,1.,0.951056516295154,1.))
REPRESENTATION_ITEM('')
);
#460=(
BOUNDED_CURVE()
B_SPLINE_CURVE(2,(#23144,#23145,#23146,#23147,#23148,#23149,#23150,#23151,
#23152,#23153,#23154,#23155,#23156,#23157,#23158,#23159,#23160,#23161,#23162,
#23163,#23164),.UNSPECIFIED.,.F.,.F.)
B_SPLINE_CURVE_WITH_KNOTS((3,2,2,2,2,2,2,2,2,2,3),(0.0681818181818182,0.0727272727272727,
0.0772727272727273,0.0818181818181818,0.0863636363636364,0.0909090909090909,
0.0954545454545455,0.1,0.104545454545455,0.109090909090909,0.113636363636364),
 .UNSPECIFIED.)
CURVE()
GEOMETRIC_REPRESENTATION_ITEM()
RATIONAL_B_SPLINE_CURVE((1.,0.951056516295154,1.,0.951056516295154,1.,0.951056516295154,
1.,0.951056516295154,1.,0.951056516295154,1.,0.951056516295154,1.,0.951056516295154,
1.,0.951056516295154,1.,0.951056516295154,1.,0.951056516295154,1.))
REPRESENTATION_ITEM('')
);
#461=(
BOUNDED_CURVE()
B_SPLINE_CURVE(2,(#23165,#23166,#23167,#23168,#23169,#23170,#23171,#23172,
#23173,#23174,#23175,#23176,#23177,#23178,#23179,#23180,#23181,#23182,#23183,
#23184,#23185),.UNSPECIFIED.,.F.,.F.)
B_SPLINE_CURVE_WITH_KNOTS((3,2,2,2,2,2,2,2,2,2,3),(0.0692728201932548,0.0738910082061384,
0.0785091962190222,0.0831273842319059,0.0877455722447895,0.0923637602576732,
0.0969819482705569,0.101600136283441,0.106218324296324,0.110836512309208,
0.115454700322092),.UNSPECIFIED.)
CURVE()
GEOMETRIC_REPRESENTATION_ITEM()
RATIONAL_B_SPLINE_CURVE((1.,0.951056516295154,1.,0.951056516295154,1.,0.951056516295154,
1.,0.951056516295154,1.,0.951056516295154,1.,0.951056516295154,1.,0.951056516295154,
1.,0.951056516295154,1.,0.951056516295154,1.,0.951056516295154,1.))
REPRESENTATION_ITEM('')
);
#462=(
BOUNDED_CURVE()
B_SPLINE_CURVE(2,(#23190,#23191,#23192,#23193,#23194,#23195,#23196,#23197,
#23198,#23199,#23200,#23201,#23202,#23203,#23204,#23205,#23206,#23207,#23208,
#23209,#23210),.UNSPECIFIED.,.F.,.F.)
B_SPLINE_CURVE_WITH_KNOTS((3,2,2,2,2,2,2,2,2,2,3),(0.113636363636364,0.118181818181818,
0.122727272727273,0.127272727272727,0.131818181818182,0.136363636363636,
0.140909090909091,0.145454545454545,0.15,0.154545454545455,0.159090909090909),
 .UNSPECIFIED.)
CURVE()
GEOMETRIC_REPRESENTATION_ITEM()
RATIONAL_B_SPLINE_CURVE((1.,0.951056516295154,1.,0.951056516295154,1.,0.951056516295154,
1.,0.951056516295154,1.,0.951056516295154,1.,0.951056516295154,1.,0.951056516295154,
1.,0.951056516295154,1.,0.951056516295154,1.,0.951056516295154,1.))
REPRESENTATION_ITEM('')
);
#463=(
BOUNDED_CURVE()
B_SPLINE_CURVE(2,(#23211,#23212,#23213,#23214,#23215,#23216,#23217,#23218,
#23219,#23220,#23221,#23222,#23223,#23224,#23225,#23226,#23227,#23228,#23229,
#23230,#23231),.UNSPECIFIED.,.F.,.F.)
B_SPLINE_CURVE_WITH_KNOTS((3,2,2,2,2,2,2,2,2,2,3),(0.115454700322092,0.120072888334975,
0.124691076347859,0.129309264360743,0.133927452373626,0.13854564038651,
0.143163828399394,0.147782016412278,0.152400204425161,0.157018392438045,
0.161636580450929),.UNSPECIFIED.)
CURVE()
GEOMETRIC_REPRESENTATION_ITEM()
RATIONAL_B_SPLINE_CURVE((1.,0.951056516295154,1.,0.951056516295154,1.,0.951056516295154,
1.,0.951056516295154,1.,0.951056516295154,1.,0.951056516295154,1.,0.951056516295154,
1.,0.951056516295154,1.,0.951056516295154,1.,0.951056516295154,1.))
REPRESENTATION_ITEM('')
);
#464=(
BOUNDED_CURVE()
B_SPLINE_CURVE(2,(#23236,#23237,#23238,#23239,#23240,#23241,#23242,#23243,
#23244,#23245,#23246,#23247,#23248,#23249,#23250,#23251,#23252,#23253,#23254,
#23255,#23256),.UNSPECIFIED.,.F.,.F.)
B_SPLINE_CURVE_WITH_KNOTS((3,2,2,2,2,2,2,2,2,2,3),(0.159090909090909,0.163636363636364,
0.168181818181818,0.172727272727273,0.177272727272727,0.181818181818182,
0.186363636363636,0.190909090909091,0.195454545454545,0.2,0.204545454545455),
 .UNSPECIFIED.)
CURVE()
GEOMETRIC_REPRESENTATION_ITEM()
RATIONAL_B_SPLINE_CURVE((1.,0.951056516295154,1.,0.951056516295154,1.,0.951056516295154,
1.,0.951056516295154,1.,0.951056516295154,1.,0.951056516295154,1.,0.951056516295154,
1.,0.951056516295154,1.,0.951056516295154,1.,0.951056516295154,1.))
REPRESENTATION_ITEM('')
);
#465=(
BOUNDED_CURVE()
B_SPLINE_CURVE(2,(#23257,#23258,#23259,#23260,#23261,#23262,#23263,#23264,
#23265,#23266,#23267,#23268,#23269,#23270,#23271,#23272,#23273,#23274,#23275,
#23276,#23277),.UNSPECIFIED.,.F.,.F.)
B_SPLINE_CURVE_WITH_KNOTS((3,2,2,2,2,2,2,2,2,2,3),(0.161636580450929,0.166254768463812,
0.170872956476696,0.17549114448958,0.180109332502463,0.184727520515347,
0.189345708528231,0.193963896541114,0.198582084553998,0.203200272566882,
0.207818460579765),.UNSPECIFIED.)
CURVE()
GEOMETRIC_REPRESENTATION_ITEM()
RATIONAL_B_SPLINE_CURVE((1.,0.951056516295154,1.,0.951056516295154,1.,0.951056516295154,
1.,0.951056516295154,1.,0.951056516295154,1.,0.951056516295154,1.,0.951056516295154,
1.,0.951056516295154,1.,0.951056516295154,1.,0.951056516295154,1.))
REPRESENTATION_ITEM('')
);
#466=(
BOUNDED_CURVE()
B_SPLINE_CURVE(2,(#23282,#23283,#23284,#23285,#23286,#23287,#23288,#23289,
#23290,#23291,#23292,#23293,#23294,#23295,#23296,#23297,#23298,#23299,#23300,
#23301,#23302),.UNSPECIFIED.,.F.,.F.)
B_SPLINE_CURVE_WITH_KNOTS((3,2,2,2,2,2,2,2,2,2,3),(0.204545454545455,0.209090909090909,
0.213636363636364,0.218181818181818,0.222727272727273,0.227272727272727,
0.231818181818182,0.236363636363636,0.240909090909091,0.245454545454545,
0.25),.UNSPECIFIED.)
CURVE()
GEOMETRIC_REPRESENTATION_ITEM()
RATIONAL_B_SPLINE_CURVE((1.,0.951056516295154,1.,0.951056516295154,1.,0.951056516295154,
1.,0.951056516295154,1.,0.951056516295154,1.,0.951056516295154,1.,0.951056516295154,
1.,0.951056516295154,1.,0.951056516295154,1.,0.951056516295154,1.))
REPRESENTATION_ITEM('')
);
#467=(
BOUNDED_CURVE()
B_SPLINE_CURVE(2,(#23303,#23304,#23305,#23306,#23307,#23308,#23309,#23310,
#23311,#23312,#23313,#23314,#23315,#23316,#23317,#23318,#23319,#23320,#23321,
#23322,#23323),.UNSPECIFIED.,.F.,.F.)
B_SPLINE_CURVE_WITH_KNOTS((3,2,2,2,2,2,2,2,2,2,3),(0.207818460579765,0.212436648592649,
0.217054836605533,0.221673024618417,0.2262912126313,0.230909400644184,0.235527588657068,
0.240145776669951,0.244763964682835,0.249382152695719,0.254000340708602),
 .UNSPECIFIED.)
CURVE()
GEOMETRIC_REPRESENTATION_ITEM()
RATIONAL_B_SPLINE_CURVE((1.,0.951056516295154,1.,0.951056516295154,1.,0.951056516295154,
1.,0.951056516295154,1.,0.951056516295154,1.,0.951056516295154,1.,0.951056516295154,
1.,0.951056516295154,1.,0.951056516295154,1.,0.951056516295154,1.))
REPRESENTATION_ITEM('')
);
#468=(
BOUNDED_CURVE()
B_SPLINE_CURVE(2,(#23328,#23329,#23330,#23331,#23332,#23333,#23334,#23335,
#23336,#23337,#23338,#23339,#23340,#23341,#23342,#23343,#23344,#23345,#23346,
#23347,#23348),.UNSPECIFIED.,.F.,.F.)
B_SPLINE_CURVE_WITH_KNOTS((3,2,2,2,2,2,2,2,2,2,3),(0.25,0.254545454545455,
0.259090909090909,0.263636363636364,0.268181818181818,0.272727272727273,
0.277272727272727,0.281818181818182,0.286363636363636,0.290909090909091,
0.295454545454545),.UNSPECIFIED.)
CURVE()
GEOMETRIC_REPRESENTATION_ITEM()
RATIONAL_B_SPLINE_CURVE((1.,0.951056516295154,1.,0.951056516295154,1.,0.951056516295154,
1.,0.951056516295154,1.,0.951056516295154,1.,0.951056516295154,1.,0.951056516295154,
1.,0.951056516295154,1.,0.951056516295154,1.,0.951056516295154,1.))
REPRESENTATION_ITEM('')
);
#469=(
BOUNDED_CURVE()
B_SPLINE_CURVE(2,(#23349,#23350,#23351,#23352,#23353,#23354,#23355,#23356,
#23357,#23358,#23359,#23360,#23361,#23362,#23363,#23364,#23365,#23366,#23367,
#23368,#23369),.UNSPECIFIED.,.F.,.F.)
B_SPLINE_CURVE_WITH_KNOTS((3,2,2,2,2,2,2,2,2,2,3),(0.254000340708602,0.258618528721486,
0.26323671673437,0.267854904747253,0.272473092760137,0.277091280773021,
0.281709468785904,0.286327656798788,0.290945844811672,0.295564032824556,
0.300182220837439),.UNSPECIFIED.)
CURVE()
GEOMETRIC_REPRESENTATION_ITEM()
RATIONAL_B_SPLINE_CURVE((1.,0.951056516295154,1.,0.951056516295154,1.,0.951056516295154,
1.,0.951056516295154,1.,0.951056516295154,1.,0.951056516295154,1.,0.951056516295154,
1.,0.951056516295154,1.,0.951056516295154,1.,0.951056516295154,1.))
REPRESENTATION_ITEM('')
);
#470=(
BOUNDED_CURVE()
B_SPLINE_CURVE(2,(#23374,#23375,#23376,#23377,#23378,#23379,#23380,#23381,
#23382,#23383,#23384,#23385,#23386,#23387,#23388,#23389,#23390,#23391,#23392,
#23393,#23394),.UNSPECIFIED.,.F.,.F.)
B_SPLINE_CURVE_WITH_KNOTS((3,2,2,2,2,2,2,2,2,2,3),(0.295454545454545,0.3,
0.304545454545455,0.309090909090909,0.313636363636364,0.318181818181818,
0.322727272727273,0.327272727272727,0.331818181818182,0.336363636363636,
0.340909090909091),.UNSPECIFIED.)
CURVE()
GEOMETRIC_REPRESENTATION_ITEM()
RATIONAL_B_SPLINE_CURVE((1.,0.951056516295154,1.,0.951056516295154,1.,0.951056516295154,
1.,0.951056516295154,1.,0.951056516295154,1.,0.951056516295154,1.,0.951056516295154,
1.,0.951056516295154,1.,0.951056516295154,1.,0.951056516295154,1.))
REPRESENTATION_ITEM('')
);
#471=(
BOUNDED_CURVE()
B_SPLINE_CURVE(2,(#23395,#23396,#23397,#23398,#23399,#23400,#23401,#23402,
#23403,#23404,#23405,#23406,#23407,#23408,#23409,#23410,#23411,#23412,#23413,
#23414,#23415),.UNSPECIFIED.,.F.,.F.)
B_SPLINE_CURVE_WITH_KNOTS((3,2,2,2,2,2,2,2,2,2,3),(0.300182220837439,0.304800408850323,
0.309418596863207,0.31403678487609,0.318654972888974,0.323273160901858,
0.327891348914741,0.332509536927625,0.337127724940509,0.341745912953392,
0.346364100966276),.UNSPECIFIED.)
CURVE()
GEOMETRIC_REPRESENTATION_ITEM()
RATIONAL_B_SPLINE_CURVE((1.,0.951056516295154,1.,0.951056516295154,1.,0.951056516295154,
1.,0.951056516295154,1.,0.951056516295154,1.,0.951056516295154,1.,0.951056516295154,
1.,0.951056516295154,1.,0.951056516295154,1.,0.951056516295154,1.))
REPRESENTATION_ITEM('')
);
#472=(
BOUNDED_CURVE()
B_SPLINE_CURVE(2,(#23420,#23421,#23422,#23423,#23424,#23425,#23426,#23427,
#23428,#23429,#23430,#23431,#23432,#23433,#23434,#23435,#23436,#23437,#23438,
#23439,#23440),.UNSPECIFIED.,.F.,.F.)
B_SPLINE_CURVE_WITH_KNOTS((3,2,2,2,2,2,2,2,2,2,3),(0.340909090909091,0.345454545454546,
0.35,0.354545454545455,0.359090909090909,0.363636363636364,0.368181818181818,
0.372727272727273,0.377272727272727,0.381818181818182,0.386363636363636),
 .UNSPECIFIED.)
CURVE()
GEOMETRIC_REPRESENTATION_ITEM()
RATIONAL_B_SPLINE_CURVE((1.,0.951056516295154,1.,0.951056516295154,1.,0.951056516295154,
1.,0.951056516295154,1.,0.951056516295154,1.,0.951056516295154,1.,0.951056516295154,
1.,0.951056516295154,1.,0.951056516295154,1.,0.951056516295154,1.))
REPRESENTATION_ITEM('')
);
#473=(
BOUNDED_CURVE()
B_SPLINE_CURVE(2,(#23441,#23442,#23443,#23444,#23445,#23446,#23447,#23448,
#23449,#23450,#23451,#23452,#23453,#23454,#23455,#23456,#23457,#23458,#23459,
#23460,#23461),.UNSPECIFIED.,.F.,.F.)
B_SPLINE_CURVE_WITH_KNOTS((3,2,2,2,2,2,2,2,2,2,3),(0.346364100966276,0.35098228897916,
0.355600476992044,0.360218665004927,0.364836853017811,0.369455041030695,
0.374073229043578,0.378691417056462,0.383309605069346,0.387927793082229,
0.392545981095113),.UNSPECIFIED.)
CURVE()
GEOMETRIC_REPRESENTATION_ITEM()
RATIONAL_B_SPLINE_CURVE((1.,0.951056516295154,1.,0.951056516295154,1.,0.951056516295154,
1.,0.951056516295154,1.,0.951056516295154,1.,0.951056516295154,1.,0.951056516295154,
1.,0.951056516295154,1.,0.951056516295154,1.,0.951056516295154,1.))
REPRESENTATION_ITEM('')
);
#474=(
BOUNDED_CURVE()
B_SPLINE_CURVE(2,(#23466,#23467,#23468,#23469,#23470,#23471,#23472,#23473,
#23474,#23475,#23476,#23477,#23478,#23479,#23480,#23481,#23482,#23483,#23484,
#23485,#23486),.UNSPECIFIED.,.F.,.F.)
B_SPLINE_CURVE_WITH_KNOTS((3,2,2,2,2,2,2,2,2,2,3),(0.386363636363636,0.390909090909091,
0.395454545454545,0.4,0.404545454545455,0.409090909090909,0.413636363636364,
0.418181818181818,0.422727272727273,0.427272727272727,0.431818181818182),
 .UNSPECIFIED.)
CURVE()
GEOMETRIC_REPRESENTATION_ITEM()
RATIONAL_B_SPLINE_CURVE((1.,0.951056516295154,1.,0.951056516295154,1.,0.951056516295154,
1.,0.951056516295154,1.,0.951056516295154,1.,0.951056516295154,1.,0.951056516295154,
1.,0.951056516295154,1.,0.951056516295154,1.,0.951056516295154,1.))
REPRESENTATION_ITEM('')
);
#475=(
BOUNDED_CURVE()
B_SPLINE_CURVE(2,(#23487,#23488,#23489,#23490,#23491,#23492,#23493,#23494,
#23495,#23496,#23497,#23498,#23499,#23500,#23501,#23502,#23503,#23504,#23505,
#23506,#23507),.UNSPECIFIED.,.F.,.F.)
B_SPLINE_CURVE_WITH_KNOTS((3,2,2,2,2,2,2,2,2,2,3),(0.392545981095113,0.397164169107997,
0.40178235712088,0.406400545133764,0.411018733146648,0.415636921159532,
0.420255109172415,0.424873297185299,0.429491485198183,0.434109673211066,
0.43872786122395),.UNSPECIFIED.)
CURVE()
GEOMETRIC_REPRESENTATION_ITEM()
RATIONAL_B_SPLINE_CURVE((1.,0.951056516295154,1.,0.951056516295154,1.,0.951056516295154,
1.,0.951056516295154,1.,0.951056516295154,1.,0.951056516295154,1.,0.951056516295154,
1.,0.951056516295154,1.,0.951056516295154,1.,0.951056516295154,1.))
REPRESENTATION_ITEM('')
);
#476=(
BOUNDED_CURVE()
B_SPLINE_CURVE(2,(#23512,#23513,#23514,#23515,#23516,#23517,#23518,#23519,
#23520,#23521,#23522,#23523,#23524,#23525,#23526,#23527,#23528,#23529,#23530,
#23531,#23532),.UNSPECIFIED.,.F.,.F.)
B_SPLINE_CURVE_WITH_KNOTS((3,2,2,2,2,2,2,2,2,2,3),(0.431818181818182,0.436363636363636,
0.440909090909091,0.445454545454545,0.45,0.454545454545455,0.459090909090909,
0.463636363636364,0.468181818181818,0.472727272727273,0.477272727272727),
 .UNSPECIFIED.)
CURVE()
GEOMETRIC_REPRESENTATION_ITEM()
RATIONAL_B_SPLINE_CURVE((1.,0.951056516295154,1.,0.951056516295154,1.,0.951056516295154,
1.,0.951056516295154,1.,0.951056516295154,1.,0.951056516295154,1.,0.951056516295154,
1.,0.951056516295154,1.,0.951056516295154,1.,0.951056516295154,1.))
REPRESENTATION_ITEM('')
);
#477=(
BOUNDED_CURVE()
B_SPLINE_CURVE(2,(#23533,#23534,#23535,#23536,#23537,#23538,#23539,#23540,
#23541,#23542,#23543,#23544,#23545,#23546,#23547,#23548,#23549,#23550,#23551,
#23552,#23553),.UNSPECIFIED.,.F.,.F.)
B_SPLINE_CURVE_WITH_KNOTS((3,2,2,2,2,2,2,2,2,2,3),(0.43872786122395,0.443346049236834,
0.447964237249717,0.452582425262601,0.457200613275485,0.461818801288368,
0.466436989301252,0.471055177314136,0.47567336532702,0.480291553339903,
0.484909741352787),.UNSPECIFIED.)
CURVE()
GEOMETRIC_REPRESENTATION_ITEM()
RATIONAL_B_SPLINE_CURVE((1.,0.951056516295154,1.,0.951056516295154,1.,0.951056516295154,
1.,0.951056516295154,1.,0.951056516295154,1.,0.951056516295154,1.,0.951056516295154,
1.,0.951056516295154,1.,0.951056516295154,1.,0.951056516295154,1.))
REPRESENTATION_ITEM('')
);
#478=(
BOUNDED_CURVE()
B_SPLINE_CURVE(2,(#23558,#23559,#23560,#23561,#23562,#23563,#23564,#23565,
#23566,#23567,#23568,#23569,#23570,#23571,#23572,#23573,#23574,#23575,#23576,
#23577,#23578),.UNSPECIFIED.,.F.,.F.)
B_SPLINE_CURVE_WITH_KNOTS((3,2,2,2,2,2,2,2,2,2,3),(0.477272727272727,0.481818181818182,
0.486363636363636,0.490909090909091,0.495454545454545,0.5,0.504545454545455,
0.509090909090909,0.513636363636364,0.518181818181818,0.522727272727273),
 .UNSPECIFIED.)
CURVE()
GEOMETRIC_REPRESENTATION_ITEM()
RATIONAL_B_SPLINE_CURVE((1.,0.951056516295154,1.,0.951056516295154,1.,0.951056516295154,
1.,0.951056516295154,1.,0.951056516295154,1.,0.951056516295154,1.,0.951056516295154,
1.,0.951056516295154,1.,0.951056516295154,1.,0.951056516295154,1.))
REPRESENTATION_ITEM('')
);
#479=(
BOUNDED_CURVE()
B_SPLINE_CURVE(2,(#23579,#23580,#23581,#23582,#23583,#23584,#23585,#23586,
#23587,#23588,#23589,#23590,#23591,#23592,#23593,#23594,#23595,#23596,#23597,
#23598,#23599),.UNSPECIFIED.,.F.,.F.)
B_SPLINE_CURVE_WITH_KNOTS((3,2,2,2,2,2,2,2,2,2,3),(0.484909741352787,0.489527929365671,
0.494146117378554,0.498764305391438,0.503382493404322,0.508000681417205,
0.512618869430089,0.517237057442973,0.521855245455856,0.52647343346874,
0.531091621481624),.UNSPECIFIED.)
CURVE()
GEOMETRIC_REPRESENTATION_ITEM()
RATIONAL_B_SPLINE_CURVE((1.,0.951056516295154,1.,0.951056516295154,1.,0.951056516295154,
1.,0.951056516295154,1.,0.951056516295154,1.,0.951056516295154,1.,0.951056516295154,
1.,0.951056516295154,1.,0.951056516295154,1.,0.951056516295154,1.))
REPRESENTATION_ITEM('')
);
#480=(
BOUNDED_CURVE()
B_SPLINE_CURVE(2,(#23604,#23605,#23606,#23607,#23608,#23609,#23610,#23611,
#23612,#23613,#23614,#23615,#23616,#23617,#23618,#23619,#23620,#23621,#23622,
#23623,#23624),.UNSPECIFIED.,.F.,.F.)
B_SPLINE_CURVE_WITH_KNOTS((3,2,2,2,2,2,2,2,2,2,3),(0.522727272727273,0.527272727272727,
0.531818181818182,0.536363636363636,0.540909090909091,0.545454545454545,
0.55,0.554545454545455,0.559090909090909,0.563636363636364,0.568181818181818),
 .UNSPECIFIED.)
CURVE()
GEOMETRIC_REPRESENTATION_ITEM()
RATIONAL_B_SPLINE_CURVE((1.,0.951056516295154,1.,0.951056516295154,1.,0.951056516295154,
1.,0.951056516295154,1.,0.951056516295154,1.,0.951056516295154,1.,0.951056516295154,
1.,0.951056516295154,1.,0.951056516295154,1.,0.951056516295154,1.))
REPRESENTATION_ITEM('')
);
#481=(
BOUNDED_CURVE()
B_SPLINE_CURVE(2,(#23625,#23626,#23627,#23628,#23629,#23630,#23631,#23632,
#23633,#23634,#23635,#23636,#23637,#23638,#23639,#23640,#23641,#23642,#23643,
#23644,#23645),.UNSPECIFIED.,.F.,.F.)
B_SPLINE_CURVE_WITH_KNOTS((3,2,2,2,2,2,2,2,2,2,3),(0.531091621481624,0.535709809494508,
0.540327997507391,0.544946185520275,0.549564373533159,0.554182561546042,
0.558800749558926,0.56341893757181,0.568037125584693,0.572655313597577,
0.577273501610461),.UNSPECIFIED.)
CURVE()
GEOMETRIC_REPRESENTATION_ITEM()
RATIONAL_B_SPLINE_CURVE((1.,0.951056516295154,1.,0.951056516295154,1.,0.951056516295154,
1.,0.951056516295154,1.,0.951056516295154,1.,0.951056516295154,1.,0.951056516295154,
1.,0.951056516295154,1.,0.951056516295154,1.,0.951056516295154,1.))
REPRESENTATION_ITEM('')
);
#482=(
BOUNDED_CURVE()
B_SPLINE_CURVE(2,(#23650,#23651,#23652,#23653,#23654,#23655,#23656,#23657,
#23658,#23659,#23660,#23661,#23662,#23663,#23664,#23665,#23666,#23667,#23668,
#23669,#23670),.UNSPECIFIED.,.F.,.F.)
B_SPLINE_CURVE_WITH_KNOTS((3,2,2,2,2,2,2,2,2,2,3),(0.568181818181818,0.572727272727273,
0.577272727272727,0.581818181818182,0.586363636363636,0.590909090909091,
0.595454545454546,0.6,0.604545454545454,0.609090909090909,0.613636363636364),
 .UNSPECIFIED.)
CURVE()
GEOMETRIC_REPRESENTATION_ITEM()
RATIONAL_B_SPLINE_CURVE((1.,0.951056516295154,1.,0.951056516295154,1.,0.951056516295154,
1.,0.951056516295154,1.,0.951056516295154,1.,0.951056516295154,1.,0.951056516295154,
1.,0.951056516295154,1.,0.951056516295154,1.,0.951056516295154,1.))
REPRESENTATION_ITEM('')
);
#483=(
BOUNDED_CURVE()
B_SPLINE_CURVE(2,(#23671,#23672,#23673,#23674,#23675,#23676,#23677,#23678,
#23679,#23680,#23681,#23682,#23683,#23684,#23685,#23686,#23687,#23688,#23689,
#23690,#23691),.UNSPECIFIED.,.F.,.F.)
B_SPLINE_CURVE_WITH_KNOTS((3,2,2,2,2,2,2,2,2,2,3),(0.577273501610461,0.581891689623344,
0.586509877636228,0.591128065649112,0.595746253661995,0.600364441674879,
0.604982629687763,0.609600817700647,0.61421900571353,0.618837193726414,
0.623455381739298),.UNSPECIFIED.)
CURVE()
GEOMETRIC_REPRESENTATION_ITEM()
RATIONAL_B_SPLINE_CURVE((1.,0.951056516295154,1.,0.951056516295154,1.,0.951056516295154,
1.,0.951056516295154,1.,0.951056516295154,1.,0.951056516295154,1.,0.951056516295154,
1.,0.951056516295154,1.,0.951056516295154,1.,0.951056516295154,1.))
REPRESENTATION_ITEM('')
);
#484=(
BOUNDED_CURVE()
B_SPLINE_CURVE(2,(#23696,#23697,#23698,#23699,#23700,#23701,#23702,#23703,
#23704,#23705,#23706,#23707,#23708,#23709,#23710,#23711,#23712,#23713,#23714,
#23715,#23716),.UNSPECIFIED.,.F.,.F.)
B_SPLINE_CURVE_WITH_KNOTS((3,2,2,2,2,2,2,2,2,2,3),(0.613636363636364,0.618181818181818,
0.622727272727273,0.627272727272727,0.631818181818182,0.636363636363636,
0.640909090909091,0.645454545454546,0.65,0.654545454545455,0.659090909090909),
 .UNSPECIFIED.)
CURVE()
GEOMETRIC_REPRESENTATION_ITEM()
RATIONAL_B_SPLINE_CURVE((1.,0.951056516295154,1.,0.951056516295154,1.,0.951056516295154,
1.,0.951056516295154,1.,0.951056516295154,1.,0.951056516295154,1.,0.951056516295154,
1.,0.951056516295154,1.,0.951056516295154,1.,0.951056516295154,1.))
REPRESENTATION_ITEM('')
);
#485=(
BOUNDED_CURVE()
B_SPLINE_CURVE(2,(#23717,#23718,#23719,#23720,#23721,#23722,#23723,#23724,
#23725,#23726,#23727,#23728,#23729,#23730,#23731,#23732,#23733,#23734,#23735,
#23736,#23737),.UNSPECIFIED.,.F.,.F.)
B_SPLINE_CURVE_WITH_KNOTS((3,2,2,2,2,2,2,2,2,2,3),(0.623455381739298,0.628073569752181,
0.632691757765065,0.637309945777949,0.641928133790832,0.646546321803716,
0.6511645098166,0.655782697829484,0.660400885842367,0.665019073855251,0.669637261868135),
 .UNSPECIFIED.)
CURVE()
GEOMETRIC_REPRESENTATION_ITEM()
RATIONAL_B_SPLINE_CURVE((1.,0.951056516295154,1.,0.951056516295154,1.,0.951056516295154,
1.,0.951056516295154,1.,0.951056516295154,1.,0.951056516295154,1.,0.951056516295154,
1.,0.951056516295154,1.,0.951056516295154,1.,0.951056516295154,1.))
REPRESENTATION_ITEM('')
);
#486=(
BOUNDED_CURVE()
B_SPLINE_CURVE(2,(#23742,#23743,#23744,#23745,#23746,#23747,#23748,#23749,
#23750,#23751,#23752,#23753,#23754,#23755,#23756,#23757,#23758,#23759,#23760,
#23761,#23762),.UNSPECIFIED.,.F.,.F.)
B_SPLINE_CURVE_WITH_KNOTS((3,2,2,2,2,2,2,2,2,2,3),(0.659090909090909,0.663636363636364,
0.668181818181818,0.672727272727273,0.677272727272727,0.681818181818182,
0.686363636363636,0.690909090909091,0.695454545454545,0.7,0.704545454545455),
 .UNSPECIFIED.)
CURVE()
GEOMETRIC_REPRESENTATION_ITEM()
RATIONAL_B_SPLINE_CURVE((1.,0.951056516295154,1.,0.951056516295154,1.,0.951056516295154,
1.,0.951056516295154,1.,0.951056516295154,1.,0.951056516295154,1.,0.951056516295154,
1.,0.951056516295154,1.,0.951056516295154,1.,0.951056516295154,1.))
REPRESENTATION_ITEM('')
);
#487=(
BOUNDED_CURVE()
B_SPLINE_CURVE(2,(#23763,#23764,#23765,#23766,#23767,#23768,#23769,#23770,
#23771,#23772,#23773,#23774,#23775,#23776,#23777,#23778,#23779,#23780,#23781,
#23782,#23783),.UNSPECIFIED.,.F.,.F.)
B_SPLINE_CURVE_WITH_KNOTS((3,2,2,2,2,2,2,2,2,2,3),(0.669637261868135,0.674255449881018,
0.678873637893902,0.683491825906786,0.688110013919669,0.692728201932553,
0.697346389945437,0.70196457795832,0.706582765971204,0.711200953984088,
0.715819141996971),.UNSPECIFIED.)
CURVE()
GEOMETRIC_REPRESENTATION_ITEM()
RATIONAL_B_SPLINE_CURVE((1.,0.951056516295154,1.,0.951056516295154,1.,0.951056516295154,
1.,0.951056516295154,1.,0.951056516295154,1.,0.951056516295154,1.,0.951056516295154,
1.,0.951056516295154,1.,0.951056516295154,1.,0.951056516295154,1.))
REPRESENTATION_ITEM('')
);
#488=(
BOUNDED_CURVE()
B_SPLINE_CURVE(2,(#23788,#23789,#23790,#23791,#23792,#23793,#23794,#23795,
#23796,#23797,#23798,#23799,#23800,#23801,#23802,#23803,#23804,#23805,#23806,
#23807,#23808),.UNSPECIFIED.,.F.,.F.)
B_SPLINE_CURVE_WITH_KNOTS((3,2,2,2,2,2,2,2,2,2,3),(0.704545454545455,0.709090909090909,
0.713636363636364,0.718181818181818,0.722727272727273,0.727272727272727,
0.731818181818182,0.736363636363636,0.740909090909091,0.745454545454545,
0.75),.UNSPECIFIED.)
CURVE()
GEOMETRIC_REPRESENTATION_ITEM()
RATIONAL_B_SPLINE_CURVE((1.,0.951056516295154,1.,0.951056516295154,1.,0.951056516295154,
1.,0.951056516295154,1.,0.951056516295154,1.,0.951056516295154,1.,0.951056516295154,
1.,0.951056516295154,1.,0.951056516295154,1.,0.951056516295154,1.))
REPRESENTATION_ITEM('')
);
#489=(
BOUNDED_CURVE()
B_SPLINE_CURVE(2,(#23809,#23810,#23811,#23812,#23813,#23814,#23815,#23816,
#23817,#23818,#23819,#23820,#23821,#23822,#23823,#23824,#23825,#23826,#23827,
#23828,#23829),.UNSPECIFIED.,.F.,.F.)
B_SPLINE_CURVE_WITH_KNOTS((3,2,2,2,2,2,2,2,2,2,3),(0.715819141996971,0.720437330009855,
0.725055518022739,0.729673706035622,0.734291894048506,0.73891008206139,
0.743528270074274,0.748146458087157,0.752764646100041,0.757382834112925,
0.762001022125808),.UNSPECIFIED.)
CURVE()
GEOMETRIC_REPRESENTATION_ITEM()
RATIONAL_B_SPLINE_CURVE((1.,0.951056516295154,1.,0.951056516295154,1.,0.951056516295154,
1.,0.951056516295154,1.,0.951056516295154,1.,0.951056516295154,1.,0.951056516295154,
1.,0.951056516295154,1.,0.951056516295154,1.,0.951056516295154,1.))
REPRESENTATION_ITEM('')
);
#490=(
BOUNDED_CURVE()
B_SPLINE_CURVE(2,(#23834,#23835,#23836,#23837,#23838,#23839,#23840,#23841,
#23842,#23843,#23844,#23845,#23846,#23847,#23848,#23849,#23850,#23851,#23852,
#23853,#23854),.UNSPECIFIED.,.F.,.F.)
B_SPLINE_CURVE_WITH_KNOTS((3,2,2,2,2,2,2,2,2,2,3),(0.75,0.754545454545455,
0.759090909090909,0.763636363636364,0.768181818181818,0.772727272727273,
0.777272727272727,0.781818181818182,0.786363636363636,0.790909090909091,
0.795454545454545),.UNSPECIFIED.)
CURVE()
GEOMETRIC_REPRESENTATION_ITEM()
RATIONAL_B_SPLINE_CURVE((1.,0.951056516295154,1.,0.951056516295154,1.,0.951056516295154,
1.,0.951056516295154,1.,0.951056516295154,1.,0.951056516295154,1.,0.951056516295154,
1.,0.951056516295154,1.,0.951056516295154,1.,0.951056516295154,1.))
REPRESENTATION_ITEM('')
);
#491=(
BOUNDED_CURVE()
B_SPLINE_CURVE(2,(#23855,#23856,#23857,#23858,#23859,#23860,#23861,#23862,
#23863,#23864,#23865,#23866,#23867,#23868,#23869,#23870,#23871,#23872,#23873,
#23874,#23875),.UNSPECIFIED.,.F.,.F.)
B_SPLINE_CURVE_WITH_KNOTS((3,2,2,2,2,2,2,2,2,2,3),(0.762001022125808,0.766619210138692,
0.771237398151576,0.775855586164459,0.780473774177343,0.785091962190227,
0.78971015020311,0.794328338215994,0.798946526228878,0.803564714241761,
0.808182902254645),.UNSPECIFIED.)
CURVE()
GEOMETRIC_REPRESENTATION_ITEM()
RATIONAL_B_SPLINE_CURVE((1.,0.951056516295154,1.,0.951056516295154,1.,0.951056516295154,
1.,0.951056516295154,1.,0.951056516295154,1.,0.951056516295154,1.,0.951056516295154,
1.,0.951056516295154,1.,0.951056516295154,1.,0.951056516295154,1.))
REPRESENTATION_ITEM('')
);
#492=(
BOUNDED_CURVE()
B_SPLINE_CURVE(2,(#23880,#23881,#23882,#23883,#23884,#23885,#23886,#23887,
#23888,#23889,#23890,#23891,#23892,#23893,#23894,#23895,#23896,#23897,#23898,
#23899,#23900),.UNSPECIFIED.,.F.,.F.)
B_SPLINE_CURVE_WITH_KNOTS((3,2,2,2,2,2,2,2,2,2,3),(0.795454545454545,0.8,
0.804545454545455,0.809090909090909,0.813636363636364,0.818181818181818,
0.822727272727273,0.827272727272727,0.831818181818182,0.836363636363636,
0.840909090909091),.UNSPECIFIED.)
CURVE()
GEOMETRIC_REPRESENTATION_ITEM()
RATIONAL_B_SPLINE_CURVE((1.,0.951056516295154,1.,0.951056516295154,1.,0.951056516295154,
1.,0.951056516295154,1.,0.951056516295154,1.,0.951056516295154,1.,0.951056516295154,
1.,0.951056516295154,1.,0.951056516295154,1.,0.951056516295154,1.))
REPRESENTATION_ITEM('')
);
#493=(
BOUNDED_CURVE()
B_SPLINE_CURVE(2,(#23901,#23902,#23903,#23904,#23905,#23906,#23907,#23908,
#23909,#23910,#23911,#23912,#23913,#23914,#23915,#23916,#23917,#23918,#23919,
#23920,#23921),.UNSPECIFIED.,.F.,.F.)
B_SPLINE_CURVE_WITH_KNOTS((3,2,2,2,2,2,2,2,2,2,3),(0.808182902254645,0.812801090267529,
0.817419278280413,0.822037466293296,0.82665565430618,0.831273842319064,
0.835892030331947,0.840510218344831,0.845128406357715,0.849746594370598,
0.854364782383482),.UNSPECIFIED.)
CURVE()
GEOMETRIC_REPRESENTATION_ITEM()
RATIONAL_B_SPLINE_CURVE((1.,0.951056516295154,1.,0.951056516295154,1.,0.951056516295154,
1.,0.951056516295154,1.,0.951056516295154,1.,0.951056516295154,1.,0.951056516295154,
1.,0.951056516295154,1.,0.951056516295154,1.,0.951056516295154,1.))
REPRESENTATION_ITEM('')
);
#494=(
BOUNDED_CURVE()
B_SPLINE_CURVE(2,(#23926,#23927,#23928,#23929,#23930,#23931,#23932,#23933,
#23934,#23935,#23936,#23937,#23938,#23939,#23940,#23941,#23942,#23943,#23944,
#23945,#23946),.UNSPECIFIED.,.F.,.F.)
B_SPLINE_CURVE_WITH_KNOTS((3,2,2,2,2,2,2,2,2,2,3),(0.840909090909091,0.845454545454545,
0.85,0.854545454545454,0.859090909090909,0.863636363636364,0.868181818181818,
0.872727272727273,0.877272727272727,0.881818181818182,0.886363636363636),
 .UNSPECIFIED.)
CURVE()
GEOMETRIC_REPRESENTATION_ITEM()
RATIONAL_B_SPLINE_CURVE((1.,0.951056516295154,1.,0.951056516295154,1.,0.951056516295154,
1.,0.951056516295154,1.,0.951056516295154,1.,0.951056516295154,1.,0.951056516295154,
1.,0.951056516295154,1.,0.951056516295154,1.,0.951056516295154,1.))
REPRESENTATION_ITEM('')
);
#495=(
BOUNDED_CURVE()
B_SPLINE_CURVE(2,(#23947,#23948,#23949,#23950,#23951,#23952,#23953,#23954,
#23955,#23956,#23957,#23958,#23959,#23960,#23961,#23962,#23963,#23964,#23965,
#23966,#23967),.UNSPECIFIED.,.F.,.F.)
B_SPLINE_CURVE_WITH_KNOTS((3,2,2,2,2,2,2,2,2,2,3),(0.854364782383482,0.858982970396366,
0.863601158409249,0.868219346422133,0.872837534435017,0.877455722447901,
0.882073910460784,0.886692098473668,0.891310286486552,0.895928474499435,
0.900546662512319),.UNSPECIFIED.)
CURVE()
GEOMETRIC_REPRESENTATION_ITEM()
RATIONAL_B_SPLINE_CURVE((1.,0.951056516295154,1.,0.951056516295154,1.,0.951056516295154,
1.,0.951056516295154,1.,0.951056516295154,1.,0.951056516295154,1.,0.951056516295154,
1.,0.951056516295154,1.,0.951056516295154,1.,0.951056516295154,1.))
REPRESENTATION_ITEM('')
);
#496=(
BOUNDED_CURVE()
B_SPLINE_CURVE(2,(#23972,#23973,#23974,#23975,#23976,#23977,#23978,#23979,
#23980,#23981,#23982,#23983,#23984,#23985,#23986,#23987,#23988,#23989,#23990,
#23991,#23992),.UNSPECIFIED.,.F.,.F.)
B_SPLINE_CURVE_WITH_KNOTS((3,2,2,2,2,2,2,2,2,2,3),(0.886363636363636,0.890909090909091,
0.895454545454546,0.9,0.904545454545455,0.909090909090909,0.913636363636364,
0.918181818181818,0.922727272727273,0.927272727272727,0.931818181818182),
 .UNSPECIFIED.)
CURVE()
GEOMETRIC_REPRESENTATION_ITEM()
RATIONAL_B_SPLINE_CURVE((1.,0.951056516295154,1.,0.951056516295154,1.,0.951056516295154,
1.,0.951056516295154,1.,0.951056516295154,1.,0.951056516295154,1.,0.951056516295154,
1.,0.951056516295154,1.,0.951056516295154,1.,0.951056516295154,1.))
REPRESENTATION_ITEM('')
);
#497=(
BOUNDED_CURVE()
B_SPLINE_CURVE(2,(#23993,#23994,#23995,#23996,#23997,#23998,#23999,#24000,
#24001,#24002,#24003,#24004,#24005,#24006,#24007,#24008,#24009,#24010,#24011,
#24012,#24013),.UNSPECIFIED.,.F.,.F.)
B_SPLINE_CURVE_WITH_KNOTS((3,2,2,2,2,2,2,2,2,2,3),(0.900546662512319,0.905164850525203,
0.909783038538087,0.91440122655097,0.919019414563854,0.923637602576737,
0.928255790589621,0.932873978602505,0.937492166615388,0.942110354628272,
0.946728542641156),.UNSPECIFIED.)
CURVE()
GEOMETRIC_REPRESENTATION_ITEM()
RATIONAL_B_SPLINE_CURVE((1.,0.951056516295154,1.,0.951056516295154,1.,0.951056516295154,
1.,0.951056516295154,1.,0.951056516295154,1.,0.951056516295154,1.,0.951056516295154,
1.,0.951056516295154,1.,0.951056516295154,1.,0.951056516295154,1.))
REPRESENTATION_ITEM('')
);
#498=(
BOUNDED_CURVE()
B_SPLINE_CURVE(2,(#24018,#24019,#24020,#24021,#24022,#24023,#24024,#24025,
#24026,#24027,#24028,#24029,#24030,#24031,#24032,#24033,#24034,#24035,#24036,
#24037,#24038),.UNSPECIFIED.,.F.,.F.)
B_SPLINE_CURVE_WITH_KNOTS((3,2,2,2,2,2,2,2,2,2,3),(0.931818181818182,0.936363636363636,
0.940909090909091,0.945454545454545,0.95,0.954545454545455,0.959090909090909,
0.963636363636364,0.968181818181818,0.972727272727273,0.977272727272727),
 .UNSPECIFIED.)
CURVE()
GEOMETRIC_REPRESENTATION_ITEM()
RATIONAL_B_SPLINE_CURVE((1.,0.951056516295154,1.,0.951056516295154,1.,0.951056516295154,
1.,0.951056516295154,1.,0.951056516295154,1.,0.951056516295154,1.,0.951056516295154,
1.,0.951056516295154,1.,0.951056516295154,1.,0.951056516295154,1.))
REPRESENTATION_ITEM('')
);
#499=(
BOUNDED_CURVE()
B_SPLINE_CURVE(2,(#24039,#24040,#24041,#24042,#24043,#24044,#24045,#24046,
#24047,#24048,#24049,#24050,#24051,#24052,#24053,#24054,#24055,#24056,#24057,
#24058,#24059),.UNSPECIFIED.,.F.,.F.)
B_SPLINE_CURVE_WITH_KNOTS((3,2,2,2,2,2,2,2,2,2,3),(0.946728542641156,0.95134673065404,
0.955964918666923,0.960583106679807,0.965201294692691,0.969819482705574,
0.974437670718458,0.979055858731342,0.983674046744225,0.988292234757109,
0.992910422769993),.UNSPECIFIED.)
CURVE()
GEOMETRIC_REPRESENTATION_ITEM()
RATIONAL_B_SPLINE_CURVE((1.,0.951056516295154,1.,0.951056516295154,1.,0.951056516295154,
1.,0.951056516295154,1.,0.951056516295154,1.,0.951056516295154,1.,0.951056516295154,
1.,0.951056516295154,1.,0.951056516295154,1.,0.951056516295154,1.))
REPRESENTATION_ITEM('')
);
#500=(
BOUNDED_CURVE()
B_SPLINE_CURVE(2,(#27442,#27443,#27444,#27445,#27446),.UNSPECIFIED.,.F.,
 .F.)
B_SPLINE_CURVE_WITH_KNOTS((3,2,3),(0.992910422769993,0.997528610782876,
0.999999992267812),.UNSPECIFIED.)
CURVE()
GEOMETRIC_REPRESENTATION_ITEM()
RATIONAL_B_SPLINE_CURVE((1.,0.951056516295154,1.,0.973808338010719,0.975649137376158))
REPRESENTATION_ITEM('')
);
#501=(
BOUNDED_CURVE()
B_SPLINE_CURVE(2,(#27448,#27449,#27450,#27451,#27452),.UNSPECIFIED.,.F.,
 .F.)
B_SPLINE_CURVE_WITH_KNOTS((3,2,3),(0.977272727272727,0.981818181818182,
0.984250640944397),.UNSPECIFIED.)
CURVE()
GEOMETRIC_REPRESENTATION_ITEM()
RATIONAL_B_SPLINE_CURVE((1.,0.951056516295154,1.,0.973808334806544,0.975649137826549))
REPRESENTATION_ITEM('')
);
#602=CONICAL_SURFACE('',#16434,4.93749999999999,0.785398163397446);
#641=TOROIDAL_SURFACE('',#16420,15.,3.);
#642=TOROIDAL_SURFACE('',#16425,15.,3.);
#679=SHAPE_REPRESENTATION_RELATIONSHIP('SRR','None',#33021,#693);
#693=ADVANCED_BREP_SHAPE_REPRESENTATION('',(#1411),#32896);
#919=CIRCLE('',#16376,6.56268467749802);
#920=CIRCLE('',#16419,7.9375);
#921=CIRCLE('',#16421,18.);
#922=CIRCLE('',#16422,3.);
#923=CIRCLE('',#16423,15.);
#924=CIRCLE('',#16424,3.);
#925=CIRCLE('',#16426,15.);
#926=CIRCLE('',#16427,3.);
#927=CIRCLE('',#16428,18.);
#928=CIRCLE('',#16429,3.);
#929=CIRCLE('',#16431,9.);
#930=CIRCLE('',#16432,9.);
#931=CIRCLE('',#16435,7.9375);
#932=CIRCLE('',#16436,4.93749999999999);
#933=CIRCLE('',#16443,1.5);
#934=CIRCLE('',#16444,1.5);
#935=CIRCLE('',#16445,1.5);
#936=CIRCLE('',#16446,1.5);
#937=CIRCLE('',#16447,3.);
#938=CIRCLE('',#16448,3.);
#939=CIRCLE('',#16449,3.);
#940=CIRCLE('',#16450,3.);
#1186=CYLINDRICAL_SURFACE('',#16375,6.56268467496113);
#1187=CYLINDRICAL_SURFACE('',#16377,6.56268467496113);
#1188=CYLINDRICAL_SURFACE('',#16378,6.56268467496113);
#1189=CYLINDRICAL_SURFACE('',#16379,6.56268467496113);
#1190=CYLINDRICAL_SURFACE('',#16380,6.56268467496113);
#1191=CYLINDRICAL_SURFACE('',#16381,6.56268467496113);
#1192=CYLINDRICAL_SURFACE('',#16382,6.56268467496113);
#1193=CYLINDRICAL_SURFACE('',#16383,6.56268467496113);
#1194=CYLINDRICAL_SURFACE('',#16384,6.56268467496113);
#1195=CYLINDRICAL_SURFACE('',#16385,6.56268467496113);
#1196=CYLINDRICAL_SURFACE('',#16386,6.56268467496113);
#1197=CYLINDRICAL_SURFACE('',#16387,6.56268467496113);
#1198=CYLINDRICAL_SURFACE('',#16388,6.56268467496113);
#1199=CYLINDRICAL_SURFACE('',#16389,6.56268467496113);
#1200=CYLINDRICAL_SURFACE('',#16390,6.56268467496113);
#1201=CYLINDRICAL_SURFACE('',#16391,6.56268467496113);
#1202=CYLINDRICAL_SURFACE('',#16392,6.56268467496113);
#1203=CYLINDRICAL_SURFACE('',#16393,6.56268467496113);
#1204=CYLINDRICAL_SURFACE('',#16394,6.56268467496113);
#1205=CYLINDRICAL_SURFACE('',#16395,6.56268467496113);
#1206=CYLINDRICAL_SURFACE('',#16396,6.56268467496113);
#1207=CYLINDRICAL_SURFACE('',#16397,6.56268467496113);
#1208=CYLINDRICAL_SURFACE('',#16398,7.9375);
#1209=CYLINDRICAL_SURFACE('',#16399,7.9375);
#1210=CYLINDRICAL_SURFACE('',#16400,7.9375);
#1211=CYLINDRICAL_SURFACE('',#16401,7.9375);
#1212=CYLINDRICAL_SURFACE('',#16402,7.9375);
#1213=CYLINDRICAL_SURFACE('',#16403,7.9375);
#1214=CYLINDRICAL_SURFACE('',#16404,7.9375);
#1215=CYLINDRICAL_SURFACE('',#16405,7.9375);
#1216=CYLINDRICAL_SURFACE('',#16406,7.9375);
#1217=CYLINDRICAL_SURFACE('',#16407,7.9375);
#1218=CYLINDRICAL_SURFACE('',#16408,7.9375);
#1219=CYLINDRICAL_SURFACE('',#16409,7.9375);
#1220=CYLINDRICAL_SURFACE('',#16410,7.9375);
#1221=CYLINDRICAL_SURFACE('',#16411,7.9375);
#1222=CYLINDRICAL_SURFACE('',#16412,7.9375);
#1223=CYLINDRICAL_SURFACE('',#16413,7.9375);
#1224=CYLINDRICAL_SURFACE('',#16414,7.9375);
#1225=CYLINDRICAL_SURFACE('',#16415,7.9375);
#1226=CYLINDRICAL_SURFACE('',#16416,7.9375);
#1227=CYLINDRICAL_SURFACE('',#16417,7.9375);
#1228=CYLINDRICAL_SURFACE('',#16418,7.9375);
#1229=CYLINDRICAL_SURFACE('',#16430,9.);
#1230=CYLINDRICAL_SURFACE('',#16433,18.);
#1231=CYLINDRICAL_SURFACE('',#16437,7.9375);
#1232=CYLINDRICAL_SURFACE('',#16442,6.56268467496113);
#1322=STYLED_ITEM('',(#33098),#1411);
#1411=MANIFOLD_SOLID_BREP('Body1',#15570);
#1599=FACE_BOUND('',#3090,.T.);
#1600=FACE_BOUND('',#3092,.T.);
#2015=FACE_OUTER_BOUND('',#3040,.T.);
#2016=FACE_OUTER_BOUND('',#3041,.T.);
#2017=FACE_OUTER_BOUND('',#3042,.T.);
#2018=FACE_OUTER_BOUND('',#3043,.T.);
#2019=FACE_OUTER_BOUND('',#3044,.T.);
#2020=FACE_OUTER_BOUND('',#3045,.T.);
#2021=FACE_OUTER_BOUND('',#3046,.T.);
#2022=FACE_OUTER_BOUND('',#3047,.T.);
#2023=FACE_OUTER_BOUND('',#3048,.T.);
#2024=FACE_OUTER_BOUND('',#3049,.T.);
#2025=FACE_OUTER_BOUND('',#3050,.T.);
#2026=FACE_OUTER_BOUND('',#3051,.T.);
#2027=FACE_OUTER_BOUND('',#3052,.T.);
#2028=FACE_OUTER_BOUND('',#3053,.T.);
#2029=FACE_OUTER_BOUND('',#3054,.T.);
#2030=FACE_OUTER_BOUND('',#3055,.T.);
#2031=FACE_OUTER_BOUND('',#3056,.T.);
#2032=FACE_OUTER_BOUND('',#3057,.T.);
#2033=FACE_OUTER_BOUND('',#3058,.T.);
#2034=FACE_OUTER_BOUND('',#3059,.T.);
#2035=FACE_OUTER_BOUND('',#3060,.T.);
#2036=FACE_OUTER_BOUND('',#3061,.T.);
#2037=FACE_OUTER_BOUND('',#3062,.T.);
#2038=FACE_OUTER_BOUND('',#3063,.T.);
#2039=FACE_OUTER_BOUND('',#3064,.T.);
#2040=FACE_OUTER_BOUND('',#3065,.T.);
#2041=FACE_OUTER_BOUND('',#3066,.T.);
#2042=FACE_OUTER_BOUND('',#3067,.T.);
#2043=FACE_OUTER_BOUND('',#3068,.T.);
#2044=FACE_OUTER_BOUND('',#3069,.T.);
#2045=FACE_OUTER_BOUND('',#3070,.T.);
#2046=FACE_OUTER_BOUND('',#3071,.T.);
#2047=FACE_OUTER_BOUND('',#3072,.T.);
#2048=FACE_OUTER_BOUND('',#3073,.T.);
#2049=FACE_OUTER_BOUND('',#3074,.T.);
#2050=FACE_OUTER_BOUND('',#3075,.T.);
#2051=FACE_OUTER_BOUND('',#3076,.T.);
#2052=FACE_OUTER_BOUND('',#3077,.T.);
#2053=FACE_OUTER_BOUND('',#3078,.T.);
#2054=FACE_OUTER_BOUND('',#3079,.T.);
#2055=FACE_OUTER_BOUND('',#3080,.T.);
#2056=FACE_OUTER_BOUND('',#3081,.T.);
#2057=FACE_OUTER_BOUND('',#3082,.T.);
#2058=FACE_OUTER_BOUND('',#3083,.T.);
#2059=FACE_OUTER_BOUND('',#3084,.T.);
#2060=FACE_OUTER_BOUND('',#3085,.T.);
#2061=FACE_OUTER_BOUND('',#3086,.T.);
#2062=FACE_OUTER_BOUND('',#3087,.T.);
#2063=FACE_OUTER_BOUND('',#3088,.T.);
#2064=FACE_OUTER_BOUND('',#3089,.T.);
#2065=FACE_OUTER_BOUND('',#3091,.T.);
#2066=FACE_OUTER_BOUND('',#3093,.T.);
#2067=FACE_OUTER_BOUND('',#3094,.T.);
#2068=FACE_OUTER_BOUND('',#3095,.T.);
#2069=FACE_OUTER_BOUND('',#3096,.T.);
#2070=FACE_OUTER_BOUND('',#3097,.T.);
#2071=FACE_OUTER_BOUND('',#3098,.T.);
#2072=FACE_OUTER_BOUND('',#3099,.T.);
#2073=FACE_OUTER_BOUND('',#3100,.T.);
#2074=FACE_OUTER_BOUND('',#3101,.T.);
#2075=FACE_OUTER_BOUND('',#3102,.T.);
#2076=FACE_OUTER_BOUND('',#3103,.T.);
#2077=FACE_OUTER_BOUND('',#3104,.T.);
#2078=FACE_OUTER_BOUND('',#3105,.T.);
#2079=FACE_OUTER_BOUND('',#3106,.T.);
#2080=FACE_OUTER_BOUND('',#3107,.T.);
#2081=FACE_OUTER_BOUND('',#3108,.T.);
#2082=FACE_OUTER_BOUND('',#3109,.T.);
#2083=FACE_OUTER_BOUND('',#3110,.T.);
#2084=FACE_OUTER_BOUND('',#3111,.T.);
#3040=EDGE_LOOP('',(#11499,#11500,#11501,#11502));
#3041=EDGE_LOOP('',(#11503,#11504,#11505,#11506));
#3042=EDGE_LOOP('',(#11507,#11508,#11509,#11510));
#3043=EDGE_LOOP('',(#11511,#11512,#11513,#11514));
#3044=EDGE_LOOP('',(#11515,#11516,#11517,#11518));
#3045=EDGE_LOOP('',(#11519,#11520,#11521,#11522));
#3046=EDGE_LOOP('',(#11523,#11524,#11525,#11526));
#3047=EDGE_LOOP('',(#11527,#11528,#11529,#11530));
#3048=EDGE_LOOP('',(#11531,#11532,#11533,#11534));
#3049=EDGE_LOOP('',(#11535,#11536,#11537,#11538));
#3050=EDGE_LOOP('',(#11539,#11540,#11541,#11542));
#3051=EDGE_LOOP('',(#11543,#11544,#11545,#11546));
#3052=EDGE_LOOP('',(#11547,#11548,#11549,#11550));
#3053=EDGE_LOOP('',(#11551,#11552,#11553,#11554));
#3054=EDGE_LOOP('',(#11555,#11556,#11557,#11558));
#3055=EDGE_LOOP('',(#11559,#11560,#11561,#11562));
#3056=EDGE_LOOP('',(#11563,#11564,#11565,#11566));
#3057=EDGE_LOOP('',(#11567,#11568,#11569,#11570));
#3058=EDGE_LOOP('',(#11571,#11572,#11573,#11574));
#3059=EDGE_LOOP('',(#11575,#11576,#11577,#11578));
#3060=EDGE_LOOP('',(#11579,#11580,#11581,#11582));
#3061=EDGE_LOOP('',(#11583,#11584,#11585,#11586));
#3062=EDGE_LOOP('',(#11587,#11588,#11589,#11590,#11591,#11592,#11593,#11594,
#11595,#11596,#11597,#11598,#11599));
#3063=EDGE_LOOP('',(#11600,#11601,#11602,#11603));
#3064=EDGE_LOOP('',(#11604,#11605,#11606,#11607));
#3065=EDGE_LOOP('',(#11608,#11609,#11610,#11611));
#3066=EDGE_LOOP('',(#11612,#11613,#11614,#11615));
#3067=EDGE_LOOP('',(#11616,#11617,#11618,#11619));
#3068=EDGE_LOOP('',(#11620,#11621,#11622,#11623));
#3069=EDGE_LOOP('',(#11624,#11625,#11626,#11627));
#3070=EDGE_LOOP('',(#11628,#11629,#11630,#11631));
#3071=EDGE_LOOP('',(#11632,#11633,#11634,#11635));
#3072=EDGE_LOOP('',(#11636,#11637,#11638,#11639));
#3073=EDGE_LOOP('',(#11640,#11641,#11642,#11643));
#3074=EDGE_LOOP('',(#11644,#11645,#11646,#11647));
#3075=EDGE_LOOP('',(#11648,#11649,#11650,#11651));
#3076=EDGE_LOOP('',(#11652,#11653,#11654,#11655));
#3077=EDGE_LOOP('',(#11656,#11657,#11658,#11659));
#3078=EDGE_LOOP('',(#11660,#11661,#11662,#11663));
#3079=EDGE_LOOP('',(#11664,#11665,#11666,#11667));
#3080=EDGE_LOOP('',(#11668,#11669,#11670,#11671));
#3081=EDGE_LOOP('',(#11672,#11673,#11674,#11675));
#3082=EDGE_LOOP('',(#11676,#11677,#11678,#11679,#11680));
#3083=EDGE_LOOP('',(#11681,#11682,#11683,#11684));
#3084=EDGE_LOOP('',(#11685,#11686,#11687,#11688));
#3085=EDGE_LOOP('',(#11689,#11690,#11691,#11692));
#3086=EDGE_LOOP('',(#11693,#11694,#11695,#11696));
#3087=EDGE_LOOP('',(#11697,#11698,#11699,#11700,#11701,#11702,#11703,#11704,
#11705));
#3088=EDGE_LOOP('',(#11706,#11707,#11708));
#3089=EDGE_LOOP('',(#11709,#11710,#11711,#11712,#11713));
#3090=EDGE_LOOP('',(#11714));
#3091=EDGE_LOOP('',(#11715,#11716,#11717,#11718,#11719));
#3092=EDGE_LOOP('',(#11720));
#3093=EDGE_LOOP('',(#11721));
#3094=EDGE_LOOP('',(#11722,#11723,#11724,#11725));
#3095=EDGE_LOOP('',(#11726,#11727,#11728,#11729,#11730,#11731,#11732,#11733,
#11734,#11735,#11736,#11737,#11738,#11739,#11740,#11741,#11742,#11743,#11744,
#11745,#11746,#11747,#11748,#11749,#11750,#11751,#11752,#11753,#11754,#11755,
#11756,#11757,#11758,#11759,#11760,#11761,#11762,#11763,#11764,#11765,#11766,
#11767,#11768,#11769,#11770,#11771,#11772,#11773));
#3096=EDGE_LOOP('',(#11774,#11775,#11776,#11777));
#3097=EDGE_LOOP('',(#11778,#11779,#11780,#11781,#11782,#11783,#11784,#11785,
#11786,#11787,#11788,#11789,#11790,#11791,#11792,#11793,#11794,#11795,#11796,
#11797,#11798,#11799,#11800,#11801,#11802,#11803,#11804,#11805,#11806,#11807,
#11808,#11809,#11810,#11811,#11812,#11813,#11814,#11815,#11816,#11817,#11818,
#11819,#11820,#11821,#11822,#11823,#11824));
#3098=EDGE_LOOP('',(#11825,#11826,#11827));
#3099=EDGE_LOOP('',(#11828,#11829,#11830,#11831,#11832,#11833));
#3100=EDGE_LOOP('',(#11834,#11835,#11836));
#3101=EDGE_LOOP('',(#11837,#11838,#11839));
#3102=EDGE_LOOP('',(#11840,#11841,#11842,#11843,#11844,#11845));
#3103=EDGE_LOOP('',(#11846,#11847,#11848));
#3104=EDGE_LOOP('',(#11849,#11850,#11851));
#3105=EDGE_LOOP('',(#11852,#11853,#11854,#11855));
#3106=EDGE_LOOP('',(#11856,#11857,#11858,#11859));
#3107=EDGE_LOOP('',(#11860,#11861,#11862));
#3108=EDGE_LOOP('',(#11863,#11864,#11865));
#3109=EDGE_LOOP('',(#11866,#11867,#11868,#11869));
#3110=EDGE_LOOP('',(#11870,#11871,#11872,#11873));
#3111=EDGE_LOOP('',(#11874,#11875,#11876));
#4178=LINE('',#23074,#5582);
#4179=LINE('',#23097,#5583);
#4180=LINE('',#23143,#5584);
#4181=LINE('',#23189,#5585);
#4182=LINE('',#23235,#5586);
#4183=LINE('',#23281,#5587);
#4184=LINE('',#23327,#5588);
#4185=LINE('',#23373,#5589);
#4186=LINE('',#23419,#5590);
#4187=LINE('',#23465,#5591);
#4188=LINE('',#23511,#5592);
#4189=LINE('',#23557,#5593);
#4190=LINE('',#23603,#5594);
#4191=LINE('',#23649,#5595);
#4192=LINE('',#23695,#5596);
#4193=LINE('',#23741,#5597);
#4194=LINE('',#23787,#5598);
#4195=LINE('',#23833,#5599);
#4196=LINE('',#23879,#5600);
#4197=LINE('',#23925,#5601);
#4198=LINE('',#23971,#5602);
#4199=LINE('',#24017,#5603);
#4200=LINE('',#24063,#5604);
#4201=LINE('',#24102,#5605);
#4202=LINE('',#24554,#5606);
#4203=LINE('',#24586,#5607);
#4204=LINE('',#24662,#5608);
#4205=LINE('',#24738,#5609);
#4206=LINE('',#24814,#5610);
#4207=LINE('',#24890,#5611);
#4208=LINE('',#24966,#5612);
#4209=LINE('',#25044,#5613);
#4210=LINE('',#25120,#5614);
#4211=LINE('',#25196,#5615);
#4212=LINE('',#25274,#5616);
#4213=LINE('',#25350,#5617);
#4214=LINE('',#25426,#5618);
#4215=LINE('',#25502,#5619);
#4216=LINE('',#25578,#5620);
#4217=LINE('',#25654,#5621);
#4218=LINE('',#25732,#5622);
#4219=LINE('',#25808,#5623);
#4220=LINE('',#25886,#5624);
#4221=LINE('',#25962,#5625);
#4222=LINE('',#26038,#5626);
#4223=LINE('',#26133,#5627);
#4224=LINE('',#26307,#5628);
#4225=LINE('',#26564,#5629);
#4226=LINE('',#26566,#5630);
#4227=LINE('',#26567,#5631);
#5582=VECTOR('',#18848,6.56268467496113);
#5583=VECTOR('',#18853,6.56268467496113);
#5584=VECTOR('',#18856,6.56268467496113);
#5585=VECTOR('',#18859,6.56268467496113);
#5586=VECTOR('',#18862,6.56268467496113);
#5587=VECTOR('',#18865,6.56268467496113);
#5588=VECTOR('',#18868,6.56268467496113);
#5589=VECTOR('',#18871,6.56268467496113);
#5590=VECTOR('',#18874,6.56268467496113);
#5591=VECTOR('',#18877,6.56268467496113);
#5592=VECTOR('',#18880,6.56268467496113);
#5593=VECTOR('',#18883,6.56268467496113);
#5594=VECTOR('',#18886,6.56268467496113);
#5595=VECTOR('',#18889,6.56268467496113);
#5596=VECTOR('',#18892,6.56268467496113);
#5597=VECTOR('',#18895,6.56268467496113);
#5598=VECTOR('',#18898,6.56268467496113);
#5599=VECTOR('',#18901,6.56268467496113);
#5600=VECTOR('',#18904,6.56268467496113);
#5601=VECTOR('',#18907,6.56268467496113);
#5602=VECTOR('',#18910,6.56268467496113);
#5603=VECTOR('',#18913,6.56268467496113);
#5604=VECTOR('',#18916,7.9375);
#5605=VECTOR('',#18917,7.9375);
#5606=VECTOR('',#18918,1000.);
#5607=VECTOR('',#18921,7.9375);
#5608=VECTOR('',#18924,7.9375);
#5609=VECTOR('',#18927,7.9375);
#5610=VECTOR('',#18930,7.9375);
#5611=VECTOR('',#18933,7.9375);
#5612=VECTOR('',#18936,7.9375);
#5613=VECTOR('',#18939,7.9375);
#5614=VECTOR('',#18942,7.9375);
#5615=VECTOR('',#18945,7.9375);
#5616=VECTOR('',#18948,7.9375);
#5617=VECTOR('',#18951,7.9375);
#5618=VECTOR('',#18954,7.9375);
#5619=VECTOR('',#18957,7.9375);
#5620=VECTOR('',#18960,7.9375);
#5621=VECTOR('',#18963,7.9375);
#5622=VECTOR('',#18966,7.9375);
#5623=VECTOR('',#18969,7.9375);
#5624=VECTOR('',#18972,7.9375);
#5625=VECTOR('',#18975,7.9375);
#5626=VECTOR('',#18978,7.9375);
#5627=VECTOR('',#19005,9.);
#5628=VECTOR('',#19014,4.93749999999999);
#5629=VECTOR('',#19027,10.);
#5630=VECTOR('',#19028,10.);
#5631=VECTOR('',#19029,10.);
#7002=VERTEX_POINT('',#23072);
#7003=VERTEX_POINT('',#23073);
#7004=VERTEX_POINT('',#23075);
#7005=VERTEX_POINT('',#23087);
#7006=VERTEX_POINT('',#23095);
#7007=VERTEX_POINT('',#23096);
#7008=VERTEX_POINT('',#23141);
#7009=VERTEX_POINT('',#23142);
#7010=VERTEX_POINT('',#23187);
#7011=VERTEX_POINT('',#23188);
#7012=VERTEX_POINT('',#23233);
#7013=VERTEX_POINT('',#23234);
#7014=VERTEX_POINT('',#23279);
#7015=VERTEX_POINT('',#23280);
#7016=VERTEX_POINT('',#23325);
#7017=VERTEX_POINT('',#23326);
#7018=VERTEX_POINT('',#23371);
#7019=VERTEX_POINT('',#23372);
#7020=VERTEX_POINT('',#23417);
#7021=VERTEX_POINT('',#23418);
#7022=VERTEX_POINT('',#23463);
#7023=VERTEX_POINT('',#23464);
#7024=VERTEX_POINT('',#23509);
#7025=VERTEX_POINT('',#23510);
#7026=VERTEX_POINT('',#23555);
#7027=VERTEX_POINT('',#23556);
#7028=VERTEX_POINT('',#23601);
#7029=VERTEX_POINT('',#23602);
#7030=VERTEX_POINT('',#23647);
#7031=VERTEX_POINT('',#23648);
#7032=VERTEX_POINT('',#23693);
#7033=VERTEX_POINT('',#23694);
#7034=VERTEX_POINT('',#23739);
#7035=VERTEX_POINT('',#23740);
#7036=VERTEX_POINT('',#23785);
#7037=VERTEX_POINT('',#23786);
#7038=VERTEX_POINT('',#23831);
#7039=VERTEX_POINT('',#23832);
#7040=VERTEX_POINT('',#23877);
#7041=VERTEX_POINT('',#23878);
#7042=VERTEX_POINT('',#23923);
#7043=VERTEX_POINT('',#23924);
#7044=VERTEX_POINT('',#23969);
#7045=VERTEX_POINT('',#23970);
#7046=VERTEX_POINT('',#24015);
#7047=VERTEX_POINT('',#24016);
#7048=VERTEX_POINT('',#24061);
#7049=VERTEX_POINT('',#24062);
#7050=VERTEX_POINT('',#24064);
#7051=VERTEX_POINT('',#24101);
#7052=VERTEX_POINT('',#24103);
#7053=VERTEX_POINT('',#24150);
#7054=VERTEX_POINT('',#24266);
#7055=VERTEX_POINT('',#24319);
#7056=VERTEX_POINT('',#24366);
#7057=VERTEX_POINT('',#24534);
#7058=VERTEX_POINT('',#24553);
#7059=VERTEX_POINT('',#24584);
#7060=VERTEX_POINT('',#24585);
#7061=VERTEX_POINT('',#24660);
#7062=VERTEX_POINT('',#24661);
#7063=VERTEX_POINT('',#24736);
#7064=VERTEX_POINT('',#24737);
#7065=VERTEX_POINT('',#24812);
#7066=VERTEX_POINT('',#24813);
#7067=VERTEX_POINT('',#24888);
#7068=VERTEX_POINT('',#24889);
#7069=VERTEX_POINT('',#24964);
#7070=VERTEX_POINT('',#24965);
#7071=VERTEX_POINT('',#25042);
#7072=VERTEX_POINT('',#25043);
#7073=VERTEX_POINT('',#25118);
#7074=VERTEX_POINT('',#25119);
#7075=VERTEX_POINT('',#25194);
#7076=VERTEX_POINT('',#25195);
#7077=VERTEX_POINT('',#25272);
#7078=VERTEX_POINT('',#25273);
#7079=VERTEX_POINT('',#25348);
#7080=VERTEX_POINT('',#25349);
#7081=VERTEX_POINT('',#25424);
#7082=VERTEX_POINT('',#25425);
#7083=VERTEX_POINT('',#25500);
#7084=VERTEX_POINT('',#25501);
#7085=VERTEX_POINT('',#25576);
#7086=VERTEX_POINT('',#25577);
#7087=VERTEX_POINT('',#25652);
#7088=VERTEX_POINT('',#25653);
#7089=VERTEX_POINT('',#25730);
#7090=VERTEX_POINT('',#25731);
#7091=VERTEX_POINT('',#25806);
#7092=VERTEX_POINT('',#25807);
#7093=VERTEX_POINT('',#25884);
#7094=VERTEX_POINT('',#25885);
#7095=VERTEX_POINT('',#25960);
#7096=VERTEX_POINT('',#25961);
#7097=VERTEX_POINT('',#26036);
#7098=VERTEX_POINT('',#26037);
#7099=VERTEX_POINT('',#26039);
#7100=VERTEX_POINT('',#26112);
#7101=VERTEX_POINT('',#26113);
#7102=VERTEX_POINT('',#26115);
#7103=VERTEX_POINT('',#26117);
#7104=VERTEX_POINT('',#26121);
#7105=VERTEX_POINT('',#26122);
#7106=VERTEX_POINT('',#26124);
#7107=VERTEX_POINT('',#26126);
#7108=VERTEX_POINT('',#26130);
#7109=VERTEX_POINT('',#26132);
#7110=VERTEX_POINT('',#26285);
#7111=VERTEX_POINT('',#26287);
#7112=VERTEX_POINT('',#26306);
#7113=VERTEX_POINT('',#26335);
#7114=VERTEX_POINT('',#26392);
#7115=VERTEX_POINT('',#26450);
#7116=VERTEX_POINT('',#26504);
#7117=VERTEX_POINT('',#26563);
#7118=VERTEX_POINT('',#26565);
#7119=VERTEX_POINT('',#28353);
#7120=VERTEX_POINT('',#28504);
#7121=VERTEX_POINT('',#28621);
#7122=VERTEX_POINT('',#28772);
#8633=EDGE_CURVE('',#7002,#7003,#4178,.T.);
#8634=EDGE_CURVE('',#7004,#7002,#456,.T.);
#8635=EDGE_CURVE('',#7005,#7004,#919,.T.);
#8636=EDGE_CURVE('',#7005,#7003,#457,.T.);
#8637=EDGE_CURVE('',#7006,#7007,#4179,.T.);
#8638=EDGE_CURVE('',#7002,#7006,#458,.T.);
#8639=EDGE_CURVE('',#7003,#7007,#459,.T.);
#8640=EDGE_CURVE('',#7008,#7009,#4180,.T.);
#8641=EDGE_CURVE('',#7006,#7008,#460,.T.);
#8642=EDGE_CURVE('',#7007,#7009,#461,.T.);
#8643=EDGE_CURVE('',#7010,#7011,#4181,.T.);
#8644=EDGE_CURVE('',#7008,#7010,#462,.T.);
#8645=EDGE_CURVE('',#7009,#7011,#463,.T.);
#8646=EDGE_CURVE('',#7012,#7013,#4182,.T.);
#8647=EDGE_CURVE('',#7010,#7012,#464,.T.);
#8648=EDGE_CURVE('',#7011,#7013,#465,.T.);
#8649=EDGE_CURVE('',#7014,#7015,#4183,.T.);
#8650=EDGE_CURVE('',#7012,#7014,#466,.T.);
#8651=EDGE_CURVE('',#7013,#7015,#467,.T.);
#8652=EDGE_CURVE('',#7016,#7017,#4184,.T.);
#8653=EDGE_CURVE('',#7014,#7016,#468,.T.);
#8654=EDGE_CURVE('',#7015,#7017,#469,.T.);
#8655=EDGE_CURVE('',#7018,#7019,#4185,.T.);
#8656=EDGE_CURVE('',#7016,#7018,#470,.T.);
#8657=EDGE_CURVE('',#7017,#7019,#471,.T.);
#8658=EDGE_CURVE('',#7020,#7021,#4186,.T.);
#8659=EDGE_CURVE('',#7018,#7020,#472,.T.);
#8660=EDGE_CURVE('',#7019,#7021,#473,.T.);
#8661=EDGE_CURVE('',#7022,#7023,#4187,.T.);
#8662=EDGE_CURVE('',#7020,#7022,#474,.T.);
#8663=EDGE_CURVE('',#7021,#7023,#475,.T.);
#8664=EDGE_CURVE('',#7024,#7025,#4188,.T.);
#8665=EDGE_CURVE('',#7022,#7024,#476,.T.);
#8666=EDGE_CURVE('',#7023,#7025,#477,.T.);
#8667=EDGE_CURVE('',#7026,#7027,#4189,.T.);
#8668=EDGE_CURVE('',#7024,#7026,#478,.T.);
#8669=EDGE_CURVE('',#7025,#7027,#479,.T.);
#8670=EDGE_CURVE('',#7028,#7029,#4190,.T.);
#8671=EDGE_CURVE('',#7026,#7028,#480,.T.);
#8672=EDGE_CURVE('',#7027,#7029,#481,.T.);
#8673=EDGE_CURVE('',#7030,#7031,#4191,.T.);
#8674=EDGE_CURVE('',#7028,#7030,#482,.T.);
#8675=EDGE_CURVE('',#7029,#7031,#483,.T.);
#8676=EDGE_CURVE('',#7032,#7033,#4192,.T.);
#8677=EDGE_CURVE('',#7030,#7032,#484,.T.);
#8678=EDGE_CURVE('',#7031,#7033,#485,.T.);
#8679=EDGE_CURVE('',#7034,#7035,#4193,.T.);
#8680=EDGE_CURVE('',#7032,#7034,#486,.T.);
#8681=EDGE_CURVE('',#7033,#7035,#487,.T.);
#8682=EDGE_CURVE('',#7036,#7037,#4194,.T.);
#8683=EDGE_CURVE('',#7034,#7036,#488,.T.);
#8684=EDGE_CURVE('',#7035,#7037,#489,.T.);
#8685=EDGE_CURVE('',#7038,#7039,#4195,.T.);
#8686=EDGE_CURVE('',#7036,#7038,#490,.T.);
#8687=EDGE_CURVE('',#7037,#7039,#491,.T.);
#8688=EDGE_CURVE('',#7040,#7041,#4196,.T.);
#8689=EDGE_CURVE('',#7038,#7040,#492,.T.);
#8690=EDGE_CURVE('',#7039,#7041,#493,.T.);
#8691=EDGE_CURVE('',#7042,#7043,#4197,.T.);
#8692=EDGE_CURVE('',#7040,#7042,#494,.T.);
#8693=EDGE_CURVE('',#7041,#7043,#495,.T.);
#8694=EDGE_CURVE('',#7044,#7045,#4198,.T.);
#8695=EDGE_CURVE('',#7042,#7044,#496,.T.);
#8696=EDGE_CURVE('',#7043,#7045,#497,.T.);
#8697=EDGE_CURVE('',#7046,#7047,#4199,.T.);
#8698=EDGE_CURVE('',#7044,#7046,#498,.T.);
#8699=EDGE_CURVE('',#7045,#7047,#499,.T.);
#8700=EDGE_CURVE('',#7048,#7049,#4200,.T.);
#8701=EDGE_CURVE('',#7048,#7050,#317,.T.);
#8702=EDGE_CURVE('',#7050,#7051,#4201,.T.);
#8703=EDGE_CURVE('',#7051,#7052,#318,.T.);
#8704=EDGE_CURVE('',#7052,#7053,#319,.T.);
#8705=EDGE_CURVE('',#7053,#7054,#320,.T.);
#8706=EDGE_CURVE('',#7054,#7055,#321,.T.);
#8707=EDGE_CURVE('',#7055,#7056,#322,.T.);
#8708=EDGE_CURVE('',#7056,#7051,#323,.T.);
#8709=EDGE_CURVE('',#7050,#7057,#324,.T.);
#8710=EDGE_CURVE('',#7057,#7058,#4202,.T.);
#8711=EDGE_CURVE('',#7049,#7058,#325,.F.);
#8712=EDGE_CURVE('',#7059,#7060,#4203,.T.);
#8713=EDGE_CURVE('',#7059,#7048,#326,.T.);
#8714=EDGE_CURVE('',#7060,#7049,#327,.F.);
#8715=EDGE_CURVE('',#7061,#7062,#4204,.T.);
#8716=EDGE_CURVE('',#7061,#7059,#328,.T.);
#8717=EDGE_CURVE('',#7062,#7060,#329,.F.);
#8718=EDGE_CURVE('',#7063,#7064,#4205,.T.);
#8719=EDGE_CURVE('',#7063,#7061,#330,.T.);
#8720=EDGE_CURVE('',#7064,#7062,#331,.F.);
#8721=EDGE_CURVE('',#7065,#7066,#4206,.T.);
#8722=EDGE_CURVE('',#7065,#7063,#332,.T.);
#8723=EDGE_CURVE('',#7066,#7064,#333,.F.);
#8724=EDGE_CURVE('',#7067,#7068,#4207,.T.);
#8725=EDGE_CURVE('',#7067,#7065,#334,.T.);
#8726=EDGE_CURVE('',#7068,#7066,#335,.F.);
#8727=EDGE_CURVE('',#7069,#7070,#4208,.T.);
#8728=EDGE_CURVE('',#7069,#7067,#336,.T.);
#8729=EDGE_CURVE('',#7070,#7068,#337,.F.);
#8730=EDGE_CURVE('',#7071,#7072,#4209,.T.);
#8731=EDGE_CURVE('',#7071,#7069,#338,.T.);
#8732=EDGE_CURVE('',#7072,#7070,#339,.F.);
#8733=EDGE_CURVE('',#7073,#7074,#4210,.T.);
#8734=EDGE_CURVE('',#7073,#7071,#340,.T.);
#8735=EDGE_CURVE('',#7074,#7072,#341,.F.);
#8736=EDGE_CURVE('',#7075,#7076,#4211,.T.);
#8737=EDGE_CURVE('',#7075,#7073,#342,.T.);
#8738=EDGE_CURVE('',#7076,#7074,#343,.F.);
#8739=EDGE_CURVE('',#7077,#7078,#4212,.T.);
#8740=EDGE_CURVE('',#7077,#7075,#344,.T.);
#8741=EDGE_CURVE('',#7078,#7076,#345,.F.);
#8742=EDGE_CURVE('',#7079,#7080,#4213,.T.);
#8743=EDGE_CURVE('',#7079,#7077,#346,.T.);
#8744=EDGE_CURVE('',#7080,#7078,#347,.F.);
#8745=EDGE_CURVE('',#7081,#7082,#4214,.T.);
#8746=EDGE_CURVE('',#7081,#7079,#348,.T.);
#8747=EDGE_CURVE('',#7082,#7080,#349,.F.);
#8748=EDGE_CURVE('',#7083,#7084,#4215,.T.);
#8749=EDGE_CURVE('',#7083,#7081,#350,.T.);
#8750=EDGE_CURVE('',#7084,#7082,#351,.F.);
#8751=EDGE_CURVE('',#7085,#7086,#4216,.T.);
#8752=EDGE_CURVE('',#7085,#7083,#352,.T.);
#8753=EDGE_CURVE('',#7086,#7084,#353,.F.);
#8754=EDGE_CURVE('',#7087,#7088,#4217,.T.);
#8755=EDGE_CURVE('',#7087,#7085,#354,.T.);
#8756=EDGE_CURVE('',#7088,#7086,#355,.F.);
#8757=EDGE_CURVE('',#7089,#7090,#4218,.T.);
#8758=EDGE_CURVE('',#7089,#7087,#356,.T.);
#8759=EDGE_CURVE('',#7090,#7088,#357,.F.);
#8760=EDGE_CURVE('',#7091,#7092,#4219,.T.);
#8761=EDGE_CURVE('',#7091,#7089,#358,.T.);
#8762=EDGE_CURVE('',#7092,#7090,#359,.F.);
#8763=EDGE_CURVE('',#7093,#7094,#4220,.T.);
#8764=EDGE_CURVE('',#7093,#7091,#360,.T.);
#8765=EDGE_CURVE('',#7094,#7092,#361,.F.);
#8766=EDGE_CURVE('',#7095,#7096,#4221,.T.);
#8767=EDGE_CURVE('',#7095,#7093,#362,.T.);
#8768=EDGE_CURVE('',#7096,#7094,#363,.F.);
#8769=EDGE_CURVE('',#7097,#7098,#4222,.T.);
#8770=EDGE_CURVE('',#7097,#7099,#920,.T.);
#8771=EDGE_CURVE('',#7099,#7095,#364,.T.);
#8772=EDGE_CURVE('',#7098,#7096,#365,.F.);
#8773=EDGE_CURVE('',#7100,#7101,#921,.T.);
#8774=EDGE_CURVE('',#7100,#7102,#922,.T.);
#8775=EDGE_CURVE('',#7103,#7102,#923,.T.);
#8776=EDGE_CURVE('',#7101,#7103,#924,.T.);
#8777=EDGE_CURVE('',#7104,#7105,#925,.T.);
#8778=EDGE_CURVE('',#7104,#7106,#926,.T.);
#8779=EDGE_CURVE('',#7107,#7106,#927,.T.);
#8780=EDGE_CURVE('',#7105,#7107,#928,.T.);
#8781=EDGE_CURVE('',#7108,#7108,#929,.T.);
#8782=EDGE_CURVE('',#7108,#7109,#4223,.T.);
#8783=EDGE_CURVE('',#7109,#7109,#930,.T.);
#8784=EDGE_CURVE('',#7106,#7100,#366,.T.);
#8785=EDGE_CURVE('',#7101,#7107,#367,.T.);
#8786=EDGE_CURVE('',#7004,#7099,#368,.T.);
#8787=EDGE_CURVE('',#7110,#7097,#931,.T.);
#8788=EDGE_CURVE('',#7110,#7111,#369,.T.);
#8789=EDGE_CURVE('',#7111,#7112,#4224,.T.);
#8790=EDGE_CURVE('',#7112,#7112,#932,.T.);
#8791=EDGE_CURVE('',#7111,#7005,#370,.T.);
#8792=EDGE_CURVE('',#7110,#7098,#371,.F.);
#8793=EDGE_CURVE('',#7105,#7113,#372,.T.);
#8794=EDGE_CURVE('',#7113,#7051,#373,.T.);
#8795=EDGE_CURVE('',#7051,#7114,#374,.T.);
#8796=EDGE_CURVE('',#7114,#7104,#375,.T.);
#8797=EDGE_CURVE('',#7102,#7115,#376,.T.);
#8798=EDGE_CURVE('',#7115,#7054,#377,.T.);
#8799=EDGE_CURVE('',#7054,#7116,#378,.T.);
#8800=EDGE_CURVE('',#7116,#7103,#379,.T.);
#8801=EDGE_CURVE('',#7058,#7117,#4225,.T.);
#8802=EDGE_CURVE('',#7118,#7057,#4226,.T.);
#8803=EDGE_CURVE('',#7117,#7118,#4227,.T.);
#8804=EDGE_CURVE('',#7047,#7117,#500,.T.);
#8805=EDGE_CURVE('',#7046,#7118,#501,.T.);
#8806=EDGE_CURVE('',#7051,#7119,#380,.T.);
#8807=EDGE_CURVE('',#7052,#7119,#933,.T.);
#8808=EDGE_CURVE('',#7119,#7107,#381,.T.);
#8809=EDGE_CURVE('',#7101,#7120,#382,.T.);
#8810=EDGE_CURVE('',#7053,#7120,#934,.T.);
#8811=EDGE_CURVE('',#7120,#7054,#383,.T.);
#8812=EDGE_CURVE('',#7054,#7121,#384,.T.);
#8813=EDGE_CURVE('',#7055,#7121,#935,.T.);
#8814=EDGE_CURVE('',#7121,#7100,#385,.T.);
#8815=EDGE_CURVE('',#7106,#7122,#386,.T.);
#8816=EDGE_CURVE('',#7056,#7122,#936,.T.);
#8817=EDGE_CURVE('',#7122,#7051,#387,.T.);
#8818=EDGE_CURVE('',#7114,#7122,#937,.T.);
#8819=EDGE_CURVE('',#7113,#7119,#938,.T.);
#8820=EDGE_CURVE('',#7121,#7115,#939,.T.);
#8821=EDGE_CURVE('',#7120,#7116,#940,.T.);
#11499=ORIENTED_EDGE('',*,*,#8633,.F.);
#11500=ORIENTED_EDGE('',*,*,#8634,.F.);
#11501=ORIENTED_EDGE('',*,*,#8635,.F.);
#11502=ORIENTED_EDGE('',*,*,#8636,.T.);
#11503=ORIENTED_EDGE('',*,*,#8637,.F.);
#11504=ORIENTED_EDGE('',*,*,#8638,.F.);
#11505=ORIENTED_EDGE('',*,*,#8633,.T.);
#11506=ORIENTED_EDGE('',*,*,#8639,.T.);
#11507=ORIENTED_EDGE('',*,*,#8640,.F.);
#11508=ORIENTED_EDGE('',*,*,#8641,.F.);
#11509=ORIENTED_EDGE('',*,*,#8637,.T.);
#11510=ORIENTED_EDGE('',*,*,#8642,.T.);
#11511=ORIENTED_EDGE('',*,*,#8643,.F.);
#11512=ORIENTED_EDGE('',*,*,#8644,.F.);
#11513=ORIENTED_EDGE('',*,*,#8640,.T.);
#11514=ORIENTED_EDGE('',*,*,#8645,.T.);
#11515=ORIENTED_EDGE('',*,*,#8646,.F.);
#11516=ORIENTED_EDGE('',*,*,#8647,.F.);
#11517=ORIENTED_EDGE('',*,*,#8643,.T.);
#11518=ORIENTED_EDGE('',*,*,#8648,.T.);
#11519=ORIENTED_EDGE('',*,*,#8649,.F.);
#11520=ORIENTED_EDGE('',*,*,#8650,.F.);
#11521=ORIENTED_EDGE('',*,*,#8646,.T.);
#11522=ORIENTED_EDGE('',*,*,#8651,.T.);
#11523=ORIENTED_EDGE('',*,*,#8652,.F.);
#11524=ORIENTED_EDGE('',*,*,#8653,.F.);
#11525=ORIENTED_EDGE('',*,*,#8649,.T.);
#11526=ORIENTED_EDGE('',*,*,#8654,.T.);
#11527=ORIENTED_EDGE('',*,*,#8655,.F.);
#11528=ORIENTED_EDGE('',*,*,#8656,.F.);
#11529=ORIENTED_EDGE('',*,*,#8652,.T.);
#11530=ORIENTED_EDGE('',*,*,#8657,.T.);
#11531=ORIENTED_EDGE('',*,*,#8658,.F.);
#11532=ORIENTED_EDGE('',*,*,#8659,.F.);
#11533=ORIENTED_EDGE('',*,*,#8655,.T.);
#11534=ORIENTED_EDGE('',*,*,#8660,.T.);
#11535=ORIENTED_EDGE('',*,*,#8661,.F.);
#11536=ORIENTED_EDGE('',*,*,#8662,.F.);
#11537=ORIENTED_EDGE('',*,*,#8658,.T.);
#11538=ORIENTED_EDGE('',*,*,#8663,.T.);
#11539=ORIENTED_EDGE('',*,*,#8664,.F.);
#11540=ORIENTED_EDGE('',*,*,#8665,.F.);
#11541=ORIENTED_EDGE('',*,*,#8661,.T.);
#11542=ORIENTED_EDGE('',*,*,#8666,.T.);
#11543=ORIENTED_EDGE('',*,*,#8667,.F.);
#11544=ORIENTED_EDGE('',*,*,#8668,.F.);
#11545=ORIENTED_EDGE('',*,*,#8664,.T.);
#11546=ORIENTED_EDGE('',*,*,#8669,.T.);
#11547=ORIENTED_EDGE('',*,*,#8670,.F.);
#11548=ORIENTED_EDGE('',*,*,#8671,.F.);
#11549=ORIENTED_EDGE('',*,*,#8667,.T.);
#11550=ORIENTED_EDGE('',*,*,#8672,.T.);
#11551=ORIENTED_EDGE('',*,*,#8673,.F.);
#11552=ORIENTED_EDGE('',*,*,#8674,.F.);
#11553=ORIENTED_EDGE('',*,*,#8670,.T.);
#11554=ORIENTED_EDGE('',*,*,#8675,.T.);
#11555=ORIENTED_EDGE('',*,*,#8676,.F.);
#11556=ORIENTED_EDGE('',*,*,#8677,.F.);
#11557=ORIENTED_EDGE('',*,*,#8673,.T.);
#11558=ORIENTED_EDGE('',*,*,#8678,.T.);
#11559=ORIENTED_EDGE('',*,*,#8679,.F.);
#11560=ORIENTED_EDGE('',*,*,#8680,.F.);
#11561=ORIENTED_EDGE('',*,*,#8676,.T.);
#11562=ORIENTED_EDGE('',*,*,#8681,.T.);
#11563=ORIENTED_EDGE('',*,*,#8682,.F.);
#11564=ORIENTED_EDGE('',*,*,#8683,.F.);
#11565=ORIENTED_EDGE('',*,*,#8679,.T.);
#11566=ORIENTED_EDGE('',*,*,#8684,.T.);
#11567=ORIENTED_EDGE('',*,*,#8685,.F.);
#11568=ORIENTED_EDGE('',*,*,#8686,.F.);
#11569=ORIENTED_EDGE('',*,*,#8682,.T.);
#11570=ORIENTED_EDGE('',*,*,#8687,.T.);
#11571=ORIENTED_EDGE('',*,*,#8688,.F.);
#11572=ORIENTED_EDGE('',*,*,#8689,.F.);
#11573=ORIENTED_EDGE('',*,*,#8685,.T.);
#11574=ORIENTED_EDGE('',*,*,#8690,.T.);
#11575=ORIENTED_EDGE('',*,*,#8691,.F.);
#11576=ORIENTED_EDGE('',*,*,#8692,.F.);
#11577=ORIENTED_EDGE('',*,*,#8688,.T.);
#11578=ORIENTED_EDGE('',*,*,#8693,.T.);
#11579=ORIENTED_EDGE('',*,*,#8694,.F.);
#11580=ORIENTED_EDGE('',*,*,#8695,.F.);
#11581=ORIENTED_EDGE('',*,*,#8691,.T.);
#11582=ORIENTED_EDGE('',*,*,#8696,.T.);
#11583=ORIENTED_EDGE('',*,*,#8697,.F.);
#11584=ORIENTED_EDGE('',*,*,#8698,.F.);
#11585=ORIENTED_EDGE('',*,*,#8694,.T.);
#11586=ORIENTED_EDGE('',*,*,#8699,.T.);
#11587=ORIENTED_EDGE('',*,*,#8700,.F.);
#11588=ORIENTED_EDGE('',*,*,#8701,.T.);
#11589=ORIENTED_EDGE('',*,*,#8702,.T.);
#11590=ORIENTED_EDGE('',*,*,#8703,.T.);
#11591=ORIENTED_EDGE('',*,*,#8704,.T.);
#11592=ORIENTED_EDGE('',*,*,#8705,.T.);
#11593=ORIENTED_EDGE('',*,*,#8706,.T.);
#11594=ORIENTED_EDGE('',*,*,#8707,.T.);
#11595=ORIENTED_EDGE('',*,*,#8708,.T.);
#11596=ORIENTED_EDGE('',*,*,#8702,.F.);
#11597=ORIENTED_EDGE('',*,*,#8709,.T.);
#11598=ORIENTED_EDGE('',*,*,#8710,.T.);
#11599=ORIENTED_EDGE('',*,*,#8711,.F.);
#11600=ORIENTED_EDGE('',*,*,#8712,.F.);
#11601=ORIENTED_EDGE('',*,*,#8713,.T.);
#11602=ORIENTED_EDGE('',*,*,#8700,.T.);
#11603=ORIENTED_EDGE('',*,*,#8714,.F.);
#11604=ORIENTED_EDGE('',*,*,#8715,.F.);
#11605=ORIENTED_EDGE('',*,*,#8716,.T.);
#11606=ORIENTED_EDGE('',*,*,#8712,.T.);
#11607=ORIENTED_EDGE('',*,*,#8717,.F.);
#11608=ORIENTED_EDGE('',*,*,#8718,.F.);
#11609=ORIENTED_EDGE('',*,*,#8719,.T.);
#11610=ORIENTED_EDGE('',*,*,#8715,.T.);
#11611=ORIENTED_EDGE('',*,*,#8720,.F.);
#11612=ORIENTED_EDGE('',*,*,#8721,.F.);
#11613=ORIENTED_EDGE('',*,*,#8722,.T.);
#11614=ORIENTED_EDGE('',*,*,#8718,.T.);
#11615=ORIENTED_EDGE('',*,*,#8723,.F.);
#11616=ORIENTED_EDGE('',*,*,#8724,.F.);
#11617=ORIENTED_EDGE('',*,*,#8725,.T.);
#11618=ORIENTED_EDGE('',*,*,#8721,.T.);
#11619=ORIENTED_EDGE('',*,*,#8726,.F.);
#11620=ORIENTED_EDGE('',*,*,#8727,.F.);
#11621=ORIENTED_EDGE('',*,*,#8728,.T.);
#11622=ORIENTED_EDGE('',*,*,#8724,.T.);
#11623=ORIENTED_EDGE('',*,*,#8729,.F.);
#11624=ORIENTED_EDGE('',*,*,#8730,.F.);
#11625=ORIENTED_EDGE('',*,*,#8731,.T.);
#11626=ORIENTED_EDGE('',*,*,#8727,.T.);
#11627=ORIENTED_EDGE('',*,*,#8732,.F.);
#11628=ORIENTED_EDGE('',*,*,#8733,.F.);
#11629=ORIENTED_EDGE('',*,*,#8734,.T.);
#11630=ORIENTED_EDGE('',*,*,#8730,.T.);
#11631=ORIENTED_EDGE('',*,*,#8735,.F.);
#11632=ORIENTED_EDGE('',*,*,#8736,.F.);
#11633=ORIENTED_EDGE('',*,*,#8737,.T.);
#11634=ORIENTED_EDGE('',*,*,#8733,.T.);
#11635=ORIENTED_EDGE('',*,*,#8738,.F.);
#11636=ORIENTED_EDGE('',*,*,#8739,.F.);
#11637=ORIENTED_EDGE('',*,*,#8740,.T.);
#11638=ORIENTED_EDGE('',*,*,#8736,.T.);
#11639=ORIENTED_EDGE('',*,*,#8741,.F.);
#11640=ORIENTED_EDGE('',*,*,#8742,.F.);
#11641=ORIENTED_EDGE('',*,*,#8743,.T.);
#11642=ORIENTED_EDGE('',*,*,#8739,.T.);
#11643=ORIENTED_EDGE('',*,*,#8744,.F.);
#11644=ORIENTED_EDGE('',*,*,#8745,.F.);
#11645=ORIENTED_EDGE('',*,*,#8746,.T.);
#11646=ORIENTED_EDGE('',*,*,#8742,.T.);
#11647=ORIENTED_EDGE('',*,*,#8747,.F.);
#11648=ORIENTED_EDGE('',*,*,#8748,.F.);
#11649=ORIENTED_EDGE('',*,*,#8749,.T.);
#11650=ORIENTED_EDGE('',*,*,#8745,.T.);
#11651=ORIENTED_EDGE('',*,*,#8750,.F.);
#11652=ORIENTED_EDGE('',*,*,#8751,.F.);
#11653=ORIENTED_EDGE('',*,*,#8752,.T.);
#11654=ORIENTED_EDGE('',*,*,#8748,.T.);
#11655=ORIENTED_EDGE('',*,*,#8753,.F.);
#11656=ORIENTED_EDGE('',*,*,#8754,.F.);
#11657=ORIENTED_EDGE('',*,*,#8755,.T.);
#11658=ORIENTED_EDGE('',*,*,#8751,.T.);
#11659=ORIENTED_EDGE('',*,*,#8756,.F.);
#11660=ORIENTED_EDGE('',*,*,#8757,.F.);
#11661=ORIENTED_EDGE('',*,*,#8758,.T.);
#11662=ORIENTED_EDGE('',*,*,#8754,.T.);
#11663=ORIENTED_EDGE('',*,*,#8759,.F.);
#11664=ORIENTED_EDGE('',*,*,#8760,.F.);
#11665=ORIENTED_EDGE('',*,*,#8761,.T.);
#11666=ORIENTED_EDGE('',*,*,#8757,.T.);
#11667=ORIENTED_EDGE('',*,*,#8762,.F.);
#11668=ORIENTED_EDGE('',*,*,#8763,.F.);
#11669=ORIENTED_EDGE('',*,*,#8764,.T.);
#11670=ORIENTED_EDGE('',*,*,#8760,.T.);
#11671=ORIENTED_EDGE('',*,*,#8765,.F.);
#11672=ORIENTED_EDGE('',*,*,#8766,.F.);
#11673=ORIENTED_EDGE('',*,*,#8767,.T.);
#11674=ORIENTED_EDGE('',*,*,#8763,.T.);
#11675=ORIENTED_EDGE('',*,*,#8768,.F.);
#11676=ORIENTED_EDGE('',*,*,#8769,.F.);
#11677=ORIENTED_EDGE('',*,*,#8770,.T.);
#11678=ORIENTED_EDGE('',*,*,#8771,.T.);
#11679=ORIENTED_EDGE('',*,*,#8766,.T.);
#11680=ORIENTED_EDGE('',*,*,#8772,.F.);
#11681=ORIENTED_EDGE('',*,*,#8773,.F.);
#11682=ORIENTED_EDGE('',*,*,#8774,.T.);
#11683=ORIENTED_EDGE('',*,*,#8775,.F.);
#11684=ORIENTED_EDGE('',*,*,#8776,.F.);
#11685=ORIENTED_EDGE('',*,*,#8777,.F.);
#11686=ORIENTED_EDGE('',*,*,#8778,.T.);
#11687=ORIENTED_EDGE('',*,*,#8779,.F.);
#11688=ORIENTED_EDGE('',*,*,#8780,.F.);
#11689=ORIENTED_EDGE('',*,*,#8781,.F.);
#11690=ORIENTED_EDGE('',*,*,#8782,.T.);
#11691=ORIENTED_EDGE('',*,*,#8783,.T.);
#11692=ORIENTED_EDGE('',*,*,#8782,.F.);
#11693=ORIENTED_EDGE('',*,*,#8779,.T.);
#11694=ORIENTED_EDGE('',*,*,#8784,.T.);
#11695=ORIENTED_EDGE('',*,*,#8773,.T.);
#11696=ORIENTED_EDGE('',*,*,#8785,.T.);
#11697=ORIENTED_EDGE('',*,*,#8635,.T.);
#11698=ORIENTED_EDGE('',*,*,#8786,.T.);
#11699=ORIENTED_EDGE('',*,*,#8770,.F.);
#11700=ORIENTED_EDGE('',*,*,#8787,.F.);
#11701=ORIENTED_EDGE('',*,*,#8788,.T.);
#11702=ORIENTED_EDGE('',*,*,#8789,.T.);
#11703=ORIENTED_EDGE('',*,*,#8790,.F.);
#11704=ORIENTED_EDGE('',*,*,#8789,.F.);
#11705=ORIENTED_EDGE('',*,*,#8791,.T.);
#11706=ORIENTED_EDGE('',*,*,#8769,.T.);
#11707=ORIENTED_EDGE('',*,*,#8792,.F.);
#11708=ORIENTED_EDGE('',*,*,#8787,.T.);
#11709=ORIENTED_EDGE('',*,*,#8777,.T.);
#11710=ORIENTED_EDGE('',*,*,#8793,.T.);
#11711=ORIENTED_EDGE('',*,*,#8794,.T.);
#11712=ORIENTED_EDGE('',*,*,#8795,.T.);
#11713=ORIENTED_EDGE('',*,*,#8796,.T.);
#11714=ORIENTED_EDGE('',*,*,#8781,.T.);
#11715=ORIENTED_EDGE('',*,*,#8797,.T.);
#11716=ORIENTED_EDGE('',*,*,#8798,.T.);
#11717=ORIENTED_EDGE('',*,*,#8799,.T.);
#11718=ORIENTED_EDGE('',*,*,#8800,.T.);
#11719=ORIENTED_EDGE('',*,*,#8775,.T.);
#11720=ORIENTED_EDGE('',*,*,#8783,.F.);
#11721=ORIENTED_EDGE('',*,*,#8790,.T.);
#11722=ORIENTED_EDGE('',*,*,#8801,.F.);
#11723=ORIENTED_EDGE('',*,*,#8710,.F.);
#11724=ORIENTED_EDGE('',*,*,#8802,.F.);
#11725=ORIENTED_EDGE('',*,*,#8803,.F.);
#11726=ORIENTED_EDGE('',*,*,#8792,.T.);
#11727=ORIENTED_EDGE('',*,*,#8772,.T.);
#11728=ORIENTED_EDGE('',*,*,#8768,.T.);
#11729=ORIENTED_EDGE('',*,*,#8765,.T.);
#11730=ORIENTED_EDGE('',*,*,#8762,.T.);
#11731=ORIENTED_EDGE('',*,*,#8759,.T.);
#11732=ORIENTED_EDGE('',*,*,#8756,.T.);
#11733=ORIENTED_EDGE('',*,*,#8753,.T.);
#11734=ORIENTED_EDGE('',*,*,#8750,.T.);
#11735=ORIENTED_EDGE('',*,*,#8747,.T.);
#11736=ORIENTED_EDGE('',*,*,#8744,.T.);
#11737=ORIENTED_EDGE('',*,*,#8741,.T.);
#11738=ORIENTED_EDGE('',*,*,#8738,.T.);
#11739=ORIENTED_EDGE('',*,*,#8735,.T.);
#11740=ORIENTED_EDGE('',*,*,#8732,.T.);
#11741=ORIENTED_EDGE('',*,*,#8729,.T.);
#11742=ORIENTED_EDGE('',*,*,#8726,.T.);
#11743=ORIENTED_EDGE('',*,*,#8723,.T.);
#11744=ORIENTED_EDGE('',*,*,#8720,.T.);
#11745=ORIENTED_EDGE('',*,*,#8717,.T.);
#11746=ORIENTED_EDGE('',*,*,#8714,.T.);
#11747=ORIENTED_EDGE('',*,*,#8711,.T.);
#11748=ORIENTED_EDGE('',*,*,#8801,.T.);
#11749=ORIENTED_EDGE('',*,*,#8804,.F.);
#11750=ORIENTED_EDGE('',*,*,#8699,.F.);
#11751=ORIENTED_EDGE('',*,*,#8696,.F.);
#11752=ORIENTED_EDGE('',*,*,#8693,.F.);
#11753=ORIENTED_EDGE('',*,*,#8690,.F.);
#11754=ORIENTED_EDGE('',*,*,#8687,.F.);
#11755=ORIENTED_EDGE('',*,*,#8684,.F.);
#11756=ORIENTED_EDGE('',*,*,#8681,.F.);
#11757=ORIENTED_EDGE('',*,*,#8678,.F.);
#11758=ORIENTED_EDGE('',*,*,#8675,.F.);
#11759=ORIENTED_EDGE('',*,*,#8672,.F.);
#11760=ORIENTED_EDGE('',*,*,#8669,.F.);
#11761=ORIENTED_EDGE('',*,*,#8666,.F.);
#11762=ORIENTED_EDGE('',*,*,#8663,.F.);
#11763=ORIENTED_EDGE('',*,*,#8660,.F.);
#11764=ORIENTED_EDGE('',*,*,#8657,.F.);
#11765=ORIENTED_EDGE('',*,*,#8654,.F.);
#11766=ORIENTED_EDGE('',*,*,#8651,.F.);
#11767=ORIENTED_EDGE('',*,*,#8648,.F.);
#11768=ORIENTED_EDGE('',*,*,#8645,.F.);
#11769=ORIENTED_EDGE('',*,*,#8642,.F.);
#11770=ORIENTED_EDGE('',*,*,#8639,.F.);
#11771=ORIENTED_EDGE('',*,*,#8636,.F.);
#11772=ORIENTED_EDGE('',*,*,#8791,.F.);
#11773=ORIENTED_EDGE('',*,*,#8788,.F.);
#11774=ORIENTED_EDGE('',*,*,#8697,.T.);
#11775=ORIENTED_EDGE('',*,*,#8804,.T.);
#11776=ORIENTED_EDGE('',*,*,#8803,.T.);
#11777=ORIENTED_EDGE('',*,*,#8805,.F.);
#11778=ORIENTED_EDGE('',*,*,#8634,.T.);
#11779=ORIENTED_EDGE('',*,*,#8638,.T.);
#11780=ORIENTED_EDGE('',*,*,#8641,.T.);
#11781=ORIENTED_EDGE('',*,*,#8644,.T.);
#11782=ORIENTED_EDGE('',*,*,#8647,.T.);
#11783=ORIENTED_EDGE('',*,*,#8650,.T.);
#11784=ORIENTED_EDGE('',*,*,#8653,.T.);
#11785=ORIENTED_EDGE('',*,*,#8656,.T.);
#11786=ORIENTED_EDGE('',*,*,#8659,.T.);
#11787=ORIENTED_EDGE('',*,*,#8662,.T.);
#11788=ORIENTED_EDGE('',*,*,#8665,.T.);
#11789=ORIENTED_EDGE('',*,*,#8668,.T.);
#11790=ORIENTED_EDGE('',*,*,#8671,.T.);
#11791=ORIENTED_EDGE('',*,*,#8674,.T.);
#11792=ORIENTED_EDGE('',*,*,#8677,.T.);
#11793=ORIENTED_EDGE('',*,*,#8680,.T.);
#11794=ORIENTED_EDGE('',*,*,#8683,.T.);
#11795=ORIENTED_EDGE('',*,*,#8686,.T.);
#11796=ORIENTED_EDGE('',*,*,#8689,.T.);
#11797=ORIENTED_EDGE('',*,*,#8692,.T.);
#11798=ORIENTED_EDGE('',*,*,#8695,.T.);
#11799=ORIENTED_EDGE('',*,*,#8698,.T.);
#11800=ORIENTED_EDGE('',*,*,#8805,.T.);
#11801=ORIENTED_EDGE('',*,*,#8802,.T.);
#11802=ORIENTED_EDGE('',*,*,#8709,.F.);
#11803=ORIENTED_EDGE('',*,*,#8701,.F.);
#11804=ORIENTED_EDGE('',*,*,#8713,.F.);
#11805=ORIENTED_EDGE('',*,*,#8716,.F.);
#11806=ORIENTED_EDGE('',*,*,#8719,.F.);
#11807=ORIENTED_EDGE('',*,*,#8722,.F.);
#11808=ORIENTED_EDGE('',*,*,#8725,.F.);
#11809=ORIENTED_EDGE('',*,*,#8728,.F.);
#11810=ORIENTED_EDGE('',*,*,#8731,.F.);
#11811=ORIENTED_EDGE('',*,*,#8734,.F.);
#11812=ORIENTED_EDGE('',*,*,#8737,.F.);
#11813=ORIENTED_EDGE('',*,*,#8740,.F.);
#11814=ORIENTED_EDGE('',*,*,#8743,.F.);
#11815=ORIENTED_EDGE('',*,*,#8746,.F.);
#11816=ORIENTED_EDGE('',*,*,#8749,.F.);
#11817=ORIENTED_EDGE('',*,*,#8752,.F.);
#11818=ORIENTED_EDGE('',*,*,#8755,.F.);
#11819=ORIENTED_EDGE('',*,*,#8758,.F.);
#11820=ORIENTED_EDGE('',*,*,#8761,.F.);
#11821=ORIENTED_EDGE('',*,*,#8764,.F.);
#11822=ORIENTED_EDGE('',*,*,#8767,.F.);
#11823=ORIENTED_EDGE('',*,*,#8771,.F.);
#11824=ORIENTED_EDGE('',*,*,#8786,.F.);
#11825=ORIENTED_EDGE('',*,*,#8703,.F.);
#11826=ORIENTED_EDGE('',*,*,#8806,.T.);
#11827=ORIENTED_EDGE('',*,*,#8807,.F.);
#11828=ORIENTED_EDGE('',*,*,#8807,.T.);
#11829=ORIENTED_EDGE('',*,*,#8808,.T.);
#11830=ORIENTED_EDGE('',*,*,#8785,.F.);
#11831=ORIENTED_EDGE('',*,*,#8809,.T.);
#11832=ORIENTED_EDGE('',*,*,#8810,.F.);
#11833=ORIENTED_EDGE('',*,*,#8704,.F.);
#11834=ORIENTED_EDGE('',*,*,#8810,.T.);
#11835=ORIENTED_EDGE('',*,*,#8811,.T.);
#11836=ORIENTED_EDGE('',*,*,#8705,.F.);
#11837=ORIENTED_EDGE('',*,*,#8706,.F.);
#11838=ORIENTED_EDGE('',*,*,#8812,.T.);
#11839=ORIENTED_EDGE('',*,*,#8813,.F.);
#11840=ORIENTED_EDGE('',*,*,#8813,.T.);
#11841=ORIENTED_EDGE('',*,*,#8814,.T.);
#11842=ORIENTED_EDGE('',*,*,#8784,.F.);
#11843=ORIENTED_EDGE('',*,*,#8815,.T.);
#11844=ORIENTED_EDGE('',*,*,#8816,.F.);
#11845=ORIENTED_EDGE('',*,*,#8707,.F.);
#11846=ORIENTED_EDGE('',*,*,#8816,.T.);
#11847=ORIENTED_EDGE('',*,*,#8817,.T.);
#11848=ORIENTED_EDGE('',*,*,#8708,.F.);
#11849=ORIENTED_EDGE('',*,*,#8795,.F.);
#11850=ORIENTED_EDGE('',*,*,#8817,.F.);
#11851=ORIENTED_EDGE('',*,*,#8818,.F.);
#11852=ORIENTED_EDGE('',*,*,#8818,.T.);
#11853=ORIENTED_EDGE('',*,*,#8815,.F.);
#11854=ORIENTED_EDGE('',*,*,#8778,.F.);
#11855=ORIENTED_EDGE('',*,*,#8796,.F.);
#11856=ORIENTED_EDGE('',*,*,#8780,.T.);
#11857=ORIENTED_EDGE('',*,*,#8808,.F.);
#11858=ORIENTED_EDGE('',*,*,#8819,.F.);
#11859=ORIENTED_EDGE('',*,*,#8793,.F.);
#11860=ORIENTED_EDGE('',*,*,#8806,.F.);
#11861=ORIENTED_EDGE('',*,*,#8794,.F.);
#11862=ORIENTED_EDGE('',*,*,#8819,.T.);
#11863=ORIENTED_EDGE('',*,*,#8812,.F.);
#11864=ORIENTED_EDGE('',*,*,#8798,.F.);
#11865=ORIENTED_EDGE('',*,*,#8820,.F.);
#11866=ORIENTED_EDGE('',*,*,#8820,.T.);
#11867=ORIENTED_EDGE('',*,*,#8797,.F.);
#11868=ORIENTED_EDGE('',*,*,#8774,.F.);
#11869=ORIENTED_EDGE('',*,*,#8814,.F.);
#11870=ORIENTED_EDGE('',*,*,#8776,.T.);
#11871=ORIENTED_EDGE('',*,*,#8800,.F.);
#11872=ORIENTED_EDGE('',*,*,#8821,.F.);
#11873=ORIENTED_EDGE('',*,*,#8809,.F.);
#11874=ORIENTED_EDGE('',*,*,#8799,.F.);
#11875=ORIENTED_EDGE('',*,*,#8811,.F.);
#11876=ORIENTED_EDGE('',*,*,#8821,.T.);
#14251=PLANE('',#16438);
#14252=PLANE('',#16439);
#14253=PLANE('',#16440);
#14254=PLANE('',#16441);
#14983=ADVANCED_FACE('',(#2015),#1186,.T.);
#14984=ADVANCED_FACE('',(#2016),#1187,.T.);
#14985=ADVANCED_FACE('',(#2017),#1188,.T.);
#14986=ADVANCED_FACE('',(#2018),#1189,.T.);
#14987=ADVANCED_FACE('',(#2019),#1190,.T.);
#14988=ADVANCED_FACE('',(#2020),#1191,.T.);
#14989=ADVANCED_FACE('',(#2021),#1192,.T.);
#14990=ADVANCED_FACE('',(#2022),#1193,.T.);
#14991=ADVANCED_FACE('',(#2023),#1194,.T.);
#14992=ADVANCED_FACE('',(#2024),#1195,.T.);
#14993=ADVANCED_FACE('',(#2025),#1196,.T.);
#14994=ADVANCED_FACE('',(#2026),#1197,.T.);
#14995=ADVANCED_FACE('',(#2027),#1198,.T.);
#14996=ADVANCED_FACE('',(#2028),#1199,.T.);
#14997=ADVANCED_FACE('',(#2029),#1200,.T.);
#14998=ADVANCED_FACE('',(#2030),#1201,.T.);
#14999=ADVANCED_FACE('',(#2031),#1202,.T.);
#15000=ADVANCED_FACE('',(#2032),#1203,.T.);
#15001=ADVANCED_FACE('',(#2033),#1204,.T.);
#15002=ADVANCED_FACE('',(#2034),#1205,.T.);
#15003=ADVANCED_FACE('',(#2035),#1206,.T.);
#15004=ADVANCED_FACE('',(#2036),#1207,.T.);
#15005=ADVANCED_FACE('',(#2037),#1208,.T.);
#15006=ADVANCED_FACE('',(#2038),#1209,.T.);
#15007=ADVANCED_FACE('',(#2039),#1210,.T.);
#15008=ADVANCED_FACE('',(#2040),#1211,.T.);
#15009=ADVANCED_FACE('',(#2041),#1212,.T.);
#15010=ADVANCED_FACE('',(#2042),#1213,.T.);
#15011=ADVANCED_FACE('',(#2043),#1214,.T.);
#15012=ADVANCED_FACE('',(#2044),#1215,.T.);
#15013=ADVANCED_FACE('',(#2045),#1216,.T.);
#15014=ADVANCED_FACE('',(#2046),#1217,.T.);
#15015=ADVANCED_FACE('',(#2047),#1218,.T.);
#15016=ADVANCED_FACE('',(#2048),#1219,.T.);
#15017=ADVANCED_FACE('',(#2049),#1220,.T.);
#15018=ADVANCED_FACE('',(#2050),#1221,.T.);
#15019=ADVANCED_FACE('',(#2051),#1222,.T.);
#15020=ADVANCED_FACE('',(#2052),#1223,.T.);
#15021=ADVANCED_FACE('',(#2053),#1224,.T.);
#15022=ADVANCED_FACE('',(#2054),#1225,.T.);
#15023=ADVANCED_FACE('',(#2055),#1226,.T.);
#15024=ADVANCED_FACE('',(#2056),#1227,.T.);
#15025=ADVANCED_FACE('',(#2057),#1228,.T.);
#15026=ADVANCED_FACE('',(#2058),#641,.T.);
#15027=ADVANCED_FACE('',(#2059),#642,.T.);
#15028=ADVANCED_FACE('',(#2060),#1229,.F.);
#15029=ADVANCED_FACE('',(#2061),#1230,.T.);
#15030=ADVANCED_FACE('',(#2062),#602,.T.);
#15031=ADVANCED_FACE('',(#2063),#1231,.T.);
#15032=ADVANCED_FACE('',(#2064,#1599),#14251,.F.);
#15033=ADVANCED_FACE('',(#2065,#1600),#14252,.T.);
#15034=ADVANCED_FACE('',(#2066),#14253,.T.);
#15035=ADVANCED_FACE('',(#2067),#14254,.T.);
#15036=ADVANCED_FACE('',(#2068),#299,.T.);
#15037=ADVANCED_FACE('',(#2069),#1232,.T.);
#15038=ADVANCED_FACE('',(#2070),#300,.T.);
#15039=ADVANCED_FACE('',(#2071),#301,.F.);
#15040=ADVANCED_FACE('',(#2072),#302,.F.);
#15041=ADVANCED_FACE('',(#2073),#303,.F.);
#15042=ADVANCED_FACE('',(#2074),#304,.F.);
#15043=ADVANCED_FACE('',(#2075),#305,.F.);
#15044=ADVANCED_FACE('',(#2076),#306,.F.);
#15045=ADVANCED_FACE('',(#2077),#307,.T.);
#15046=ADVANCED_FACE('',(#2078),#308,.T.);
#15047=ADVANCED_FACE('',(#2079),#309,.T.);
#15048=ADVANCED_FACE('',(#2080),#310,.T.);
#15049=ADVANCED_FACE('',(#2081),#311,.T.);
#15050=ADVANCED_FACE('',(#2082),#312,.T.);
#15051=ADVANCED_FACE('',(#2083),#313,.T.);
#15052=ADVANCED_FACE('',(#2084),#314,.T.);
#15570=CLOSED_SHELL('',(#14983,#14984,#14985,#14986,#14987,#14988,#14989,
#14990,#14991,#14992,#14993,#14994,#14995,#14996,#14997,#14998,#14999,#15000,
#15001,#15002,#15003,#15004,#15005,#15006,#15007,#15008,#15009,#15010,#15011,
#15012,#15013,#15014,#15015,#15016,#15017,#15018,#15019,#15020,#15021,#15022,
#15023,#15024,#15025,#15026,#15027,#15028,#15029,#15030,#15031,#15032,#15033,
#15034,#15035,#15036,#15037,#15038,#15039,#15040,#15041,#15042,#15043,#15044,
#15045,#15046,#15047,#15048,#15049,#15050,#15051,#15052));
#16374=AXIS2_PLACEMENT_3D('',#23070,#18844,#18845);
#16375=AXIS2_PLACEMENT_3D('',#23071,#18846,#18847);
#16376=AXIS2_PLACEMENT_3D('',#23088,#18849,#18850);
#16377=AXIS2_PLACEMENT_3D('',#23094,#18851,#18852);
#16378=AXIS2_PLACEMENT_3D('',#23140,#18854,#18855);
#16379=AXIS2_PLACEMENT_3D('',#23186,#18857,#18858);
#16380=AXIS2_PLACEMENT_3D('',#23232,#18860,#18861);
#16381=AXIS2_PLACEMENT_3D('',#23278,#18863,#18864);
#16382=AXIS2_PLACEMENT_3D('',#23324,#18866,#18867);
#16383=AXIS2_PLACEMENT_3D('',#23370,#18869,#18870);
#16384=AXIS2_PLACEMENT_3D('',#23416,#18872,#18873);
#16385=AXIS2_PLACEMENT_3D('',#23462,#18875,#18876);
#16386=AXIS2_PLACEMENT_3D('',#23508,#18878,#18879);
#16387=AXIS2_PLACEMENT_3D('',#23554,#18881,#18882);
#16388=AXIS2_PLACEMENT_3D('',#23600,#18884,#18885);
#16389=AXIS2_PLACEMENT_3D('',#23646,#18887,#18888);
#16390=AXIS2_PLACEMENT_3D('',#23692,#18890,#18891);
#16391=AXIS2_PLACEMENT_3D('',#23738,#18893,#18894);
#16392=AXIS2_PLACEMENT_3D('',#23784,#18896,#18897);
#16393=AXIS2_PLACEMENT_3D('',#23830,#18899,#18900);
#16394=AXIS2_PLACEMENT_3D('',#23876,#18902,#18903);
#16395=AXIS2_PLACEMENT_3D('',#23922,#18905,#18906);
#16396=AXIS2_PLACEMENT_3D('',#23968,#18908,#18909);
#16397=AXIS2_PLACEMENT_3D('',#24014,#18911,#18912);
#16398=AXIS2_PLACEMENT_3D('',#24060,#18914,#18915);
#16399=AXIS2_PLACEMENT_3D('',#24583,#18919,#18920);
#16400=AXIS2_PLACEMENT_3D('',#24659,#18922,#18923);
#16401=AXIS2_PLACEMENT_3D('',#24735,#18925,#18926);
#16402=AXIS2_PLACEMENT_3D('',#24811,#18928,#18929);
#16403=AXIS2_PLACEMENT_3D('',#24887,#18931,#18932);
#16404=AXIS2_PLACEMENT_3D('',#24963,#18934,#18935);
#16405=AXIS2_PLACEMENT_3D('',#25041,#18937,#18938);
#16406=AXIS2_PLACEMENT_3D('',#25117,#18940,#18941);
#16407=AXIS2_PLACEMENT_3D('',#25193,#18943,#18944);
#16408=AXIS2_PLACEMENT_3D('',#25271,#18946,#18947);
#16409=AXIS2_PLACEMENT_3D('',#25347,#18949,#18950);
#16410=AXIS2_PLACEMENT_3D('',#25423,#18952,#18953);
#16411=AXIS2_PLACEMENT_3D('',#25499,#18955,#18956);
#16412=AXIS2_PLACEMENT_3D('',#25575,#18958,#18959);
#16413=AXIS2_PLACEMENT_3D('',#25651,#18961,#18962);
#16414=AXIS2_PLACEMENT_3D('',#25729,#18964,#18965);
#16415=AXIS2_PLACEMENT_3D('',#25805,#18967,#18968);
#16416=AXIS2_PLACEMENT_3D('',#25883,#18970,#18971);
#16417=AXIS2_PLACEMENT_3D('',#25959,#18973,#18974);
#16418=AXIS2_PLACEMENT_3D('',#26035,#18976,#18977);
#16419=AXIS2_PLACEMENT_3D('',#26040,#18979,#18980);
#16420=AXIS2_PLACEMENT_3D('',#26111,#18981,#18982);
#16421=AXIS2_PLACEMENT_3D('',#26114,#18983,#18984);
#16422=AXIS2_PLACEMENT_3D('',#26116,#18985,#18986);
#16423=AXIS2_PLACEMENT_3D('',#26118,#18987,#18988);
#16424=AXIS2_PLACEMENT_3D('',#26119,#18989,#18990);
#16425=AXIS2_PLACEMENT_3D('',#26120,#18991,#18992);
#16426=AXIS2_PLACEMENT_3D('',#26123,#18993,#18994);
#16427=AXIS2_PLACEMENT_3D('',#26125,#18995,#18996);
#16428=AXIS2_PLACEMENT_3D('',#26127,#18997,#18998);
#16429=AXIS2_PLACEMENT_3D('',#26128,#18999,#19000);
#16430=AXIS2_PLACEMENT_3D('',#26129,#19001,#19002);
#16431=AXIS2_PLACEMENT_3D('',#26131,#19003,#19004);
#16432=AXIS2_PLACEMENT_3D('',#26134,#19006,#19007);
#16433=AXIS2_PLACEMENT_3D('',#26135,#19008,#19009);
#16434=AXIS2_PLACEMENT_3D('',#26270,#19010,#19011);
#16435=AXIS2_PLACEMENT_3D('',#26286,#19012,#19013);
#16436=AXIS2_PLACEMENT_3D('',#26308,#19015,#19016);
#16437=AXIS2_PLACEMENT_3D('',#26327,#19017,#19018);
#16438=AXIS2_PLACEMENT_3D('',#26334,#19019,#19020);
#16439=AXIS2_PLACEMENT_3D('',#26449,#19021,#19022);
#16440=AXIS2_PLACEMENT_3D('',#26561,#19023,#19024);
#16441=AXIS2_PLACEMENT_3D('',#26562,#19025,#19026);
#16442=AXIS2_PLACEMENT_3D('',#27447,#19030,#19031);
#16443=AXIS2_PLACEMENT_3D('',#28364,#19032,#19033);
#16444=AXIS2_PLACEMENT_3D('',#28548,#19034,#19035);
#16445=AXIS2_PLACEMENT_3D('',#28632,#19036,#19037);
#16446=AXIS2_PLACEMENT_3D('',#28816,#19038,#19039);
#16447=AXIS2_PLACEMENT_3D('',#28907,#19040,#19041);
#16448=AXIS2_PLACEMENT_3D('',#28950,#19042,#19043);
#16449=AXIS2_PLACEMENT_3D('',#29047,#19044,#19045);
#16450=AXIS2_PLACEMENT_3D('',#29090,#19046,#19047);
#18844=DIRECTION('axis',(0.,0.,1.));
#18845=DIRECTION('refdir',(1.,0.,0.));
#18846=DIRECTION('center_axis',(-8.74191357972136E-14,-1.,-3.36681878624147E-12));
#18847=DIRECTION('ref_axis',(-1.,8.79694822162854E-14,-1.3364594413628E-14));
#18848=DIRECTION('',(8.74191357972136E-14,1.,3.36681878624147E-12));
#18849=DIRECTION('center_axis',(2.81985569403837E-14,1.,-2.75774902090784E-13));
#18850=DIRECTION('ref_axis',(-3.32000459135762E-14,-2.76088836387462E-13,
-1.));
#18851=DIRECTION('center_axis',(-8.74191357972136E-14,-1.,-3.36681878624147E-12));
#18852=DIRECTION('ref_axis',(-1.,8.79694822162854E-14,-1.3364594413628E-14));
#18853=DIRECTION('',(8.74191357972136E-14,1.,3.36681878624147E-12));
#18854=DIRECTION('center_axis',(-8.74191357972136E-14,-1.,-3.36681878624147E-12));
#18855=DIRECTION('ref_axis',(-1.,8.79694822162854E-14,-1.3364594413628E-14));
#18856=DIRECTION('',(8.74191357972136E-14,1.,3.36681878624147E-12));
#18857=DIRECTION('center_axis',(-8.74191357972136E-14,-1.,-3.36681878624147E-12));
#18858=DIRECTION('ref_axis',(-1.,8.79694822162854E-14,-1.3364594413628E-14));
#18859=DIRECTION('',(8.74191357972136E-14,1.,3.36681878624147E-12));
#18860=DIRECTION('center_axis',(-8.74191357972136E-14,-1.,-3.36681878624147E-12));
#18861=DIRECTION('ref_axis',(-1.,8.79694822162854E-14,-1.3364594413628E-14));
#18862=DIRECTION('',(8.74191357972136E-14,1.,3.36681878624147E-12));
#18863=DIRECTION('center_axis',(-8.74191357972136E-14,-1.,-3.36681878624147E-12));
#18864=DIRECTION('ref_axis',(-1.,8.79694822162854E-14,-1.3364594413628E-14));
#18865=DIRECTION('',(8.74191357972136E-14,1.,3.36681878624147E-12));
#18866=DIRECTION('center_axis',(-8.74191357972136E-14,-1.,-3.36681878624147E-12));
#18867=DIRECTION('ref_axis',(-1.,8.79694822162854E-14,-1.3364594413628E-14));
#18868=DIRECTION('',(8.74191357972136E-14,1.,3.36681878624147E-12));
#18869=DIRECTION('center_axis',(-8.74191357972136E-14,-1.,-3.36681878624147E-12));
#18870=DIRECTION('ref_axis',(-1.,8.79694822162854E-14,-1.3364594413628E-14));
#18871=DIRECTION('',(8.74191357972136E-14,1.,3.36681878624147E-12));
#18872=DIRECTION('center_axis',(-8.74191357972136E-14,-1.,-3.36681878624147E-12));
#18873=DIRECTION('ref_axis',(-1.,8.79694822162854E-14,-1.3364594413628E-14));
#18874=DIRECTION('',(8.74191357972136E-14,1.,3.36681878624147E-12));
#18875=DIRECTION('center_axis',(-8.74191357972136E-14,-1.,-3.36681878624147E-12));
#18876=DIRECTION('ref_axis',(-1.,8.79694822162854E-14,-1.3364594413628E-14));
#18877=DIRECTION('',(8.74191357972136E-14,1.,3.36681878624147E-12));
#18878=DIRECTION('center_axis',(-8.74191357972136E-14,-1.,-3.36681878624147E-12));
#18879=DIRECTION('ref_axis',(-1.,8.79694822162854E-14,-1.3364594413628E-14));
#18880=DIRECTION('',(8.74191357972136E-14,1.,3.36681878624147E-12));
#18881=DIRECTION('center_axis',(-8.74191357972136E-14,-1.,-3.36681878624147E-12));
#18882=DIRECTION('ref_axis',(-1.,8.79694822162854E-14,-1.3364594413628E-14));
#18883=DIRECTION('',(8.74191357972136E-14,1.,3.36681878624147E-12));
#18884=DIRECTION('center_axis',(-8.74191357972136E-14,-1.,-3.36681878624147E-12));
#18885=DIRECTION('ref_axis',(-1.,8.79694822162854E-14,-1.3364594413628E-14));
#18886=DIRECTION('',(8.74191357972136E-14,1.,3.36681878624147E-12));
#18887=DIRECTION('center_axis',(-8.74191357972136E-14,-1.,-3.36681878624147E-12));
#18888=DIRECTION('ref_axis',(-1.,8.79694822162854E-14,-1.3364594413628E-14));
#18889=DIRECTION('',(8.74191357972136E-14,1.,3.36681878624147E-12));
#18890=DIRECTION('center_axis',(-8.74191357972136E-14,-1.,-3.36681878624147E-12));
#18891=DIRECTION('ref_axis',(-1.,8.79694822162854E-14,-1.3364594413628E-14));
#18892=DIRECTION('',(8.74191357972136E-14,1.,3.36681878624147E-12));
#18893=DIRECTION('center_axis',(-8.74191357972136E-14,-1.,-3.36681878624147E-12));
#18894=DIRECTION('ref_axis',(-1.,8.79694822162854E-14,-1.3364594413628E-14));
#18895=DIRECTION('',(8.74191357972136E-14,1.,3.36681878624147E-12));
#18896=DIRECTION('center_axis',(-8.74191357972136E-14,-1.,-3.36681878624147E-12));
#18897=DIRECTION('ref_axis',(-1.,8.79694822162854E-14,-1.3364594413628E-14));
#18898=DIRECTION('',(8.74191357972136E-14,1.,3.36681878624147E-12));
#18899=DIRECTION('center_axis',(-8.74191357972136E-14,-1.,-3.36681878624147E-12));
#18900=DIRECTION('ref_axis',(-1.,8.79694822162854E-14,-1.3364594413628E-14));
#18901=DIRECTION('',(8.74191357972136E-14,1.,3.36681878624147E-12));
#18902=DIRECTION('center_axis',(-8.74191357972136E-14,-1.,-3.36681878624147E-12));
#18903=DIRECTION('ref_axis',(-1.,8.79694822162854E-14,-1.3364594413628E-14));
#18904=DIRECTION('',(8.74191357972136E-14,1.,3.36681878624147E-12));
#18905=DIRECTION('center_axis',(-8.74191357972136E-14,-1.,-3.36681878624147E-12));
#18906=DIRECTION('ref_axis',(-1.,8.79694822162854E-14,-1.3364594413628E-14));
#18907=DIRECTION('',(8.74191357972136E-14,1.,3.36681878624147E-12));
#18908=DIRECTION('center_axis',(-8.74191357972136E-14,-1.,-3.36681878624147E-12));
#18909=DIRECTION('ref_axis',(-1.,8.79694822162854E-14,-1.3364594413628E-14));
#18910=DIRECTION('',(8.74191357972136E-14,1.,3.36681878624147E-12));
#18911=DIRECTION('center_axis',(-8.74191357972136E-14,-1.,-3.36681878624147E-12));
#18912=DIRECTION('ref_axis',(-1.,8.79694822162854E-14,-1.3364594413628E-14));
#18913=DIRECTION('',(8.74191357972136E-14,1.,3.36681878624147E-12));
#18914=DIRECTION('center_axis',(0.,1.,0.));
#18915=DIRECTION('ref_axis',(1.16649072924818E-39,0.,1.));
#18916=DIRECTION('',(0.,-1.,0.));
#18917=DIRECTION('',(0.,-1.,0.));
#18918=DIRECTION('',(0.,1.,0.));
#18919=DIRECTION('center_axis',(0.,1.,0.));
#18920=DIRECTION('ref_axis',(1.16649072924818E-39,0.,1.));
#18921=DIRECTION('',(0.,-1.,0.));
#18922=DIRECTION('center_axis',(0.,1.,0.));
#18923=DIRECTION('ref_axis',(1.16649072924818E-39,0.,1.));
#18924=DIRECTION('',(0.,-1.,0.));
#18925=DIRECTION('center_axis',(0.,1.,0.));
#18926=DIRECTION('ref_axis',(1.16649072924818E-39,0.,1.));
#18927=DIRECTION('',(0.,-1.,0.));
#18928=DIRECTION('center_axis',(0.,1.,0.));
#18929=DIRECTION('ref_axis',(1.16649072924818E-39,0.,1.));
#18930=DIRECTION('',(0.,-1.,0.));
#18931=DIRECTION('center_axis',(0.,1.,0.));
#18932=DIRECTION('ref_axis',(1.16649072924818E-39,0.,1.));
#18933=DIRECTION('',(0.,-1.,0.));
#18934=DIRECTION('center_axis',(0.,1.,0.));
#18935=DIRECTION('ref_axis',(1.16649072924818E-39,0.,1.));
#18936=DIRECTION('',(0.,-1.,0.));
#18937=DIRECTION('center_axis',(0.,1.,0.));
#18938=DIRECTION('ref_axis',(1.16649072924818E-39,0.,1.));
#18939=DIRECTION('',(0.,-1.,0.));
#18940=DIRECTION('center_axis',(0.,1.,0.));
#18941=DIRECTION('ref_axis',(1.16649072924818E-39,0.,1.));
#18942=DIRECTION('',(0.,-1.,0.));
#18943=DIRECTION('center_axis',(0.,1.,0.));
#18944=DIRECTION('ref_axis',(1.16649072924818E-39,0.,1.));
#18945=DIRECTION('',(0.,-1.,0.));
#18946=DIRECTION('center_axis',(0.,1.,0.));
#18947=DIRECTION('ref_axis',(1.16649072924818E-39,0.,1.));
#18948=DIRECTION('',(0.,-1.,0.));
#18949=DIRECTION('center_axis',(0.,1.,0.));
#18950=DIRECTION('ref_axis',(1.16649072924818E-39,0.,1.));
#18951=DIRECTION('',(0.,-1.,0.));
#18952=DIRECTION('center_axis',(0.,1.,0.));
#18953=DIRECTION('ref_axis',(1.16649072924818E-39,0.,1.));
#18954=DIRECTION('',(0.,-1.,0.));
#18955=DIRECTION('center_axis',(0.,1.,0.));
#18956=DIRECTION('ref_axis',(1.16649072924818E-39,0.,1.));
#18957=DIRECTION('',(0.,-1.,0.));
#18958=DIRECTION('center_axis',(0.,1.,0.));
#18959=DIRECTION('ref_axis',(1.16649072924818E-39,0.,1.));
#18960=DIRECTION('',(0.,-1.,0.));
#18961=DIRECTION('center_axis',(0.,1.,0.));
#18962=DIRECTION('ref_axis',(1.16649072924818E-39,0.,1.));
#18963=DIRECTION('',(0.,-1.,0.));
#18964=DIRECTION('center_axis',(0.,1.,0.));
#18965=DIRECTION('ref_axis',(1.16649072924818E-39,0.,1.));
#18966=DIRECTION('',(0.,-1.,0.));
#18967=DIRECTION('center_axis',(0.,1.,0.));
#18968=DIRECTION('ref_axis',(1.16649072924818E-39,0.,1.));
#18969=DIRECTION('',(0.,-1.,0.));
#18970=DIRECTION('center_axis',(0.,1.,0.));
#18971=DIRECTION('ref_axis',(1.16649072924818E-39,0.,1.));
#18972=DIRECTION('',(0.,-1.,0.));
#18973=DIRECTION('center_axis',(0.,1.,0.));
#18974=DIRECTION('ref_axis',(1.16649072924818E-39,0.,1.));
#18975=DIRECTION('',(0.,-1.,0.));
#18976=DIRECTION('center_axis',(0.,1.,0.));
#18977=DIRECTION('ref_axis',(1.16649072924818E-39,0.,1.));
#18978=DIRECTION('',(0.,-1.,0.));
#18979=DIRECTION('center_axis',(0.,-1.,0.));
#18980=DIRECTION('ref_axis',(1.16649072924818E-39,0.,1.));
#18981=DIRECTION('center_axis',(1.16649072924818E-39,0.,1.));
#18982=DIRECTION('ref_axis',(4.24488671257339E-14,-1.,0.));
#18983=DIRECTION('center_axis',(-1.16649072924818E-39,0.,-1.));
#18984=DIRECTION('ref_axis',(1.,-1.77635683940025E-15,-1.16649072924818E-39));
#18985=DIRECTION('center_axis',(0.910978406333114,-0.41245404979801,8.88703851014501E-13));
#18986=DIRECTION('ref_axis',(0.41245404979801,0.910978406333114,5.10955463663556E-29));
#18987=DIRECTION('center_axis',(1.16649072924818E-39,0.,1.));
#18988=DIRECTION('ref_axis',(1.,0.,-1.16649072924818E-39));
#18989=DIRECTION('center_axis',(0.910978406332847,0.4124540497986,2.48846969464753E-17));
#18990=DIRECTION('ref_axis',(-0.4124540497986,0.910978406332847,6.09192071292252E-33));
#18991=DIRECTION('center_axis',(1.16649072924818E-39,0.,1.));
#18992=DIRECTION('ref_axis',(-3.12699417093765E-14,-1.,0.));
#18993=DIRECTION('center_axis',(-1.16649072924818E-39,0.,-1.));
#18994=DIRECTION('ref_axis',(1.,1.77635683940025E-15,-1.16649072924818E-39));
#18995=DIRECTION('center_axis',(0.910978406332846,-0.412454049798602,0.));
#18996=DIRECTION('ref_axis',(0.412454049798602,0.910978406332846,0.));
#18997=DIRECTION('center_axis',(1.16649072924818E-39,0.,1.));
#18998=DIRECTION('ref_axis',(1.,0.,-1.16649072924818E-39));
#18999=DIRECTION('center_axis',(0.91097840633287,0.41245404979855,-2.46519032881566E-32));
#19000=DIRECTION('ref_axis',(-0.41245404979855,0.91097840633287,3.95416291609754E-48));
#19001=DIRECTION('center_axis',(1.16649072924818E-39,0.,1.));
#19002=DIRECTION('ref_axis',(1.,0.,-1.16649072924818E-39));
#19003=DIRECTION('center_axis',(1.16649072924818E-39,0.,1.));
#19004=DIRECTION('ref_axis',(1.,0.,-1.16649072924818E-39));
#19005=DIRECTION('',(1.16649072924818E-39,0.,1.));
#19006=DIRECTION('center_axis',(1.16649072924818E-39,0.,1.));
#19007=DIRECTION('ref_axis',(1.,0.,-1.16649072924818E-39));
#19008=DIRECTION('center_axis',(1.16649072924818E-39,0.,1.));
#19009=DIRECTION('ref_axis',(1.22508008559297E-14,-1.,-1.43194181381079E-53));
#19010=DIRECTION('center_axis',(0.,-1.,0.));
#19011=DIRECTION('ref_axis',(-1.16649072924818E-39,0.,-1.));
#19012=DIRECTION('center_axis',(0.,-1.,0.));
#19013=DIRECTION('ref_axis',(1.16649072924818E-39,0.,1.));
#19014=DIRECTION('',(8.65956056235491E-17,0.707106781186549,-0.707106781186546));
#19015=DIRECTION('center_axis',(0.,1.,0.));
#19016=DIRECTION('ref_axis',(1.16649072924818E-39,0.,1.));
#19017=DIRECTION('center_axis',(0.,1.,0.));
#19018=DIRECTION('ref_axis',(1.16649072924818E-39,0.,1.));
#19019=DIRECTION('center_axis',(-4.10522660630389E-39,0.,1.));
#19020=DIRECTION('ref_axis',(1.,0.,4.10522660630389E-39));
#19021=DIRECTION('center_axis',(-4.10522660630389E-39,0.,1.));
#19022=DIRECTION('ref_axis',(1.,0.,4.10522660630389E-39));
#19023=DIRECTION('center_axis',(0.,1.,0.));
#19024=DIRECTION('ref_axis',(1.16649072924818E-39,0.,1.));
#19025=DIRECTION('center_axis',(0.82190098044174,-4.46990853844586E-7,-0.569630387487103));
#19026=DIRECTION('ref_axis',(-0.56963038748716,-1.73470922087194E-18,-0.821900980441822));
#19027=DIRECTION('',(-0.493314502157547,-0.500000206354386,-0.711786903227801));
#19028=DIRECTION('',(0.49331421807717,-0.499999953061901,0.711787278040994));
#19029=DIRECTION('',(-3.67380332447989E-7,-0.9999999999999,2.54622298822739E-7));
#19030=DIRECTION('center_axis',(-8.74191357972136E-14,-1.,-3.36681878624147E-12));
#19031=DIRECTION('ref_axis',(-1.,8.79694822162854E-14,-1.3364594413628E-14));
#19032=DIRECTION('center_axis',(0.819989320180851,0.222433203783064,-0.527390732421558));
#19033=DIRECTION('ref_axis',(0.540942459779129,-2.5942501678163E-15,0.841059602649007));
#19034=DIRECTION('center_axis',(-0.81998932018085,-0.222433203783066,-0.527390732421559));
#19035=DIRECTION('ref_axis',(-0.540942459779129,3.37126789014689E-16,0.841059602649007));
#19036=DIRECTION('center_axis',(-0.81998932018085,0.222433203783066,0.527390732421559));
#19037=DIRECTION('ref_axis',(-0.54094245977913,-2.61757894185044E-15,-0.841059602649006));
#19038=DIRECTION('center_axis',(0.81998932018085,-0.222433203783066,0.527390732421559));
#19039=DIRECTION('ref_axis',(0.540942459779129,3.89141485738082E-16,-0.841059602649007));
#19040=DIRECTION('center_axis',(0.657353107750377,-0.75358270397543,2.46519032881566E-32));
#19041=DIRECTION('ref_axis',(0.75358270397543,0.657353107750377,-7.87577085156886E-48));
#19042=DIRECTION('center_axis',(0.657353107750364,0.753582703975442,0.));
#19043=DIRECTION('ref_axis',(-0.753582703975442,0.657353107750364,0.));
#19044=DIRECTION('center_axis',(0.657353107750348,-0.753582703975456,2.25915523143719E-14));
#19045=DIRECTION('ref_axis',(0.753582703975456,0.657353107750348,-8.1055088485032E-31));
#19046=DIRECTION('center_axis',(0.657353107749659,0.753582703976057,-1.03785565759232E-12));
#19047=DIRECTION('ref_axis',(-0.753582703976057,0.657353107749659,8.77882633459361E-29));
#23070=CARTESIAN_POINT('',(0.,0.,0.));
#23071=CARTESIAN_POINT('Origin',(-2.53888687851145E-9,74.888750003468,-7.9374999999999));
#23072=CARTESIAN_POINT('',(6.5626846775001,73.3012500034686,-7.93750000000257));
#23073=CARTESIAN_POINT('',(6.5626846775001,73.9362500034686,-7.9375000000015));
#23074=CARTESIAN_POINT('',(6.56268467242224,74.8887500034674,-7.93749999999981));
#23075=CARTESIAN_POINT('',(-5.80913668152327,74.3748153225002,-10.9908197002073));
#23076=CARTESIAN_POINT('Ctrl Pts',(-5.80913668152327,74.3748153225002,-10.9908197002073));
#23077=CARTESIAN_POINT('Ctrl Pts',(-5.58830892045767,74.3455189140323,-11.4109586876241));
#23078=CARTESIAN_POINT('Ctrl Pts',(-5.30932343282159,74.3172500034687,-11.7949492688802));
#23079=CARTESIAN_POINT('Ctrl Pts',(-4.05596218814306,74.1902500034686,-13.5200530258749));
#23080=CARTESIAN_POINT('Ctrl Pts',(-2.02798109407148,74.0632500034687,-14.1789840269267));
#23081=CARTESIAN_POINT('Ctrl Pts',(1.1673575708729E-13,73.9362500034686,
-14.8379150279786));
#23082=CARTESIAN_POINT('Ctrl Pts',(2.0279810940716,73.8092500034687,-14.1789840269267));
#23083=CARTESIAN_POINT('Ctrl Pts',(4.05596218814324,73.6822500034687,-13.5200530258749));
#23084=CARTESIAN_POINT('Ctrl Pts',(5.30932343282159,73.5552500034686,-11.7949492688802));
#23085=CARTESIAN_POINT('Ctrl Pts',(6.56268467750003,73.4282500034686,-10.0698455118856));
#23086=CARTESIAN_POINT('Ctrl Pts',(6.5626846775001,73.3012500034686,-7.93749999999999));
#23087=CARTESIAN_POINT('',(3.07575458830291,74.3748153227072,-13.7347893553626));
#23088=CARTESIAN_POINT('Origin',(2.12052597703405E-13,74.3748153225018,
-7.93750000000196));
#23089=CARTESIAN_POINT('Ctrl Pts',(3.07575458898229,74.3748153225002,-13.7347893566431));
#23090=CARTESIAN_POINT('Ctrl Pts',(4.41692449403691,74.2806745843362,-13.0232310340711));
#23091=CARTESIAN_POINT('Ctrl Pts',(5.30932343282159,74.1902500034686,-11.7949492688802));
#23092=CARTESIAN_POINT('Ctrl Pts',(6.56268467750008,74.0632500034686,-10.0698455118856));
#23093=CARTESIAN_POINT('Ctrl Pts',(6.5626846775001,73.9362500034686,-7.93749999999999));
#23094=CARTESIAN_POINT('Origin',(-2.53888687851145E-9,74.888750003468,-7.9374999999999));
#23095=CARTESIAN_POINT('',(6.56268467749999,70.7612500034687,-7.93750000000685));
#23096=CARTESIAN_POINT('',(6.5626846775001,71.3962500034686,-7.93750000000578));
#23097=CARTESIAN_POINT('',(6.56268467242224,74.8887500034674,-7.93749999999981));
#23098=CARTESIAN_POINT('Ctrl Pts',(6.5626846775001,73.3012500034686,-7.93749999999999));
#23099=CARTESIAN_POINT('Ctrl Pts',(6.56268467750003,73.1742500034686,-5.80515448811441));
#23100=CARTESIAN_POINT('Ctrl Pts',(5.30932343282164,73.0472500034686,-4.08005073111967));
#23101=CARTESIAN_POINT('Ctrl Pts',(4.05596218814318,72.9202500034686,-2.35494697412514));
#23102=CARTESIAN_POINT('Ctrl Pts',(2.02798109407154,72.7932500034686,-1.69601597307328));
#23103=CARTESIAN_POINT('Ctrl Pts',(1.1673575708729E-13,72.6662500034686,
-1.0370849720215));
#23104=CARTESIAN_POINT('Ctrl Pts',(-2.02798109407165,72.5392500034687,-1.69601597307328));
#23105=CARTESIAN_POINT('Ctrl Pts',(-4.05596218814312,72.4122500034686,-2.35494697412514));
#23106=CARTESIAN_POINT('Ctrl Pts',(-5.30932343282153,72.2852500034685,-4.08005073111967));
#23107=CARTESIAN_POINT('Ctrl Pts',(-6.56268467750008,72.1582500034687,-5.80515448811441));
#23108=CARTESIAN_POINT('Ctrl Pts',(-6.56268467750004,72.0312500034686,-7.93749999999999));
#23109=CARTESIAN_POINT('Ctrl Pts',(-6.56268467750003,71.9042500034686,-10.0698455118856));
#23110=CARTESIAN_POINT('Ctrl Pts',(-5.30932343282159,71.7772500034686,-11.7949492688802));
#23111=CARTESIAN_POINT('Ctrl Pts',(-4.05596218814318,71.6502500034686,-13.5200530258749));
#23112=CARTESIAN_POINT('Ctrl Pts',(-2.0279810940716,71.5232500034686,-14.1789840269267));
#23113=CARTESIAN_POINT('Ctrl Pts',(0.,71.3962500034686,-14.8379150279786));
#23114=CARTESIAN_POINT('Ctrl Pts',(2.02798109407165,71.2692500034687,-14.1789840269267));
#23115=CARTESIAN_POINT('Ctrl Pts',(4.05596218814312,71.1422500034685,-13.5200530258749));
#23116=CARTESIAN_POINT('Ctrl Pts',(5.30932343282159,71.0152500034686,-11.7949492688802));
#23117=CARTESIAN_POINT('Ctrl Pts',(6.56268467750003,70.8882500034686,-10.0698455118856));
#23118=CARTESIAN_POINT('Ctrl Pts',(6.56268467749999,70.7612500034687,-7.93749999999999));
#23119=CARTESIAN_POINT('Ctrl Pts',(6.5626846775001,73.9362500034686,-7.93749999999999));
#23120=CARTESIAN_POINT('Ctrl Pts',(6.56268467749991,73.8092500034686,-5.80515448811441));
#23121=CARTESIAN_POINT('Ctrl Pts',(5.30932343282159,73.6822500034686,-4.08005073111967));
#23122=CARTESIAN_POINT('Ctrl Pts',(4.05596218814324,73.5552500034685,-2.35494697412514));
#23123=CARTESIAN_POINT('Ctrl Pts',(2.02798109407165,73.4282500034686,-1.69601597307328));
#23124=CARTESIAN_POINT('Ctrl Pts',(0.,73.3012500034685,-1.0370849720215));
#23125=CARTESIAN_POINT('Ctrl Pts',(-2.02798109407154,73.1742500034685,-1.69601597307328));
#23126=CARTESIAN_POINT('Ctrl Pts',(-4.05596218814312,73.0472500034687,-2.35494697412514));
#23127=CARTESIAN_POINT('Ctrl Pts',(-5.30932343282159,72.9202500034686,-4.08005073111967));
#23128=CARTESIAN_POINT('Ctrl Pts',(-6.56268467750003,72.7932500034685,-5.80515448811441));
#23129=CARTESIAN_POINT('Ctrl Pts',(-6.56268467749993,72.6662500034687,-7.93749999999999));
#23130=CARTESIAN_POINT('Ctrl Pts',(-6.56268467749997,72.5392500034685,-10.0698455118856));
#23131=CARTESIAN_POINT('Ctrl Pts',(-5.30932343282159,72.4122500034687,-11.7949492688802));
#23132=CARTESIAN_POINT('Ctrl Pts',(-4.05596218814312,72.2852500034686,-13.5200530258749));
#23133=CARTESIAN_POINT('Ctrl Pts',(-2.0279810940716,72.1582500034688,-14.1789840269267));
#23134=CARTESIAN_POINT('Ctrl Pts',(0.,72.0312500034686,-14.8379150279786));
#23135=CARTESIAN_POINT('Ctrl Pts',(2.02798109407154,71.9042500034687,-14.1789840269267));
#23136=CARTESIAN_POINT('Ctrl Pts',(4.05596218814318,71.7772500034686,-13.5200530258749));
#23137=CARTESIAN_POINT('Ctrl Pts',(5.30932343282159,71.6502500034686,-11.7949492688802));
#23138=CARTESIAN_POINT('Ctrl Pts',(6.56268467750003,71.5232500034685,-10.0698455118856));
#23139=CARTESIAN_POINT('Ctrl Pts',(6.5626846775001,71.3962500034686,-7.93749999999999));
#23140=CARTESIAN_POINT('Origin',(-2.53888687851145E-9,74.888750003468,-7.9374999999999));
#23141=CARTESIAN_POINT('',(6.56268467749999,68.2212500034686,-7.93750000001112));
#23142=CARTESIAN_POINT('',(6.56268467749999,68.8562500034686,-7.93750000001005));
#23143=CARTESIAN_POINT('',(6.56268467242224,74.8887500034674,-7.93749999999981));
#23144=CARTESIAN_POINT('Ctrl Pts',(6.56268467749999,70.7612500034687,-7.93749999999999));
#23145=CARTESIAN_POINT('Ctrl Pts',(6.56268467750003,70.6342500034686,-5.80515448811441));
#23146=CARTESIAN_POINT('Ctrl Pts',(5.30932343282164,70.5072500034686,-4.08005073111967));
#23147=CARTESIAN_POINT('Ctrl Pts',(4.05596218814324,70.3802500034686,-2.35494697412514));
#23148=CARTESIAN_POINT('Ctrl Pts',(2.0279810940716,70.2532500034686,-1.69601597307328));
#23149=CARTESIAN_POINT('Ctrl Pts',(0.,70.1262500034686,-1.0370849720215));
#23150=CARTESIAN_POINT('Ctrl Pts',(-2.0279810940716,69.9992500034686,-1.69601597307328));
#23151=CARTESIAN_POINT('Ctrl Pts',(-4.05596218814312,69.8722500034686,-2.35494697412514));
#23152=CARTESIAN_POINT('Ctrl Pts',(-5.30932343282159,69.7452500034687,-4.08005073111967));
#23153=CARTESIAN_POINT('Ctrl Pts',(-6.56268467749997,69.6182500034686,-5.80515448811441));
#23154=CARTESIAN_POINT('Ctrl Pts',(-6.56268467749999,69.4912500034686,-7.93749999999999));
#23155=CARTESIAN_POINT('Ctrl Pts',(-6.56268467749997,69.3642500034686,-10.0698455118856));
#23156=CARTESIAN_POINT('Ctrl Pts',(-5.30932343282153,69.2372500034686,-11.7949492688802));
#23157=CARTESIAN_POINT('Ctrl Pts',(-4.05596218814312,69.1102500034686,-13.5200530258749));
#23158=CARTESIAN_POINT('Ctrl Pts',(-2.02798109407154,68.9832500034687,-14.1789840269267));
#23159=CARTESIAN_POINT('Ctrl Pts',(0.,68.8562500034685,-14.8379150279786));
#23160=CARTESIAN_POINT('Ctrl Pts',(2.02798109407165,68.7292500034686,-14.1789840269267));
#23161=CARTESIAN_POINT('Ctrl Pts',(4.05596218814312,68.6022500034686,-13.5200530258749));
#23162=CARTESIAN_POINT('Ctrl Pts',(5.30932343282164,68.4752500034687,-11.7949492688802));
#23163=CARTESIAN_POINT('Ctrl Pts',(6.56268467749997,68.3482500034685,-10.0698455118856));
#23164=CARTESIAN_POINT('Ctrl Pts',(6.56268467749999,68.2212500034686,-7.93749999999999));
#23165=CARTESIAN_POINT('Ctrl Pts',(6.5626846775001,71.3962500034686,-7.93749999999999));
#23166=CARTESIAN_POINT('Ctrl Pts',(6.56268467750008,71.2692500034686,-5.80515448811441));
#23167=CARTESIAN_POINT('Ctrl Pts',(5.30932343282153,71.1422500034686,-4.08005073111967));
#23168=CARTESIAN_POINT('Ctrl Pts',(4.05596218814312,71.0152500034686,-2.35494697412514));
#23169=CARTESIAN_POINT('Ctrl Pts',(2.0279810940716,70.8882500034687,-1.69601597307328));
#23170=CARTESIAN_POINT('Ctrl Pts',(0.,70.7612500034686,-1.0370849720215));
#23171=CARTESIAN_POINT('Ctrl Pts',(-2.02798109407148,70.6342500034686,-1.69601597307328));
#23172=CARTESIAN_POINT('Ctrl Pts',(-4.05596218814318,70.5072500034686,-2.35494697412514));
#23173=CARTESIAN_POINT('Ctrl Pts',(-5.30932343282159,70.3802500034686,-4.08005073111967));
#23174=CARTESIAN_POINT('Ctrl Pts',(-6.56268467750003,70.2532500034686,-5.80515448811441));
#23175=CARTESIAN_POINT('Ctrl Pts',(-6.56268467749999,70.1262500034686,-7.93749999999999));
#23176=CARTESIAN_POINT('Ctrl Pts',(-6.56268467750003,69.9992500034686,-10.0698455118856));
#23177=CARTESIAN_POINT('Ctrl Pts',(-5.30932343282153,69.8722500034687,-11.7949492688802));
#23178=CARTESIAN_POINT('Ctrl Pts',(-4.05596218814324,69.7452500034685,-13.5200530258749));
#23179=CARTESIAN_POINT('Ctrl Pts',(-2.02798109407154,69.6182500034687,-14.1789840269267));
#23180=CARTESIAN_POINT('Ctrl Pts',(-5.83678785436452E-14,69.4912500034686,
-14.8379150279786));
#23181=CARTESIAN_POINT('Ctrl Pts',(2.02798109407154,69.3642500034687,-14.1789840269267));
#23182=CARTESIAN_POINT('Ctrl Pts',(4.05596218814318,69.2372500034687,-13.5200530258749));
#23183=CARTESIAN_POINT('Ctrl Pts',(5.30932343282164,69.1102500034686,-11.7949492688802));
#23184=CARTESIAN_POINT('Ctrl Pts',(6.56268467750003,68.9832500034685,-10.0698455118856));
#23185=CARTESIAN_POINT('Ctrl Pts',(6.56268467749999,68.8562500034686,-7.93749999999999));
#23186=CARTESIAN_POINT('Origin',(-2.53888687851145E-9,74.888750003468,-7.9374999999999));
#23187=CARTESIAN_POINT('',(6.56268467749999,65.6812500034686,-7.9375000000154));
#23188=CARTESIAN_POINT('',(6.56268467749999,66.3162500034687,-7.93750000001433));
#23189=CARTESIAN_POINT('',(6.56268467242224,74.8887500034674,-7.93749999999981));
#23190=CARTESIAN_POINT('Ctrl Pts',(6.56268467749999,68.2212500034686,-7.93749999999999));
#23191=CARTESIAN_POINT('Ctrl Pts',(6.56268467750003,68.0942500034685,-5.80515448811441));
#23192=CARTESIAN_POINT('Ctrl Pts',(5.3093234328217,67.9672500034686,-4.08005073111967));
#23193=CARTESIAN_POINT('Ctrl Pts',(4.05596218814312,67.8402500034685,-2.35494697412514));
#23194=CARTESIAN_POINT('Ctrl Pts',(2.0279810940716,67.7132500034686,-1.69601597307328));
#23195=CARTESIAN_POINT('Ctrl Pts',(1.1673575708729E-13,67.5862500034685,
-1.0370849720215));
#23196=CARTESIAN_POINT('Ctrl Pts',(-2.0279810940716,67.4592500034686,-1.69601597307328));
#23197=CARTESIAN_POINT('Ctrl Pts',(-4.05596218814312,67.3322500034685,-2.35494697412514));
#23198=CARTESIAN_POINT('Ctrl Pts',(-5.30932343282153,67.2052500034686,-4.08005073111967));
#23199=CARTESIAN_POINT('Ctrl Pts',(-6.56268467750003,67.0782500034685,-5.80515448811441));
#23200=CARTESIAN_POINT('Ctrl Pts',(-6.56268467749999,66.9512500034686,-7.93749999999999));
#23201=CARTESIAN_POINT('Ctrl Pts',(-6.56268467749997,66.8242500034685,-10.0698455118856));
#23202=CARTESIAN_POINT('Ctrl Pts',(-5.30932343282153,66.6972500034686,-11.7949492688802));
#23203=CARTESIAN_POINT('Ctrl Pts',(-4.05596218814312,66.5702500034686,-13.5200530258749));
#23204=CARTESIAN_POINT('Ctrl Pts',(-2.02798109407165,66.4432500034688,-14.1789840269267));
#23205=CARTESIAN_POINT('Ctrl Pts',(0.,66.3162500034685,-14.8379150279786));
#23206=CARTESIAN_POINT('Ctrl Pts',(2.02798109407154,66.1892500034688,-14.1789840269267));
#23207=CARTESIAN_POINT('Ctrl Pts',(4.05596218814312,66.0622500034686,-13.5200530258749));
#23208=CARTESIAN_POINT('Ctrl Pts',(5.30932343282164,65.9352500034686,-11.7949492688802));
#23209=CARTESIAN_POINT('Ctrl Pts',(6.56268467750008,65.8082500034686,-10.0698455118856));
#23210=CARTESIAN_POINT('Ctrl Pts',(6.56268467749999,65.6812500034686,-7.93749999999999));
#23211=CARTESIAN_POINT('Ctrl Pts',(6.56268467749999,68.8562500034686,-7.93749999999999));
#23212=CARTESIAN_POINT('Ctrl Pts',(6.56268467750003,68.7292500034685,-5.80515448811441));
#23213=CARTESIAN_POINT('Ctrl Pts',(5.30932343282159,68.6022500034686,-4.08005073111967));
#23214=CARTESIAN_POINT('Ctrl Pts',(4.05596218814318,68.4752500034685,-2.35494697412514));
#23215=CARTESIAN_POINT('Ctrl Pts',(2.0279810940716,68.3482500034686,-1.69601597307328));
#23216=CARTESIAN_POINT('Ctrl Pts',(-1.1673575708729E-13,68.2212500034685,
-1.0370849720215));
#23217=CARTESIAN_POINT('Ctrl Pts',(-2.02798109407154,68.0942500034687,-1.69601597307328));
#23218=CARTESIAN_POINT('Ctrl Pts',(-4.05596218814306,67.9672500034686,-2.35494697412514));
#23219=CARTESIAN_POINT('Ctrl Pts',(-5.30932343282159,67.8402500034686,-4.08005073111967));
#23220=CARTESIAN_POINT('Ctrl Pts',(-6.56268467749997,67.7132500034685,-5.80515448811441));
#23221=CARTESIAN_POINT('Ctrl Pts',(-6.56268467749999,67.5862500034686,-7.93749999999999));
#23222=CARTESIAN_POINT('Ctrl Pts',(-6.56268467749991,67.4592500034685,-10.0698455118856));
#23223=CARTESIAN_POINT('Ctrl Pts',(-5.30932343282153,67.3322500034686,-11.7949492688802));
#23224=CARTESIAN_POINT('Ctrl Pts',(-4.05596218814312,67.2052500034686,-13.5200530258749));
#23225=CARTESIAN_POINT('Ctrl Pts',(-2.02798109407154,67.0782500034687,-14.1789840269267));
#23226=CARTESIAN_POINT('Ctrl Pts',(0.,66.9512500034685,-14.8379150279786));
#23227=CARTESIAN_POINT('Ctrl Pts',(2.02798109407154,66.8242500034687,-14.1789840269267));
#23228=CARTESIAN_POINT('Ctrl Pts',(4.05596218814318,66.6972500034686,-13.5200530258749));
#23229=CARTESIAN_POINT('Ctrl Pts',(5.30932343282153,66.5702500034686,-11.7949492688802));
#23230=CARTESIAN_POINT('Ctrl Pts',(6.56268467750003,66.4432500034685,-10.0698455118856));
#23231=CARTESIAN_POINT('Ctrl Pts',(6.56268467749999,66.3162500034687,-7.93749999999999));
#23232=CARTESIAN_POINT('Origin',(-2.53888687851145E-9,74.888750003468,-7.9374999999999));
#23233=CARTESIAN_POINT('',(6.56268467750004,63.1412500034686,-7.93750000001967));
#23234=CARTESIAN_POINT('',(6.56268467749999,63.7762500034686,-7.9375000000186));
#23235=CARTESIAN_POINT('',(6.56268467242224,74.8887500034674,-7.93749999999981));
#23236=CARTESIAN_POINT('Ctrl Pts',(6.56268467749999,65.6812500034686,-7.93749999999999));
#23237=CARTESIAN_POINT('Ctrl Pts',(6.56268467749991,65.5542500034687,-5.80515448811441));
#23238=CARTESIAN_POINT('Ctrl Pts',(5.3093234328217,65.4272500034686,-4.08005073111967));
#23239=CARTESIAN_POINT('Ctrl Pts',(4.05596218814324,65.3002500034687,-2.35494697412514));
#23240=CARTESIAN_POINT('Ctrl Pts',(2.0279810940716,65.1732500034686,-1.69601597307328));
#23241=CARTESIAN_POINT('Ctrl Pts',(0.,65.0462500034686,-1.0370849720215));
#23242=CARTESIAN_POINT('Ctrl Pts',(-2.0279810940716,64.9192500034686,-1.69601597307328));
#23243=CARTESIAN_POINT('Ctrl Pts',(-4.05596218814312,64.7922500034686,-2.35494697412514));
#23244=CARTESIAN_POINT('Ctrl Pts',(-5.30932343282153,64.6652500034686,-4.08005073111967));
#23245=CARTESIAN_POINT('Ctrl Pts',(-6.56268467750003,64.5382500034686,-5.80515448811441));
#23246=CARTESIAN_POINT('Ctrl Pts',(-6.56268467749999,64.4112500034687,-7.93749999999999));
#23247=CARTESIAN_POINT('Ctrl Pts',(-6.56268467749997,64.2842500034685,-10.0698455118856));
#23248=CARTESIAN_POINT('Ctrl Pts',(-5.30932343282148,64.1572500034686,-11.7949492688802));
#23249=CARTESIAN_POINT('Ctrl Pts',(-4.05596218814312,64.0302500034686,-13.5200530258749));
#23250=CARTESIAN_POINT('Ctrl Pts',(-2.02798109407165,63.9032500034688,-14.1789840269267));
#23251=CARTESIAN_POINT('Ctrl Pts',(0.,63.7762500034686,-14.8379150279786));
#23252=CARTESIAN_POINT('Ctrl Pts',(2.0279810940716,63.6492500034688,-14.1789840269267));
#23253=CARTESIAN_POINT('Ctrl Pts',(4.05596218814312,63.5222500034685,-13.5200530258749));
#23254=CARTESIAN_POINT('Ctrl Pts',(5.3093234328217,63.3952500034686,-11.7949492688802));
#23255=CARTESIAN_POINT('Ctrl Pts',(6.56268467749997,63.2682500034685,-10.0698455118856));
#23256=CARTESIAN_POINT('Ctrl Pts',(6.56268467750004,63.1412500034686,-7.93749999999999));
#23257=CARTESIAN_POINT('Ctrl Pts',(6.56268467749999,66.3162500034687,-7.93749999999999));
#23258=CARTESIAN_POINT('Ctrl Pts',(6.56268467749997,66.1892500034686,-5.80515448811441));
#23259=CARTESIAN_POINT('Ctrl Pts',(5.30932343282159,66.0622500034686,-4.08005073111967));
#23260=CARTESIAN_POINT('Ctrl Pts',(4.05596218814318,65.9352500034686,-2.35494697412514));
#23261=CARTESIAN_POINT('Ctrl Pts',(2.02798109407148,65.8082500034686,-1.69601597307328));
#23262=CARTESIAN_POINT('Ctrl Pts',(5.83678785436452E-14,65.6812500034686,
-1.0370849720215));
#23263=CARTESIAN_POINT('Ctrl Pts',(-2.0279810940716,65.5542500034686,-1.69601597307328));
#23264=CARTESIAN_POINT('Ctrl Pts',(-4.05596218814318,65.4272500034686,-2.35494697412514));
#23265=CARTESIAN_POINT('Ctrl Pts',(-5.30932343282153,65.3002500034686,-4.08005073111967));
#23266=CARTESIAN_POINT('Ctrl Pts',(-6.56268467749997,65.1732500034685,-5.80515448811441));
#23267=CARTESIAN_POINT('Ctrl Pts',(-6.56268467749999,65.0462500034685,-7.93749999999999));
#23268=CARTESIAN_POINT('Ctrl Pts',(-6.56268467750003,64.9192500034685,-10.0698455118856));
#23269=CARTESIAN_POINT('Ctrl Pts',(-5.30932343282159,64.7922500034686,-11.7949492688802));
#23270=CARTESIAN_POINT('Ctrl Pts',(-4.05596218814306,64.6652500034686,-13.5200530258749));
#23271=CARTESIAN_POINT('Ctrl Pts',(-2.02798109407154,64.5382500034687,-14.1789840269267));
#23272=CARTESIAN_POINT('Ctrl Pts',(1.1673575708729E-13,64.4112500034686,
-14.8379150279786));
#23273=CARTESIAN_POINT('Ctrl Pts',(2.0279810940716,64.2842500034687,-14.1789840269267));
#23274=CARTESIAN_POINT('Ctrl Pts',(4.05596218814324,64.1572500034685,-13.5200530258749));
#23275=CARTESIAN_POINT('Ctrl Pts',(5.30932343282159,64.0302500034686,-11.7949492688802));
#23276=CARTESIAN_POINT('Ctrl Pts',(6.56268467750003,63.9032500034685,-10.0698455118856));
#23277=CARTESIAN_POINT('Ctrl Pts',(6.56268467749999,63.7762500034686,-7.93749999999999));
#23278=CARTESIAN_POINT('Origin',(-2.53888687851145E-9,74.888750003468,-7.9374999999999));
#23279=CARTESIAN_POINT('',(6.5626846775001,60.6012500034686,-7.93750000002395));
#23280=CARTESIAN_POINT('',(6.56268467749993,61.2362500034686,-7.93750000002288));
#23281=CARTESIAN_POINT('',(6.56268467242224,74.8887500034674,-7.93749999999981));
#23282=CARTESIAN_POINT('Ctrl Pts',(6.56268467750004,63.1412500034686,-7.93749999999999));
#23283=CARTESIAN_POINT('Ctrl Pts',(6.56268467750003,63.0142500034686,-5.80515448811441));
#23284=CARTESIAN_POINT('Ctrl Pts',(5.30932343282164,62.8872500034686,-4.08005073111967));
#23285=CARTESIAN_POINT('Ctrl Pts',(4.05596218814312,62.7602500034686,-2.35494697412514));
#23286=CARTESIAN_POINT('Ctrl Pts',(2.02798109407165,62.6332500034686,-1.69601597307328));
#23287=CARTESIAN_POINT('Ctrl Pts',(0.,62.5062500034686,-1.0370849720215));
#23288=CARTESIAN_POINT('Ctrl Pts',(-2.02798109407154,62.3792500034686,-1.69601597307328));
#23289=CARTESIAN_POINT('Ctrl Pts',(-4.05596218814324,62.2522500034685,-2.35494697412514));
#23290=CARTESIAN_POINT('Ctrl Pts',(-5.30932343282148,62.1252500034686,-4.08005073111967));
#23291=CARTESIAN_POINT('Ctrl Pts',(-6.56268467750003,61.9982500034685,-5.80515448811441));
#23292=CARTESIAN_POINT('Ctrl Pts',(-6.5626846775001,61.8712500034687,-7.93749999999999));
#23293=CARTESIAN_POINT('Ctrl Pts',(-6.56268467750008,61.7442500034686,-10.0698455118856));
#23294=CARTESIAN_POINT('Ctrl Pts',(-5.30932343282148,61.6172500034687,-11.7949492688802));
#23295=CARTESIAN_POINT('Ctrl Pts',(-4.05596218814312,61.4902500034686,-13.5200530258749));
#23296=CARTESIAN_POINT('Ctrl Pts',(-2.0279810940716,61.3632500034687,-14.1789840269267));
#23297=CARTESIAN_POINT('Ctrl Pts',(0.,61.2362500034686,-14.8379150279786));
#23298=CARTESIAN_POINT('Ctrl Pts',(2.0279810940716,61.1092500034687,-14.1789840269267));
#23299=CARTESIAN_POINT('Ctrl Pts',(4.05596218814318,60.9822500034686,-13.5200530258749));
#23300=CARTESIAN_POINT('Ctrl Pts',(5.3093234328217,60.8552500034686,-11.7949492688802));
#23301=CARTESIAN_POINT('Ctrl Pts',(6.56268467750003,60.7282500034687,-10.0698455118856));
#23302=CARTESIAN_POINT('Ctrl Pts',(6.5626846775001,60.6012500034686,-7.93749999999999));
#23303=CARTESIAN_POINT('Ctrl Pts',(6.56268467749999,63.7762500034686,-7.93749999999999));
#23304=CARTESIAN_POINT('Ctrl Pts',(6.56268467750008,63.6492500034686,-5.80515448811441));
#23305=CARTESIAN_POINT('Ctrl Pts',(5.30932343282159,63.5222500034686,-4.08005073111967));
#23306=CARTESIAN_POINT('Ctrl Pts',(4.05596218814318,63.3952500034686,-2.35494697412514));
#23307=CARTESIAN_POINT('Ctrl Pts',(2.02798109407154,63.2682500034685,-1.69601597307328));
#23308=CARTESIAN_POINT('Ctrl Pts',(0.,63.1412500034685,-1.0370849720215));
#23309=CARTESIAN_POINT('Ctrl Pts',(-2.02798109407154,63.0142500034686,-1.69601597307328));
#23310=CARTESIAN_POINT('Ctrl Pts',(-4.05596218814318,62.8872500034686,-2.35494697412514));
#23311=CARTESIAN_POINT('Ctrl Pts',(-5.30932343282164,62.7602500034687,-4.08005073111967));
#23312=CARTESIAN_POINT('Ctrl Pts',(-6.56268467749997,62.6332500034685,-5.80515448811441));
#23313=CARTESIAN_POINT('Ctrl Pts',(-6.56268467749999,62.5062500034685,-7.93749999999999));
#23314=CARTESIAN_POINT('Ctrl Pts',(-6.56268467750003,62.3792500034687,-10.0698455118856));
#23315=CARTESIAN_POINT('Ctrl Pts',(-5.30932343282159,62.2522500034686,-11.7949492688802));
#23316=CARTESIAN_POINT('Ctrl Pts',(-4.05596218814318,62.1252500034685,-13.5200530258749));
#23317=CARTESIAN_POINT('Ctrl Pts',(-2.02798109407148,61.9982500034687,-14.1789840269267));
#23318=CARTESIAN_POINT('Ctrl Pts',(0.,61.8712500034686,-14.8379150279786));
#23319=CARTESIAN_POINT('Ctrl Pts',(2.0279810940716,61.7442500034687,-14.1789840269267));
#23320=CARTESIAN_POINT('Ctrl Pts',(4.05596218814312,61.6172500034686,-13.5200530258749));
#23321=CARTESIAN_POINT('Ctrl Pts',(5.30932343282159,61.4902500034686,-11.7949492688802));
#23322=CARTESIAN_POINT('Ctrl Pts',(6.56268467749991,61.3632500034686,-10.0698455118856));
#23323=CARTESIAN_POINT('Ctrl Pts',(6.56268467749993,61.2362500034686,-7.93749999999999));
#23324=CARTESIAN_POINT('Origin',(-2.53888687851145E-9,74.888750003468,-7.9374999999999));
#23325=CARTESIAN_POINT('',(6.5626846775001,58.0612500034686,-7.93750000002823));
#23326=CARTESIAN_POINT('',(6.56268467749999,58.6962500034686,-7.93750000002716));
#23327=CARTESIAN_POINT('',(6.56268467242224,74.8887500034674,-7.93749999999981));
#23328=CARTESIAN_POINT('Ctrl Pts',(6.5626846775001,60.6012500034686,-7.93749999999999));
#23329=CARTESIAN_POINT('Ctrl Pts',(6.56268467750008,60.4742500034686,-5.80515448811441));
#23330=CARTESIAN_POINT('Ctrl Pts',(5.30932343282159,60.3472500034687,-4.08005073111967));
#23331=CARTESIAN_POINT('Ctrl Pts',(4.05596218814312,60.2202500034686,-2.35494697412514));
#23332=CARTESIAN_POINT('Ctrl Pts',(2.02798109407165,60.0932500034686,-1.69601597307328));
#23333=CARTESIAN_POINT('Ctrl Pts',(0.,59.9662500034686,-1.0370849720215));
#23334=CARTESIAN_POINT('Ctrl Pts',(-2.02798109407165,59.8392500034686,-1.69601597307317));
#23335=CARTESIAN_POINT('Ctrl Pts',(-4.05596218814306,59.7122500034685,-2.35494697412514));
#23336=CARTESIAN_POINT('Ctrl Pts',(-5.30932343282148,59.5852500034686,-4.08005073111967));
#23337=CARTESIAN_POINT('Ctrl Pts',(-6.56268467750003,59.4582500034686,-5.80515448811441));
#23338=CARTESIAN_POINT('Ctrl Pts',(-6.56268467750004,59.3312500034686,-7.93749999999999));
#23339=CARTESIAN_POINT('Ctrl Pts',(-6.56268467749991,59.2042500034686,-10.0698455118856));
#23340=CARTESIAN_POINT('Ctrl Pts',(-5.30932343282148,59.0772500034686,-11.7949492688802));
#23341=CARTESIAN_POINT('Ctrl Pts',(-4.05596218814312,58.9502500034686,-13.5200530258749));
#23342=CARTESIAN_POINT('Ctrl Pts',(-2.0279810940716,58.8232500034687,-14.1789840269267));
#23343=CARTESIAN_POINT('Ctrl Pts',(0.,58.6962500034686,-14.8379150279786));
#23344=CARTESIAN_POINT('Ctrl Pts',(2.0279810940716,58.5692500034687,-14.1789840269267));
#23345=CARTESIAN_POINT('Ctrl Pts',(4.05596218814318,58.4422500034685,-13.5200530258749));
#23346=CARTESIAN_POINT('Ctrl Pts',(5.30932343282159,58.3152500034686,-11.7949492688802));
#23347=CARTESIAN_POINT('Ctrl Pts',(6.56268467750003,58.1882500034686,-10.0698455118856));
#23348=CARTESIAN_POINT('Ctrl Pts',(6.5626846775001,58.0612500034686,-7.93749999999999));
#23349=CARTESIAN_POINT('Ctrl Pts',(6.56268467749993,61.2362500034686,-7.93749999999999));
#23350=CARTESIAN_POINT('Ctrl Pts',(6.56268467750003,61.1092500034686,-5.80515448811441));
#23351=CARTESIAN_POINT('Ctrl Pts',(5.30932343282159,60.9822500034687,-4.08005073111967));
#23352=CARTESIAN_POINT('Ctrl Pts',(4.05596218814306,60.8552500034686,-2.35494697412514));
#23353=CARTESIAN_POINT('Ctrl Pts',(2.02798109407154,60.7282500034685,-1.69601597307328));
#23354=CARTESIAN_POINT('Ctrl Pts',(0.,60.6012500034686,-1.0370849720215));
#23355=CARTESIAN_POINT('Ctrl Pts',(-2.02798109407154,60.4742500034686,-1.69601597307317));
#23356=CARTESIAN_POINT('Ctrl Pts',(-4.05596218814312,60.3472500034685,-2.35494697412514));
#23357=CARTESIAN_POINT('Ctrl Pts',(-5.30932343282159,60.2202500034686,-4.08005073111967));
#23358=CARTESIAN_POINT('Ctrl Pts',(-6.56268467749997,60.0932500034686,-5.80515448811441));
#23359=CARTESIAN_POINT('Ctrl Pts',(-6.56268467749999,59.9662500034687,-7.93749999999999));
#23360=CARTESIAN_POINT('Ctrl Pts',(-6.56268467750003,59.8392500034686,-10.0698455118856));
#23361=CARTESIAN_POINT('Ctrl Pts',(-5.30932343282159,59.7122500034685,-11.7949492688802));
#23362=CARTESIAN_POINT('Ctrl Pts',(-4.05596218814306,59.5852500034686,-13.5200530258749));
#23363=CARTESIAN_POINT('Ctrl Pts',(-2.02798109407148,59.4582500034687,-14.1789840269267));
#23364=CARTESIAN_POINT('Ctrl Pts',(1.1673575708729E-13,59.3312500034686,
-14.8379150279786));
#23365=CARTESIAN_POINT('Ctrl Pts',(2.02798109407148,59.2042500034687,-14.1789840269267));
#23366=CARTESIAN_POINT('Ctrl Pts',(4.05596218814324,59.0772500034685,-13.5200530258749));
#23367=CARTESIAN_POINT('Ctrl Pts',(5.30932343282159,58.9502500034686,-11.7949492688802));
#23368=CARTESIAN_POINT('Ctrl Pts',(6.56268467750008,58.8232500034686,-10.0698455118856));
#23369=CARTESIAN_POINT('Ctrl Pts',(6.56268467749999,58.6962500034686,-7.93749999999999));
#23370=CARTESIAN_POINT('Origin',(-2.53888687851145E-9,74.888750003468,-7.9374999999999));
#23371=CARTESIAN_POINT('',(6.5626846775001,55.5212500034686,-7.9375000000325));
#23372=CARTESIAN_POINT('',(6.56268467749999,56.1562500034686,-7.93750000003143));
#23373=CARTESIAN_POINT('',(6.56268467242224,74.8887500034674,-7.93749999999981));
#23374=CARTESIAN_POINT('Ctrl Pts',(6.5626846775001,58.0612500034686,-7.93749999999999));
#23375=CARTESIAN_POINT('Ctrl Pts',(6.56268467749997,57.9342500034686,-5.80515448811441));
#23376=CARTESIAN_POINT('Ctrl Pts',(5.30932343282164,57.8072500034686,-4.08005073111967));
#23377=CARTESIAN_POINT('Ctrl Pts',(4.05596218814318,57.6802500034686,-2.35494697412514));
#23378=CARTESIAN_POINT('Ctrl Pts',(2.02798109407154,57.5532500034686,-1.69601597307317));
#23379=CARTESIAN_POINT('Ctrl Pts',(0.,57.4262500034686,-1.0370849720215));
#23380=CARTESIAN_POINT('Ctrl Pts',(-2.0279810940716,57.2992500034686,-1.69601597307317));
#23381=CARTESIAN_POINT('Ctrl Pts',(-4.05596218814318,57.1722500034686,-2.35494697412514));
#23382=CARTESIAN_POINT('Ctrl Pts',(-5.30932343282148,57.0452500034685,-4.08005073111967));
#23383=CARTESIAN_POINT('Ctrl Pts',(-6.56268467749997,56.9182500034686,-5.80515448811441));
#23384=CARTESIAN_POINT('Ctrl Pts',(-6.56268467750004,56.7912500034686,-7.93749999999999));
#23385=CARTESIAN_POINT('Ctrl Pts',(-6.56268467750003,56.6642500034685,-10.0698455118856));
#23386=CARTESIAN_POINT('Ctrl Pts',(-5.30932343282159,56.5372500034686,-11.7949492688802));
#23387=CARTESIAN_POINT('Ctrl Pts',(-4.05596218814312,56.4102500034685,-13.5200530258749));
#23388=CARTESIAN_POINT('Ctrl Pts',(-2.0279810940716,56.2832500034686,-14.1789840269267));
#23389=CARTESIAN_POINT('Ctrl Pts',(0.,56.1562500034686,-14.8379150279786));
#23390=CARTESIAN_POINT('Ctrl Pts',(2.02798109407165,56.0292500034687,-14.1789840269267));
#23391=CARTESIAN_POINT('Ctrl Pts',(4.05596218814318,55.9022500034686,-13.5200530258749));
#23392=CARTESIAN_POINT('Ctrl Pts',(5.30932343282148,55.7752500034686,-11.7949492688802));
#23393=CARTESIAN_POINT('Ctrl Pts',(6.56268467750003,55.6482500034686,-10.0698455118856));
#23394=CARTESIAN_POINT('Ctrl Pts',(6.5626846775001,55.5212500034686,-7.93749999999999));
#23395=CARTESIAN_POINT('Ctrl Pts',(6.56268467749999,58.6962500034686,-7.93749999999999));
#23396=CARTESIAN_POINT('Ctrl Pts',(6.56268467750003,58.5692500034686,-5.80515448811441));
#23397=CARTESIAN_POINT('Ctrl Pts',(5.30932343282159,58.4422500034686,-4.08005073111967));
#23398=CARTESIAN_POINT('Ctrl Pts',(4.05596218814312,58.3152500034686,-2.35494697412514));
#23399=CARTESIAN_POINT('Ctrl Pts',(2.02798109407154,58.1882500034687,-1.69601597307328));
#23400=CARTESIAN_POINT('Ctrl Pts',(5.83678785436452E-14,58.0612500034686,
-1.0370849720215));
#23401=CARTESIAN_POINT('Ctrl Pts',(-2.02798109407154,57.9342500034686,-1.69601597307317));
#23402=CARTESIAN_POINT('Ctrl Pts',(-4.05596218814312,57.8072500034686,-2.35494697412514));
#23403=CARTESIAN_POINT('Ctrl Pts',(-5.30932343282159,57.6802500034686,-4.08005073111967));
#23404=CARTESIAN_POINT('Ctrl Pts',(-6.56268467750003,57.5532500034687,-5.80515448811441));
#23405=CARTESIAN_POINT('Ctrl Pts',(-6.56268467749993,57.4262500034687,-7.93749999999999));
#23406=CARTESIAN_POINT('Ctrl Pts',(-6.56268467749997,57.2992500034685,-10.0698455118856));
#23407=CARTESIAN_POINT('Ctrl Pts',(-5.30932343282159,57.1722500034686,-11.7949492688802));
#23408=CARTESIAN_POINT('Ctrl Pts',(-4.05596218814312,57.0452500034685,-13.5200530258749));
#23409=CARTESIAN_POINT('Ctrl Pts',(-2.0279810940716,56.9182500034687,-14.1789840269267));
#23410=CARTESIAN_POINT('Ctrl Pts',(0.,56.7912500034686,-14.8379150279786));
#23411=CARTESIAN_POINT('Ctrl Pts',(2.02798109407154,56.6642500034688,-14.1789840269267));
#23412=CARTESIAN_POINT('Ctrl Pts',(4.05596218814312,56.5372500034686,-13.5200530258749));
#23413=CARTESIAN_POINT('Ctrl Pts',(5.30932343282159,56.4102500034686,-11.7949492688802));
#23414=CARTESIAN_POINT('Ctrl Pts',(6.56268467750008,56.2832500034686,-10.0698455118856));
#23415=CARTESIAN_POINT('Ctrl Pts',(6.56268467749999,56.1562500034686,-7.93749999999999));
#23416=CARTESIAN_POINT('Origin',(-2.53888687851145E-9,74.888750003468,-7.9374999999999));
#23417=CARTESIAN_POINT('',(6.56268467749999,52.9812500034686,-7.93750000003681));
#23418=CARTESIAN_POINT('',(6.56268467749999,53.6162500034686,-7.93750000003573));
#23419=CARTESIAN_POINT('',(6.56268467242224,74.8887500034674,-7.93749999999981));
#23420=CARTESIAN_POINT('Ctrl Pts',(6.5626846775001,55.5212500034686,-7.93749999999999));
#23421=CARTESIAN_POINT('Ctrl Pts',(6.56268467750008,55.3942500034686,-5.80515448811441));
#23422=CARTESIAN_POINT('Ctrl Pts',(5.30932343282153,55.2672500034686,-4.08005073111967));
#23423=CARTESIAN_POINT('Ctrl Pts',(4.05596218814318,55.1402500034685,-2.35494697412514));
#23424=CARTESIAN_POINT('Ctrl Pts',(2.0279810940716,55.0132500034686,-1.69601597307317));
#23425=CARTESIAN_POINT('Ctrl Pts',(-5.83678785436452E-14,54.8862500034686,
-1.0370849720215));
#23426=CARTESIAN_POINT('Ctrl Pts',(-2.0279810940716,54.7592500034686,-1.69601597307323));
#23427=CARTESIAN_POINT('Ctrl Pts',(-4.05596218814318,54.6322500034686,-2.35494697412514));
#23428=CARTESIAN_POINT('Ctrl Pts',(-5.30932343282159,54.5052500034687,-4.08005073111972));
#23429=CARTESIAN_POINT('Ctrl Pts',(-6.56268467749997,54.3782500034686,-5.80515448811441));
#23430=CARTESIAN_POINT('Ctrl Pts',(-6.56268467749999,54.2512500034685,-7.93750000000004));
#23431=CARTESIAN_POINT('Ctrl Pts',(-6.56268467750003,54.1242500034686,-10.0698455118856));
#23432=CARTESIAN_POINT('Ctrl Pts',(-5.30932343282153,53.9972500034686,-11.7949492688803));
#23433=CARTESIAN_POINT('Ctrl Pts',(-4.05596218814318,53.8702500034686,-13.5200530258749));
#23434=CARTESIAN_POINT('Ctrl Pts',(-2.02798109407154,53.7432500034686,-14.1789840269267));
#23435=CARTESIAN_POINT('Ctrl Pts',(0.,53.6162500034685,-14.8379150279786));
#23436=CARTESIAN_POINT('Ctrl Pts',(2.02798109407165,53.4892500034686,-14.1789840269267));
#23437=CARTESIAN_POINT('Ctrl Pts',(4.05596218814312,53.3622500034686,-13.5200530258749));
#23438=CARTESIAN_POINT('Ctrl Pts',(5.30932343282153,53.2352500034686,-11.7949492688803));
#23439=CARTESIAN_POINT('Ctrl Pts',(6.56268467750003,53.1082500034686,-10.0698455118856));
#23440=CARTESIAN_POINT('Ctrl Pts',(6.56268467749999,52.9812500034686,-7.93750000000004));
#23441=CARTESIAN_POINT('Ctrl Pts',(6.56268467749999,56.1562500034686,-7.93749999999999));
#23442=CARTESIAN_POINT('Ctrl Pts',(6.56268467750003,56.0292500034686,-5.80515448811441));
#23443=CARTESIAN_POINT('Ctrl Pts',(5.30932343282164,55.9022500034686,-4.08005073111967));
#23444=CARTESIAN_POINT('Ctrl Pts',(4.05596218814324,55.7752500034686,-2.35494697412514));
#23445=CARTESIAN_POINT('Ctrl Pts',(2.0279810940716,55.6482500034686,-1.69601597307317));
#23446=CARTESIAN_POINT('Ctrl Pts',(0.,55.5212500034686,-1.0370849720215));
#23447=CARTESIAN_POINT('Ctrl Pts',(-2.02798109407148,55.3942500034686,-1.69601597307317));
#23448=CARTESIAN_POINT('Ctrl Pts',(-4.05596218814312,55.2672500034686,-2.35494697412514));
#23449=CARTESIAN_POINT('Ctrl Pts',(-5.30932343282159,55.1402500034686,-4.08005073111967));
#23450=CARTESIAN_POINT('Ctrl Pts',(-6.56268467749991,55.0132500034686,-5.80515448811441));
#23451=CARTESIAN_POINT('Ctrl Pts',(-6.56268467749987,54.8862500034686,-7.93750000000004));
#23452=CARTESIAN_POINT('Ctrl Pts',(-6.56268467749997,54.7592500034686,-10.0698455118856));
#23453=CARTESIAN_POINT('Ctrl Pts',(-5.30932343282153,54.6322500034687,-11.7949492688803));
#23454=CARTESIAN_POINT('Ctrl Pts',(-4.05596218814312,54.5052500034686,-13.5200530258749));
#23455=CARTESIAN_POINT('Ctrl Pts',(-2.02798109407154,54.3782500034687,-14.1789840269267));
#23456=CARTESIAN_POINT('Ctrl Pts',(0.,54.2512500034685,-14.8379150279786));
#23457=CARTESIAN_POINT('Ctrl Pts',(2.02798109407154,54.1242500034687,-14.1789840269267));
#23458=CARTESIAN_POINT('Ctrl Pts',(4.05596218814312,53.9972500034686,-13.5200530258749));
#23459=CARTESIAN_POINT('Ctrl Pts',(5.30932343282164,53.8702500034687,-11.7949492688803));
#23460=CARTESIAN_POINT('Ctrl Pts',(6.56268467749997,53.7432500034685,-10.0698455118856));
#23461=CARTESIAN_POINT('Ctrl Pts',(6.56268467749999,53.6162500034686,-7.93750000000004));
#23462=CARTESIAN_POINT('Origin',(-2.53888687851145E-9,74.888750003468,-7.9374999999999));
#23463=CARTESIAN_POINT('',(6.56268467749999,50.4412500034686,-7.93750000004108));
#23464=CARTESIAN_POINT('',(6.56268467749999,51.0762500034687,-7.93750000004001));
#23465=CARTESIAN_POINT('',(6.56268467242224,74.8887500034674,-7.93749999999981));
#23466=CARTESIAN_POINT('Ctrl Pts',(6.56268467749999,52.9812500034686,-7.93750000000004));
#23467=CARTESIAN_POINT('Ctrl Pts',(6.56268467749997,52.8542500034685,-5.80515448811441));
#23468=CARTESIAN_POINT('Ctrl Pts',(5.30932343282159,52.7272500034686,-4.08005073111972));
#23469=CARTESIAN_POINT('Ctrl Pts',(4.05596218814318,52.6002500034685,-2.35494697412514));
#23470=CARTESIAN_POINT('Ctrl Pts',(2.0279810940716,52.4732500034685,-1.69601597307323));
#23471=CARTESIAN_POINT('Ctrl Pts',(0.,52.3462500034685,-1.0370849720215));
#23472=CARTESIAN_POINT('Ctrl Pts',(-2.0279810940716,52.2192500034686,-1.69601597307323));
#23473=CARTESIAN_POINT('Ctrl Pts',(-4.05596218814318,52.0922500034686,-2.35494697412514));
#23474=CARTESIAN_POINT('Ctrl Pts',(-5.30932343282153,51.9652500034687,-4.08005073111972));
#23475=CARTESIAN_POINT('Ctrl Pts',(-6.56268467749997,51.8382500034685,-5.80515448811441));
#23476=CARTESIAN_POINT('Ctrl Pts',(-6.56268467749999,51.7112500034686,-7.93750000000004));
#23477=CARTESIAN_POINT('Ctrl Pts',(-6.56268467750003,51.5842500034685,-10.0698455118856));
#23478=CARTESIAN_POINT('Ctrl Pts',(-5.30932343282153,51.4572500034685,-11.7949492688803));
#23479=CARTESIAN_POINT('Ctrl Pts',(-4.05596218814306,51.3302500034686,-13.5200530258749));
#23480=CARTESIAN_POINT('Ctrl Pts',(-2.02798109407154,51.2032500034688,-14.1789840269267));
#23481=CARTESIAN_POINT('Ctrl Pts',(1.1673575708729E-13,51.0762500034686,
-14.8379150279786));
#23482=CARTESIAN_POINT('Ctrl Pts',(2.02798109407154,50.9492500034687,-14.1789840269267));
#23483=CARTESIAN_POINT('Ctrl Pts',(4.05596218814324,50.8222500034686,-13.5200530258749));
#23484=CARTESIAN_POINT('Ctrl Pts',(5.30932343282153,50.6952500034686,-11.7949492688803));
#23485=CARTESIAN_POINT('Ctrl Pts',(6.56268467750003,50.5682500034686,-10.0698455118856));
#23486=CARTESIAN_POINT('Ctrl Pts',(6.56268467749999,50.4412500034686,-7.93750000000004));
#23487=CARTESIAN_POINT('Ctrl Pts',(6.56268467749999,53.6162500034686,-7.93750000000004));
#23488=CARTESIAN_POINT('Ctrl Pts',(6.56268467750003,53.4892500034685,-5.80515448811441));
#23489=CARTESIAN_POINT('Ctrl Pts',(5.30932343282159,53.3622500034686,-4.08005073111972));
#23490=CARTESIAN_POINT('Ctrl Pts',(4.05596218814312,53.2352500034685,-2.35494697412514));
#23491=CARTESIAN_POINT('Ctrl Pts',(2.0279810940716,53.1082500034686,-1.69601597307323));
#23492=CARTESIAN_POINT('Ctrl Pts',(0.,52.9812500034685,-1.0370849720215));
#23493=CARTESIAN_POINT('Ctrl Pts',(-2.02798109407148,52.8542500034686,-1.69601597307323));
#23494=CARTESIAN_POINT('Ctrl Pts',(-4.05596218814312,52.7272500034686,-2.35494697412514));
#23495=CARTESIAN_POINT('Ctrl Pts',(-5.30932343282159,52.6002500034685,-4.08005073111972));
#23496=CARTESIAN_POINT('Ctrl Pts',(-6.56268467750003,52.4732500034686,-5.80515448811441));
#23497=CARTESIAN_POINT('Ctrl Pts',(-6.56268467749999,52.3462500034686,-7.93750000000004));
#23498=CARTESIAN_POINT('Ctrl Pts',(-6.56268467749997,52.2192500034685,-10.0698455118856));
#23499=CARTESIAN_POINT('Ctrl Pts',(-5.30932343282153,52.0922500034686,-11.7949492688803));
#23500=CARTESIAN_POINT('Ctrl Pts',(-4.05596218814312,51.9652500034685,-13.5200530258749));
#23501=CARTESIAN_POINT('Ctrl Pts',(-2.02798109407154,51.8382500034687,-14.1789840269267));
#23502=CARTESIAN_POINT('Ctrl Pts',(0.,51.7112500034685,-14.8379150279786));
#23503=CARTESIAN_POINT('Ctrl Pts',(2.02798109407154,51.5842500034687,-14.1789840269267));
#23504=CARTESIAN_POINT('Ctrl Pts',(4.05596218814312,51.4572500034685,-13.5200530258749));
#23505=CARTESIAN_POINT('Ctrl Pts',(5.30932343282164,51.3302500034686,-11.7949492688803));
#23506=CARTESIAN_POINT('Ctrl Pts',(6.56268467750008,51.2032500034686,-10.0698455118856));
#23507=CARTESIAN_POINT('Ctrl Pts',(6.56268467749999,51.0762500034687,-7.93750000000004));
#23508=CARTESIAN_POINT('Origin',(-2.53888687851145E-9,74.888750003468,-7.9374999999999));
#23509=CARTESIAN_POINT('',(6.56268467750004,47.9012500034686,-7.93750000004536));
#23510=CARTESIAN_POINT('',(6.56268467750004,48.5362500034686,-7.93750000004429));
#23511=CARTESIAN_POINT('',(6.56268467242224,74.8887500034674,-7.93749999999981));
#23512=CARTESIAN_POINT('Ctrl Pts',(6.56268467749999,50.4412500034686,-7.93750000000004));
#23513=CARTESIAN_POINT('Ctrl Pts',(6.56268467750003,50.3142500034686,-5.80515448811441));
#23514=CARTESIAN_POINT('Ctrl Pts',(5.30932343282159,50.1872500034685,-4.08005073111972));
#23515=CARTESIAN_POINT('Ctrl Pts',(4.05596218814318,50.0602500034686,-2.35494697412514));
#23516=CARTESIAN_POINT('Ctrl Pts',(2.0279810940716,49.9332500034686,-1.69601597307323));
#23517=CARTESIAN_POINT('Ctrl Pts',(1.1673575708729E-13,49.8062500034686,
-1.0370849720215));
#23518=CARTESIAN_POINT('Ctrl Pts',(-2.0279810940716,49.6792500034686,-1.69601597307323));
#23519=CARTESIAN_POINT('Ctrl Pts',(-4.05596218814312,49.5522500034686,-2.35494697412514));
#23520=CARTESIAN_POINT('Ctrl Pts',(-5.30932343282153,49.4252500034686,-4.08005073111972));
#23521=CARTESIAN_POINT('Ctrl Pts',(-6.56268467750008,49.2982500034686,-5.80515448811441));
#23522=CARTESIAN_POINT('Ctrl Pts',(-6.56268467749999,49.1712500034686,-7.93750000000004));
#23523=CARTESIAN_POINT('Ctrl Pts',(-6.56268467750003,49.0442500034686,-10.0698455118856));
#23524=CARTESIAN_POINT('Ctrl Pts',(-5.30932343282148,48.9172500034685,-11.7949492688803));
#23525=CARTESIAN_POINT('Ctrl Pts',(-4.05596218814318,48.7902500034686,-13.5200530258749));
#23526=CARTESIAN_POINT('Ctrl Pts',(-2.02798109407165,48.6632500034687,-14.1789840269267));
#23527=CARTESIAN_POINT('Ctrl Pts',(0.,48.5362500034685,-14.8379150279786));
#23528=CARTESIAN_POINT('Ctrl Pts',(2.0279810940716,48.4092500034688,-14.1789840269267));
#23529=CARTESIAN_POINT('Ctrl Pts',(4.05596218814312,48.2822500034686,-13.5200530258749));
#23530=CARTESIAN_POINT('Ctrl Pts',(5.30932343282159,48.1552500034686,-11.7949492688803));
#23531=CARTESIAN_POINT('Ctrl Pts',(6.56268467750008,48.0282500034685,-10.0698455118856));
#23532=CARTESIAN_POINT('Ctrl Pts',(6.56268467750004,47.9012500034686,-7.93750000000004));
#23533=CARTESIAN_POINT('Ctrl Pts',(6.56268467749999,51.0762500034687,-7.93750000000004));
#23534=CARTESIAN_POINT('Ctrl Pts',(6.56268467749997,50.9492500034685,-5.80515448811441));
#23535=CARTESIAN_POINT('Ctrl Pts',(5.30932343282159,50.8222500034686,-4.08005073111972));
#23536=CARTESIAN_POINT('Ctrl Pts',(4.05596218814312,50.6952500034686,-2.35494697412514));
#23537=CARTESIAN_POINT('Ctrl Pts',(2.0279810940716,50.5682500034686,-1.69601597307323));
#23538=CARTESIAN_POINT('Ctrl Pts',(0.,50.4412500034686,-1.0370849720215));
#23539=CARTESIAN_POINT('Ctrl Pts',(-2.0279810940716,50.3142500034687,-1.69601597307323));
#23540=CARTESIAN_POINT('Ctrl Pts',(-4.05596218814312,50.1872500034686,-2.35494697412514));
#23541=CARTESIAN_POINT('Ctrl Pts',(-5.30932343282153,50.0602500034686,-4.08005073111972));
#23542=CARTESIAN_POINT('Ctrl Pts',(-6.56268467750003,49.9332500034686,-5.80515448811441));
#23543=CARTESIAN_POINT('Ctrl Pts',(-6.56268467749999,49.8062500034686,-7.93750000000004));
#23544=CARTESIAN_POINT('Ctrl Pts',(-6.56268467749997,49.6792500034685,-10.0698455118856));
#23545=CARTESIAN_POINT('Ctrl Pts',(-5.30932343282159,49.5522500034686,-11.7949492688803));
#23546=CARTESIAN_POINT('Ctrl Pts',(-4.05596218814312,49.4252500034686,-13.5200530258749));
#23547=CARTESIAN_POINT('Ctrl Pts',(-2.02798109407154,49.2982500034686,-14.1789840269267));
#23548=CARTESIAN_POINT('Ctrl Pts',(0.,49.1712500034685,-14.8379150279786));
#23549=CARTESIAN_POINT('Ctrl Pts',(2.0279810940716,49.0442500034687,-14.1789840269267));
#23550=CARTESIAN_POINT('Ctrl Pts',(4.05596218814318,48.9172500034685,-13.5200530258749));
#23551=CARTESIAN_POINT('Ctrl Pts',(5.30932343282159,48.7902500034686,-11.7949492688803));
#23552=CARTESIAN_POINT('Ctrl Pts',(6.56268467750003,48.6632500034685,-10.0698455118856));
#23553=CARTESIAN_POINT('Ctrl Pts',(6.56268467750004,48.5362500034686,-7.93750000000004));
#23554=CARTESIAN_POINT('Origin',(-2.53888687851145E-9,74.888750003468,-7.9374999999999));
#23555=CARTESIAN_POINT('',(6.5626846775001,45.3612500034686,-7.93750000004963));
#23556=CARTESIAN_POINT('',(6.56268467749993,45.9962500034686,-7.93750000004856));
#23557=CARTESIAN_POINT('',(6.56268467242224,74.8887500034674,-7.93749999999981));
#23558=CARTESIAN_POINT('Ctrl Pts',(6.56268467750004,47.9012500034686,-7.93750000000004));
#23559=CARTESIAN_POINT('Ctrl Pts',(6.56268467750003,47.7742500034685,-5.80515448811441));
#23560=CARTESIAN_POINT('Ctrl Pts',(5.30932343282159,47.6472500034686,-4.08005073111972));
#23561=CARTESIAN_POINT('Ctrl Pts',(4.05596218814324,47.5202500034686,-2.35494697412514));
#23562=CARTESIAN_POINT('Ctrl Pts',(2.02798109407165,47.3932500034687,-1.69601597307323));
#23563=CARTESIAN_POINT('Ctrl Pts',(0.,47.2662500034685,-1.0370849720215));
#23564=CARTESIAN_POINT('Ctrl Pts',(-2.02798109407154,47.1392500034686,-1.69601597307323));
#23565=CARTESIAN_POINT('Ctrl Pts',(-4.05596218814312,47.0122500034686,-2.35494697412514));
#23566=CARTESIAN_POINT('Ctrl Pts',(-5.30932343282148,46.8852500034686,-4.08005073111972));
#23567=CARTESIAN_POINT('Ctrl Pts',(-6.56268467749991,46.7582500034685,-5.80515448811441));
#23568=CARTESIAN_POINT('Ctrl Pts',(-6.56268467749999,46.6312500034686,-7.93750000000004));
#23569=CARTESIAN_POINT('Ctrl Pts',(-6.56268467749997,46.5042500034685,-10.0698455118856));
#23570=CARTESIAN_POINT('Ctrl Pts',(-5.30932343282148,46.3772500034686,-11.7949492688803));
#23571=CARTESIAN_POINT('Ctrl Pts',(-4.05596218814312,46.2502500034686,-13.5200530258749));
#23572=CARTESIAN_POINT('Ctrl Pts',(-2.0279810940716,46.1232500034687,-14.1789840269267));
#23573=CARTESIAN_POINT('Ctrl Pts',(0.,45.9962500034684,-14.8379150279786));
#23574=CARTESIAN_POINT('Ctrl Pts',(2.0279810940716,45.8692500034687,-14.1789840269267));
#23575=CARTESIAN_POINT('Ctrl Pts',(4.05596218814312,45.7422500034686,-13.5200530258749));
#23576=CARTESIAN_POINT('Ctrl Pts',(5.30932343282159,45.6152500034686,-11.7949492688803));
#23577=CARTESIAN_POINT('Ctrl Pts',(6.56268467749997,45.4882500034686,-10.0698455118856));
#23578=CARTESIAN_POINT('Ctrl Pts',(6.5626846775001,45.3612500034686,-7.93750000000004));
#23579=CARTESIAN_POINT('Ctrl Pts',(6.56268467750004,48.5362500034686,-7.93750000000004));
#23580=CARTESIAN_POINT('Ctrl Pts',(6.56268467750008,48.4092500034685,-5.80515448811441));
#23581=CARTESIAN_POINT('Ctrl Pts',(5.30932343282159,48.2822500034686,-4.08005073111972));
#23582=CARTESIAN_POINT('Ctrl Pts',(4.05596218814312,48.1552500034686,-2.35494697412514));
#23583=CARTESIAN_POINT('Ctrl Pts',(2.02798109407154,48.0282500034685,-1.69601597307323));
#23584=CARTESIAN_POINT('Ctrl Pts',(0.,47.9012500034685,-1.0370849720215));
#23585=CARTESIAN_POINT('Ctrl Pts',(-2.02798109407154,47.7742500034686,-1.69601597307323));
#23586=CARTESIAN_POINT('Ctrl Pts',(-4.05596218814318,47.6472500034685,-2.35494697412514));
#23587=CARTESIAN_POINT('Ctrl Pts',(-5.30932343282153,47.5202500034686,-4.08005073111972));
#23588=CARTESIAN_POINT('Ctrl Pts',(-6.56268467750003,47.3932500034686,-5.80515448811441));
#23589=CARTESIAN_POINT('Ctrl Pts',(-6.56268467749999,47.2662500034685,-7.93750000000004));
#23590=CARTESIAN_POINT('Ctrl Pts',(-6.56268467750003,47.1392500034685,-10.0698455118856));
#23591=CARTESIAN_POINT('Ctrl Pts',(-5.30932343282159,47.0122500034686,-11.7949492688803));
#23592=CARTESIAN_POINT('Ctrl Pts',(-4.05596218814324,46.8852500034686,-13.5200530258749));
#23593=CARTESIAN_POINT('Ctrl Pts',(-2.02798109407148,46.7582500034687,-14.1789840269267));
#23594=CARTESIAN_POINT('Ctrl Pts',(-1.1673575708729E-13,46.6312500034685,
-14.8379150279786));
#23595=CARTESIAN_POINT('Ctrl Pts',(2.0279810940716,46.5042500034687,-14.1789840269267));
#23596=CARTESIAN_POINT('Ctrl Pts',(4.05596218814318,46.3772500034686,-13.5200530258749));
#23597=CARTESIAN_POINT('Ctrl Pts',(5.30932343282159,46.2502500034686,-11.7949492688803));
#23598=CARTESIAN_POINT('Ctrl Pts',(6.56268467750003,46.1232500034686,-10.0698455118856));
#23599=CARTESIAN_POINT('Ctrl Pts',(6.56268467749993,45.9962500034686,-7.93750000000004));
#23600=CARTESIAN_POINT('Origin',(-2.53888687851145E-9,74.888750003468,-7.9374999999999));
#23601=CARTESIAN_POINT('',(6.5626846775001,42.8212500034686,-7.93750000005391));
#23602=CARTESIAN_POINT('',(6.56268467749999,43.4562500034686,-7.93750000005284));
#23603=CARTESIAN_POINT('',(6.56268467242224,74.8887500034674,-7.93749999999981));
#23604=CARTESIAN_POINT('Ctrl Pts',(6.5626846775001,45.3612500034686,-7.93750000000004));
#23605=CARTESIAN_POINT('Ctrl Pts',(6.56268467750003,45.2342500034686,-5.80515448811441));
#23606=CARTESIAN_POINT('Ctrl Pts',(5.30932343282153,45.1072500034687,-4.08005073111972));
#23607=CARTESIAN_POINT('Ctrl Pts',(4.05596218814312,44.9802500034686,-2.35494697412514));
#23608=CARTESIAN_POINT('Ctrl Pts',(2.02798109407165,44.8532500034686,-1.69601597307323));
#23609=CARTESIAN_POINT('Ctrl Pts',(0.,44.7262500034686,-1.0370849720215));
#23610=CARTESIAN_POINT('Ctrl Pts',(-2.02798109407154,44.5992500034686,-1.69601597307323));
#23611=CARTESIAN_POINT('Ctrl Pts',(-4.05596218814312,44.4722500034685,-2.35494697412514));
#23612=CARTESIAN_POINT('Ctrl Pts',(-5.30932343282148,44.3452500034686,-4.08005073111972));
#23613=CARTESIAN_POINT('Ctrl Pts',(-6.56268467750003,44.2182500034685,-5.80515448811441));
#23614=CARTESIAN_POINT('Ctrl Pts',(-6.56268467750004,44.0912500034686,-7.93750000000004));
#23615=CARTESIAN_POINT('Ctrl Pts',(-6.56268467749997,43.9642500034686,-10.0698455118856));
#23616=CARTESIAN_POINT('Ctrl Pts',(-5.30932343282148,43.8372500034686,-11.7949492688803));
#23617=CARTESIAN_POINT('Ctrl Pts',(-4.05596218814312,43.7102500034686,-13.5200530258749));
#23618=CARTESIAN_POINT('Ctrl Pts',(-2.0279810940716,43.5832500034687,-14.1789840269267));
#23619=CARTESIAN_POINT('Ctrl Pts',(0.,43.4562500034686,-14.8379150279786));
#23620=CARTESIAN_POINT('Ctrl Pts',(2.0279810940716,43.3292500034687,-14.1789840269267));
#23621=CARTESIAN_POINT('Ctrl Pts',(4.05596218814312,43.2022500034684,-13.5200530258749));
#23622=CARTESIAN_POINT('Ctrl Pts',(5.30932343282159,43.0752500034686,-11.7949492688803));
#23623=CARTESIAN_POINT('Ctrl Pts',(6.56268467750008,42.9482500034686,-10.0698455118856));
#23624=CARTESIAN_POINT('Ctrl Pts',(6.5626846775001,42.8212500034686,-7.93750000000004));
#23625=CARTESIAN_POINT('Ctrl Pts',(6.56268467749993,45.9962500034686,-7.93750000000004));
#23626=CARTESIAN_POINT('Ctrl Pts',(6.56268467750008,45.8692500034686,-5.80515448811441));
#23627=CARTESIAN_POINT('Ctrl Pts',(5.30932343282159,45.7422500034685,-4.08005073111972));
#23628=CARTESIAN_POINT('Ctrl Pts',(4.05596218814318,45.6152500034686,-2.35494697412514));
#23629=CARTESIAN_POINT('Ctrl Pts',(2.02798109407154,45.4882500034685,-1.69601597307323));
#23630=CARTESIAN_POINT('Ctrl Pts',(-1.1673575708729E-13,45.3612500034685,
-1.0370849720215));
#23631=CARTESIAN_POINT('Ctrl Pts',(-2.02798109407154,45.2342500034686,-1.69601597307323));
#23632=CARTESIAN_POINT('Ctrl Pts',(-4.05596218814306,45.1072500034685,-2.35494697412514));
#23633=CARTESIAN_POINT('Ctrl Pts',(-5.30932343282159,44.9802500034686,-4.08005073111972));
#23634=CARTESIAN_POINT('Ctrl Pts',(-6.56268467749997,44.8532500034685,-5.80515448811441));
#23635=CARTESIAN_POINT('Ctrl Pts',(-6.56268467749993,44.7262500034686,-7.93750000000004));
#23636=CARTESIAN_POINT('Ctrl Pts',(-6.56268467749991,44.5992500034686,-10.0698455118856));
#23637=CARTESIAN_POINT('Ctrl Pts',(-5.30932343282159,44.4722500034685,-11.7949492688803));
#23638=CARTESIAN_POINT('Ctrl Pts',(-4.05596218814306,44.3452500034686,-13.5200530258749));
#23639=CARTESIAN_POINT('Ctrl Pts',(-2.02798109407148,44.2182500034687,-14.1789840269267));
#23640=CARTESIAN_POINT('Ctrl Pts',(0.,44.0912500034687,-14.8379150279786));
#23641=CARTESIAN_POINT('Ctrl Pts',(2.0279810940716,43.9642500034687,-14.1789840269267));
#23642=CARTESIAN_POINT('Ctrl Pts',(4.05596218814318,43.8372500034685,-13.5200530258749));
#23643=CARTESIAN_POINT('Ctrl Pts',(5.30932343282159,43.7102500034686,-11.7949492688803));
#23644=CARTESIAN_POINT('Ctrl Pts',(6.56268467750003,43.5832500034686,-10.0698455118856));
#23645=CARTESIAN_POINT('Ctrl Pts',(6.56268467749999,43.4562500034686,-7.93750000000004));
#23646=CARTESIAN_POINT('Origin',(-2.53888687851145E-9,74.888750003468,-7.9374999999999));
#23647=CARTESIAN_POINT('',(6.5626846775001,40.2812500034686,-7.93750000005818));
#23648=CARTESIAN_POINT('',(6.56268467749999,40.9162500034685,-7.93750000005712));
#23649=CARTESIAN_POINT('',(6.56268467242224,74.8887500034674,-7.93749999999981));
#23650=CARTESIAN_POINT('Ctrl Pts',(6.5626846775001,42.8212500034686,-7.93750000000004));
#23651=CARTESIAN_POINT('Ctrl Pts',(6.56268467750003,42.6942500034686,-5.80515448811441));
#23652=CARTESIAN_POINT('Ctrl Pts',(5.30932343282153,42.5672500034686,-4.08005073111972));
#23653=CARTESIAN_POINT('Ctrl Pts',(4.05596218814324,42.4402500034686,-2.35494697412514));
#23654=CARTESIAN_POINT('Ctrl Pts',(2.02798109407165,42.3132500034686,-1.69601597307323));
#23655=CARTESIAN_POINT('Ctrl Pts',(0.,42.1862500034686,-1.0370849720215));
#23656=CARTESIAN_POINT('Ctrl Pts',(-2.0279810940716,42.0592500034685,-1.69601597307323));
#23657=CARTESIAN_POINT('Ctrl Pts',(-4.05596218814312,41.9322500034686,-2.35494697412514));
#23658=CARTESIAN_POINT('Ctrl Pts',(-5.30932343282148,41.8052500034685,-4.08005073111972));
#23659=CARTESIAN_POINT('Ctrl Pts',(-6.56268467750003,41.6782500034686,-5.80515448811441));
#23660=CARTESIAN_POINT('Ctrl Pts',(-6.56268467750004,41.5512500034686,-7.93750000000004));
#23661=CARTESIAN_POINT('Ctrl Pts',(-6.56268467749997,41.4242500034686,-10.0698455118856));
#23662=CARTESIAN_POINT('Ctrl Pts',(-5.30932343282153,41.2972500034686,-11.7949492688803));
#23663=CARTESIAN_POINT('Ctrl Pts',(-4.05596218814312,41.1702500034685,-13.5200530258749));
#23664=CARTESIAN_POINT('Ctrl Pts',(-2.0279810940716,41.0432500034686,-14.1789840269267));
#23665=CARTESIAN_POINT('Ctrl Pts',(0.,40.9162500034686,-14.8379150279786));
#23666=CARTESIAN_POINT('Ctrl Pts',(2.02798109407165,40.7892500034687,-14.1789840269267));
#23667=CARTESIAN_POINT('Ctrl Pts',(4.05596218814312,40.6622500034685,-13.5200530258749));
#23668=CARTESIAN_POINT('Ctrl Pts',(5.30932343282153,40.5352500034686,-11.7949492688803));
#23669=CARTESIAN_POINT('Ctrl Pts',(6.56268467749997,40.4082500034686,-10.0698455118856));
#23670=CARTESIAN_POINT('Ctrl Pts',(6.5626846775001,40.2812500034686,-7.93750000000004));
#23671=CARTESIAN_POINT('Ctrl Pts',(6.56268467749999,43.4562500034686,-7.93750000000004));
#23672=CARTESIAN_POINT('Ctrl Pts',(6.56268467749997,43.3292500034686,-5.80515448811441));
#23673=CARTESIAN_POINT('Ctrl Pts',(5.30932343282164,43.2022500034686,-4.08005073111972));
#23674=CARTESIAN_POINT('Ctrl Pts',(4.05596218814306,43.0752500034686,-2.35494697412514));
#23675=CARTESIAN_POINT('Ctrl Pts',(2.02798109407154,42.9482500034687,-1.69601597307323));
#23676=CARTESIAN_POINT('Ctrl Pts',(1.1673575708729E-13,42.8212500034686,
-1.0370849720215));
#23677=CARTESIAN_POINT('Ctrl Pts',(-2.02798109407154,42.6942500034686,-1.69601597307323));
#23678=CARTESIAN_POINT('Ctrl Pts',(-4.05596218814318,42.5672500034685,-2.35494697412514));
#23679=CARTESIAN_POINT('Ctrl Pts',(-5.30932343282159,42.4402500034686,-4.08005073111972));
#23680=CARTESIAN_POINT('Ctrl Pts',(-6.56268467749997,42.3132500034686,-5.80515448811441));
#23681=CARTESIAN_POINT('Ctrl Pts',(-6.56268467749993,42.1862500034687,-7.93750000000004));
#23682=CARTESIAN_POINT('Ctrl Pts',(-6.56268467750003,42.0592500034685,-10.0698455118856));
#23683=CARTESIAN_POINT('Ctrl Pts',(-5.30932343282159,41.9322500034685,-11.7949492688803));
#23684=CARTESIAN_POINT('Ctrl Pts',(-4.05596218814306,41.8052500034685,-13.5200530258749));
#23685=CARTESIAN_POINT('Ctrl Pts',(-2.02798109407148,41.6782500034687,-14.1789840269267));
#23686=CARTESIAN_POINT('Ctrl Pts',(1.1673575708729E-13,41.5512500034686,
-14.8379150279786));
#23687=CARTESIAN_POINT('Ctrl Pts',(2.02798109407154,41.4242500034688,-14.1789840269267));
#23688=CARTESIAN_POINT('Ctrl Pts',(4.05596218814324,41.2972500034684,-13.5200530258749));
#23689=CARTESIAN_POINT('Ctrl Pts',(5.30932343282159,41.1702500034686,-11.7949492688803));
#23690=CARTESIAN_POINT('Ctrl Pts',(6.56268467750003,41.0432500034686,-10.0698455118856));
#23691=CARTESIAN_POINT('Ctrl Pts',(6.56268467749999,40.9162500034685,-7.93750000000004));
#23692=CARTESIAN_POINT('Origin',(-2.53888687851145E-9,74.888750003468,-7.9374999999999));
#23693=CARTESIAN_POINT('',(6.56268467749999,37.7412500034686,-7.93750000006246));
#23694=CARTESIAN_POINT('',(6.56268467749999,38.3762500034686,-7.93750000006139));
#23695=CARTESIAN_POINT('',(6.56268467242224,74.8887500034674,-7.93749999999981));
#23696=CARTESIAN_POINT('Ctrl Pts',(6.5626846775001,40.2812500034686,-7.93750000000004));
#23697=CARTESIAN_POINT('Ctrl Pts',(6.56268467750008,40.1542500034685,-5.80515448811441));
#23698=CARTESIAN_POINT('Ctrl Pts',(5.30932343282153,40.0272500034686,-4.08005073111972));
#23699=CARTESIAN_POINT('Ctrl Pts',(4.05596218814312,39.9002500034686,-2.35494697412514));
#23700=CARTESIAN_POINT('Ctrl Pts',(2.0279810940716,39.7732500034685,-1.69601597307323));
#23701=CARTESIAN_POINT('Ctrl Pts',(0.,39.6462500034686,-1.0370849720215));
#23702=CARTESIAN_POINT('Ctrl Pts',(-2.0279810940716,39.5192500034686,-1.69601597307323));
#23703=CARTESIAN_POINT('Ctrl Pts',(-4.05596218814324,39.3922500034686,-2.35494697412514));
#23704=CARTESIAN_POINT('Ctrl Pts',(-5.30932343282148,39.2652500034686,-4.08005073111972));
#23705=CARTESIAN_POINT('Ctrl Pts',(-6.56268467749991,39.1382500034686,-5.80515448811441));
#23706=CARTESIAN_POINT('Ctrl Pts',(-6.56268467749999,39.0112500034685,-7.93750000000004));
#23707=CARTESIAN_POINT('Ctrl Pts',(-6.56268467750008,38.8842500034686,-10.0698455118856));
#23708=CARTESIAN_POINT('Ctrl Pts',(-5.30932343282153,38.7572500034686,-11.7949492688803));
#23709=CARTESIAN_POINT('Ctrl Pts',(-4.05596218814312,38.6302500034686,-13.5200530258749));
#23710=CARTESIAN_POINT('Ctrl Pts',(-2.02798109407154,38.5032500034686,-14.1789840269267));
#23711=CARTESIAN_POINT('Ctrl Pts',(0.,38.3762500034685,-14.8379150279786));
#23712=CARTESIAN_POINT('Ctrl Pts',(2.02798109407165,38.2492500034686,-14.1789840269267));
#23713=CARTESIAN_POINT('Ctrl Pts',(4.05596218814318,38.1222500034686,-13.5200530258749));
#23714=CARTESIAN_POINT('Ctrl Pts',(5.30932343282153,37.9952500034686,-11.7949492688803));
#23715=CARTESIAN_POINT('Ctrl Pts',(6.56268467750003,37.8682500034686,-10.0698455118856));
#23716=CARTESIAN_POINT('Ctrl Pts',(6.56268467749999,37.7412500034686,-7.93750000000004));
#23717=CARTESIAN_POINT('Ctrl Pts',(6.56268467749999,40.9162500034685,-7.93750000000004));
#23718=CARTESIAN_POINT('Ctrl Pts',(6.56268467750014,40.7892500034686,-5.80515448811441));
#23719=CARTESIAN_POINT('Ctrl Pts',(5.30932343282164,40.6622500034686,-4.08005073111972));
#23720=CARTESIAN_POINT('Ctrl Pts',(4.05596218814318,40.5352500034686,-2.35494697412514));
#23721=CARTESIAN_POINT('Ctrl Pts',(2.0279810940716,40.4082500034686,-1.69601597307323));
#23722=CARTESIAN_POINT('Ctrl Pts',(0.,40.2812500034686,-1.0370849720215));
#23723=CARTESIAN_POINT('Ctrl Pts',(-2.02798109407148,40.1542500034686,-1.69601597307323));
#23724=CARTESIAN_POINT('Ctrl Pts',(-4.05596218814312,40.0272500034685,-2.35494697412514));
#23725=CARTESIAN_POINT('Ctrl Pts',(-5.30932343282159,39.9002500034686,-4.08005073111972));
#23726=CARTESIAN_POINT('Ctrl Pts',(-6.56268467749997,39.7732500034686,-5.80515448811441));
#23727=CARTESIAN_POINT('Ctrl Pts',(-6.56268467749987,39.6462500034686,-7.93750000000004));
#23728=CARTESIAN_POINT('Ctrl Pts',(-6.56268467750003,39.5192500034686,-10.0698455118856));
#23729=CARTESIAN_POINT('Ctrl Pts',(-5.30932343282153,39.3922500034687,-11.7949492688803));
#23730=CARTESIAN_POINT('Ctrl Pts',(-4.05596218814318,39.2652500034686,-13.5200530258749));
#23731=CARTESIAN_POINT('Ctrl Pts',(-2.02798109407154,39.1382500034687,-14.1789840269267));
#23732=CARTESIAN_POINT('Ctrl Pts',(0.,39.0112500034685,-14.8379150279786));
#23733=CARTESIAN_POINT('Ctrl Pts',(2.02798109407154,38.8842500034687,-14.1789840269267));
#23734=CARTESIAN_POINT('Ctrl Pts',(4.05596218814312,38.7572500034686,-13.5200530258749));
#23735=CARTESIAN_POINT('Ctrl Pts',(5.30932343282164,38.6302500034687,-11.7949492688803));
#23736=CARTESIAN_POINT('Ctrl Pts',(6.56268467749991,38.5032500034686,-10.0698455118856));
#23737=CARTESIAN_POINT('Ctrl Pts',(6.56268467749999,38.3762500034686,-7.93750000000004));
#23738=CARTESIAN_POINT('Origin',(-2.53888687851145E-9,74.888750003468,-7.9374999999999));
#23739=CARTESIAN_POINT('',(6.56268467749999,35.2012500034686,-7.93750000006674));
#23740=CARTESIAN_POINT('',(6.56268467749999,35.8362500034687,-7.93750000006567));
#23741=CARTESIAN_POINT('',(6.56268467242224,74.8887500034674,-7.93749999999981));
#23742=CARTESIAN_POINT('Ctrl Pts',(6.56268467749999,37.7412500034686,-7.93750000000004));
#23743=CARTESIAN_POINT('Ctrl Pts',(6.56268467750008,37.6142500034686,-5.80515448811441));
#23744=CARTESIAN_POINT('Ctrl Pts',(5.30932343282159,37.4872500034686,-4.08005073111972));
#23745=CARTESIAN_POINT('Ctrl Pts',(4.05596218814312,37.3602500034685,-2.35494697412514));
#23746=CARTESIAN_POINT('Ctrl Pts',(2.0279810940716,37.2332500034685,-1.69601597307323));
#23747=CARTESIAN_POINT('Ctrl Pts',(-1.1673575708729E-13,37.1062500034685,
-1.0370849720215));
#23748=CARTESIAN_POINT('Ctrl Pts',(-2.0279810940716,36.9792500034686,-1.69601597307323));
#23749=CARTESIAN_POINT('Ctrl Pts',(-4.05596218814306,36.8522500034687,-2.35494697412514));
#23750=CARTESIAN_POINT('Ctrl Pts',(-5.30932343282153,36.7252500034687,-4.08005073111972));
#23751=CARTESIAN_POINT('Ctrl Pts',(-6.56268467750003,36.5982500034685,-5.80515448811441));
#23752=CARTESIAN_POINT('Ctrl Pts',(-6.56268467749999,36.4712500034686,-7.93750000000004));
#23753=CARTESIAN_POINT('Ctrl Pts',(-6.56268467749991,36.3442500034685,-10.0698455118856));
#23754=CARTESIAN_POINT('Ctrl Pts',(-5.30932343282153,36.2172500034686,-11.7949492688803));
#23755=CARTESIAN_POINT('Ctrl Pts',(-4.05596218814312,36.0902500034685,-13.5200530258749));
#23756=CARTESIAN_POINT('Ctrl Pts',(-2.02798109407154,35.9632500034688,-14.1789840269267));
#23757=CARTESIAN_POINT('Ctrl Pts',(0.,35.8362500034686,-14.8379150279786));
#23758=CARTESIAN_POINT('Ctrl Pts',(2.02798109407165,35.7092500034686,-14.1789840269267));
#23759=CARTESIAN_POINT('Ctrl Pts',(4.05596218814318,35.5822500034686,-13.5200530258749));
#23760=CARTESIAN_POINT('Ctrl Pts',(5.30932343282153,35.4552500034687,-11.7949492688803));
#23761=CARTESIAN_POINT('Ctrl Pts',(6.56268467750003,35.3282500034686,-10.0698455118856));
#23762=CARTESIAN_POINT('Ctrl Pts',(6.56268467749999,35.2012500034686,-7.93750000000004));
#23763=CARTESIAN_POINT('Ctrl Pts',(6.56268467749999,38.3762500034686,-7.93750000000004));
#23764=CARTESIAN_POINT('Ctrl Pts',(6.56268467750003,38.2492500034685,-5.80515448811441));
#23765=CARTESIAN_POINT('Ctrl Pts',(5.3093234328217,38.1222500034686,-4.08005073111972));
#23766=CARTESIAN_POINT('Ctrl Pts',(4.05596218814312,37.9952500034685,-2.35494697412514));
#23767=CARTESIAN_POINT('Ctrl Pts',(2.0279810940716,37.8682500034686,-1.69601597307323));
#23768=CARTESIAN_POINT('Ctrl Pts',(0.,37.7412500034685,-1.0370849720215));
#23769=CARTESIAN_POINT('Ctrl Pts',(-2.02798109407148,37.6142500034686,-1.69601597307323));
#23770=CARTESIAN_POINT('Ctrl Pts',(-4.05596218814312,37.4872500034686,-2.35494697412514));
#23771=CARTESIAN_POINT('Ctrl Pts',(-5.30932343282153,37.3602500034685,-4.08005073111972));
#23772=CARTESIAN_POINT('Ctrl Pts',(-6.56268467749997,37.2332500034686,-5.80515448811441));
#23773=CARTESIAN_POINT('Ctrl Pts',(-6.56268467749999,37.1062500034686,-7.93750000000004));
#23774=CARTESIAN_POINT('Ctrl Pts',(-6.56268467749997,36.9792500034686,-10.0698455118856));
#23775=CARTESIAN_POINT('Ctrl Pts',(-5.30932343282153,36.8522500034686,-11.7949492688803));
#23776=CARTESIAN_POINT('Ctrl Pts',(-4.05596218814306,36.7252500034685,-13.5200530258749));
#23777=CARTESIAN_POINT('Ctrl Pts',(-2.02798109407154,36.5982500034687,-14.1789840269267));
#23778=CARTESIAN_POINT('Ctrl Pts',(1.1673575708729E-13,36.4712500034686,
-14.8379150279786));
#23779=CARTESIAN_POINT('Ctrl Pts',(2.02798109407154,36.3442500034687,-14.1789840269267));
#23780=CARTESIAN_POINT('Ctrl Pts',(4.05596218814324,36.2172500034686,-13.5200530258749));
#23781=CARTESIAN_POINT('Ctrl Pts',(5.30932343282164,36.0902500034686,-11.7949492688803));
#23782=CARTESIAN_POINT('Ctrl Pts',(6.56268467750008,35.9632500034686,-10.0698455118856));
#23783=CARTESIAN_POINT('Ctrl Pts',(6.56268467749999,35.8362500034687,-7.93750000000004));
#23784=CARTESIAN_POINT('Origin',(-2.53888687851145E-9,74.888750003468,-7.9374999999999));
#23785=CARTESIAN_POINT('',(6.56268467750004,32.6612500034686,-7.93750000007101));
#23786=CARTESIAN_POINT('',(6.56268467750004,33.2962500034686,-7.93750000006994));
#23787=CARTESIAN_POINT('',(6.56268467242224,74.8887500034674,-7.93749999999981));
#23788=CARTESIAN_POINT('Ctrl Pts',(6.56268467749999,35.2012500034686,-7.93750000000004));
#23789=CARTESIAN_POINT('Ctrl Pts',(6.56268467749997,35.0742500034685,-5.80515448811441));
#23790=CARTESIAN_POINT('Ctrl Pts',(5.30932343282159,34.9472500034685,-4.08005073111972));
#23791=CARTESIAN_POINT('Ctrl Pts',(4.05596218814318,34.8202500034686,-2.35494697412514));
#23792=CARTESIAN_POINT('Ctrl Pts',(2.0279810940716,34.6932500034686,-1.69601597307323));
#23793=CARTESIAN_POINT('Ctrl Pts',(0.,34.5662500034686,-1.0370849720215));
#23794=CARTESIAN_POINT('Ctrl Pts',(-2.0279810940716,34.4392500034686,-1.69601597307323));
#23795=CARTESIAN_POINT('Ctrl Pts',(-4.05596218814318,34.3122500034686,-2.35494697412514));
#23796=CARTESIAN_POINT('Ctrl Pts',(-5.30932343282153,34.1852500034686,-4.08005073111972));
#23797=CARTESIAN_POINT('Ctrl Pts',(-6.56268467749997,34.0582500034686,-5.80515448811441));
#23798=CARTESIAN_POINT('Ctrl Pts',(-6.56268467749999,33.9312500034686,-7.93750000000004));
#23799=CARTESIAN_POINT('Ctrl Pts',(-6.56268467750003,33.8042500034686,-10.0698455118856));
#23800=CARTESIAN_POINT('Ctrl Pts',(-5.30932343282148,33.6772500034685,-11.7949492688803));
#23801=CARTESIAN_POINT('Ctrl Pts',(-4.05596218814306,33.5502500034685,-13.5200530258749));
#23802=CARTESIAN_POINT('Ctrl Pts',(-2.02798109407154,33.4232500034688,-14.1789840269267));
#23803=CARTESIAN_POINT('Ctrl Pts',(0.,33.2962500034685,-14.8379150279786));
#23804=CARTESIAN_POINT('Ctrl Pts',(2.02798109407165,33.1692500034688,-14.1789840269267));
#23805=CARTESIAN_POINT('Ctrl Pts',(4.05596218814318,33.0422500034686,-13.5200530258749));
#23806=CARTESIAN_POINT('Ctrl Pts',(5.30932343282159,32.9152500034686,-11.7949492688803));
#23807=CARTESIAN_POINT('Ctrl Pts',(6.56268467750003,32.7882500034685,-10.0698455118856));
#23808=CARTESIAN_POINT('Ctrl Pts',(6.56268467750004,32.6612500034686,-7.93750000000004));
#23809=CARTESIAN_POINT('Ctrl Pts',(6.56268467749999,35.8362500034687,-7.93750000000004));
#23810=CARTESIAN_POINT('Ctrl Pts',(6.56268467750003,35.7092500034686,-5.80515448811441));
#23811=CARTESIAN_POINT('Ctrl Pts',(5.30932343282159,35.5822500034686,-4.08005073111972));
#23812=CARTESIAN_POINT('Ctrl Pts',(4.05596218814312,35.4552500034686,-2.35494697412514));
#23813=CARTESIAN_POINT('Ctrl Pts',(2.0279810940716,35.3282500034686,-1.69601597307323));
#23814=CARTESIAN_POINT('Ctrl Pts',(5.83678785436452E-14,35.2012500034686,
-1.0370849720215));
#23815=CARTESIAN_POINT('Ctrl Pts',(-2.02798109407148,35.0742500034686,-1.69601597307323));
#23816=CARTESIAN_POINT('Ctrl Pts',(-4.05596218814312,34.9472500034686,-2.35494697412514));
#23817=CARTESIAN_POINT('Ctrl Pts',(-5.30932343282153,34.8202500034686,-4.08005073111972));
#23818=CARTESIAN_POINT('Ctrl Pts',(-6.56268467750003,34.6932500034686,-5.80515448811441));
#23819=CARTESIAN_POINT('Ctrl Pts',(-6.56268467749999,34.5662500034686,-7.93750000000004));
#23820=CARTESIAN_POINT('Ctrl Pts',(-6.56268467749997,34.4392500034686,-10.0698455118856));
#23821=CARTESIAN_POINT('Ctrl Pts',(-5.30932343282148,34.3122500034686,-11.7949492688803));
#23822=CARTESIAN_POINT('Ctrl Pts',(-4.05596218814312,34.1852500034684,-13.5200530258749));
#23823=CARTESIAN_POINT('Ctrl Pts',(-2.02798109407154,34.0582500034686,-14.1789840269267));
#23824=CARTESIAN_POINT('Ctrl Pts',(0.,33.9312500034685,-14.8379150279786));
#23825=CARTESIAN_POINT('Ctrl Pts',(2.0279810940716,33.8042500034687,-14.1789840269267));
#23826=CARTESIAN_POINT('Ctrl Pts',(4.05596218814312,33.6772500034686,-13.5200530258749));
#23827=CARTESIAN_POINT('Ctrl Pts',(5.30932343282164,33.5502500034686,-11.7949492688803));
#23828=CARTESIAN_POINT('Ctrl Pts',(6.56268467750008,33.4232500034685,-10.0698455118856));
#23829=CARTESIAN_POINT('Ctrl Pts',(6.56268467750004,33.2962500034686,-7.93750000000004));
#23830=CARTESIAN_POINT('Origin',(-2.53888687851145E-9,74.888750003468,-7.9374999999999));
#23831=CARTESIAN_POINT('',(6.5626846775001,30.1212500034686,-7.93750000007529));
#23832=CARTESIAN_POINT('',(6.56268467750004,30.7562500034686,-7.93750000007422));
#23833=CARTESIAN_POINT('',(6.56268467242224,74.8887500034674,-7.93749999999981));
#23834=CARTESIAN_POINT('Ctrl Pts',(6.56268467750004,32.6612500034686,-7.93750000000004));
#23835=CARTESIAN_POINT('Ctrl Pts',(6.56268467750008,32.5342500034685,-5.80515448811441));
#23836=CARTESIAN_POINT('Ctrl Pts',(5.30932343282159,32.4072500034686,-4.08005073111972));
#23837=CARTESIAN_POINT('Ctrl Pts',(4.05596218814318,32.2802500034685,-2.35494697412514));
#23838=CARTESIAN_POINT('Ctrl Pts',(2.02798109407165,32.1532500034687,-1.69601597307323));
#23839=CARTESIAN_POINT('Ctrl Pts',(0.,32.0262500034685,-1.0370849720215));
#23840=CARTESIAN_POINT('Ctrl Pts',(-2.02798109407154,31.8992500034685,-1.69601597307323));
#23841=CARTESIAN_POINT('Ctrl Pts',(-4.05596218814318,31.7722500034685,-2.35494697412514));
#23842=CARTESIAN_POINT('Ctrl Pts',(-5.30932343282148,31.6452500034686,-4.08005073111972));
#23843=CARTESIAN_POINT('Ctrl Pts',(-6.56268467749997,31.5182500034685,-5.80515448811441));
#23844=CARTESIAN_POINT('Ctrl Pts',(-6.56268467749999,31.3912500034687,-7.93750000000004));
#23845=CARTESIAN_POINT('Ctrl Pts',(-6.56268467750003,31.2642500034685,-10.0698455118856));
#23846=CARTESIAN_POINT('Ctrl Pts',(-5.30932343282148,31.1372500034686,-11.7949492688803));
#23847=CARTESIAN_POINT('Ctrl Pts',(-4.05596218814318,31.0102500034686,-13.5200530258749));
#23848=CARTESIAN_POINT('Ctrl Pts',(-2.0279810940716,30.8832500034687,-14.1789840269267));
#23849=CARTESIAN_POINT('Ctrl Pts',(0.,30.7562500034685,-14.8379150279786));
#23850=CARTESIAN_POINT('Ctrl Pts',(2.0279810940716,30.6292500034687,-14.1789840269267));
#23851=CARTESIAN_POINT('Ctrl Pts',(4.05596218814312,30.5022500034686,-13.5200530258749));
#23852=CARTESIAN_POINT('Ctrl Pts',(5.30932343282159,30.3752500034686,-11.7949492688803));
#23853=CARTESIAN_POINT('Ctrl Pts',(6.56268467750003,30.2482500034686,-10.0698455118856));
#23854=CARTESIAN_POINT('Ctrl Pts',(6.5626846775001,30.1212500034686,-7.93750000000004));
#23855=CARTESIAN_POINT('Ctrl Pts',(6.56268467750004,33.2962500034686,-7.93750000000004));
#23856=CARTESIAN_POINT('Ctrl Pts',(6.56268467749991,33.1692500034685,-5.80515448811441));
#23857=CARTESIAN_POINT('Ctrl Pts',(5.30932343282159,33.0422500034686,-4.08005073111972));
#23858=CARTESIAN_POINT('Ctrl Pts',(4.05596218814324,32.9152500034685,-2.35494697412514));
#23859=CARTESIAN_POINT('Ctrl Pts',(2.02798109407165,32.7882500034686,-1.69601597307323));
#23860=CARTESIAN_POINT('Ctrl Pts',(0.,32.6612500034685,-1.0370849720215));
#23861=CARTESIAN_POINT('Ctrl Pts',(-2.02798109407154,32.5342500034686,-1.69601597307323));
#23862=CARTESIAN_POINT('Ctrl Pts',(-4.05596218814312,32.4072500034686,-2.35494697412514));
#23863=CARTESIAN_POINT('Ctrl Pts',(-5.30932343282148,32.2802500034686,-4.08005073111972));
#23864=CARTESIAN_POINT('Ctrl Pts',(-6.56268467749991,32.1532500034685,-5.80515448811441));
#23865=CARTESIAN_POINT('Ctrl Pts',(-6.56268467749999,32.0262500034685,-7.93750000000004));
#23866=CARTESIAN_POINT('Ctrl Pts',(-6.56268467749997,31.8992500034685,-10.0698455118856));
#23867=CARTESIAN_POINT('Ctrl Pts',(-5.30932343282159,31.7722500034686,-11.7949492688803));
#23868=CARTESIAN_POINT('Ctrl Pts',(-4.05596218814312,31.6452500034686,-13.5200530258749));
#23869=CARTESIAN_POINT('Ctrl Pts',(-2.02798109407148,31.5182500034687,-14.1789840269267));
#23870=CARTESIAN_POINT('Ctrl Pts',(0.,31.3912500034685,-14.8379150279786));
#23871=CARTESIAN_POINT('Ctrl Pts',(2.0279810940716,31.2642500034687,-14.1789840269267));
#23872=CARTESIAN_POINT('Ctrl Pts',(4.05596218814312,31.1372500034686,-13.5200530258749));
#23873=CARTESIAN_POINT('Ctrl Pts',(5.30932343282159,31.0102500034686,-11.7949492688803));
#23874=CARTESIAN_POINT('Ctrl Pts',(6.56268467749997,30.8832500034686,-10.0698455118856));
#23875=CARTESIAN_POINT('Ctrl Pts',(6.56268467750004,30.7562500034686,-7.93750000000004));
#23876=CARTESIAN_POINT('Origin',(-2.53888687851145E-9,74.888750003468,-7.9374999999999));
#23877=CARTESIAN_POINT('',(6.5626846775001,27.5812500034686,-7.93750000007956));
#23878=CARTESIAN_POINT('',(6.56268467749999,28.2162500034686,-7.93750000007849));
#23879=CARTESIAN_POINT('',(6.56268467242224,74.8887500034674,-7.93749999999981));
#23880=CARTESIAN_POINT('Ctrl Pts',(6.5626846775001,30.1212500034686,-7.93750000000004));
#23881=CARTESIAN_POINT('Ctrl Pts',(6.56268467750003,29.9942500034686,-5.80515448811441));
#23882=CARTESIAN_POINT('Ctrl Pts',(5.30932343282159,29.8672500034686,-4.08005073111972));
#23883=CARTESIAN_POINT('Ctrl Pts',(4.05596218814318,29.7402500034686,-2.35494697412514));
#23884=CARTESIAN_POINT('Ctrl Pts',(2.02798109407165,29.6132500034686,-1.69601597307323));
#23885=CARTESIAN_POINT('Ctrl Pts',(0.,29.4862500034686,-1.0370849720215));
#23886=CARTESIAN_POINT('Ctrl Pts',(-2.02798109407154,29.3592500034686,-1.69601597307323));
#23887=CARTESIAN_POINT('Ctrl Pts',(-4.05596218814312,29.2322500034686,-2.35494697412503));
#23888=CARTESIAN_POINT('Ctrl Pts',(-5.30932343282159,29.1052500034686,-4.08005073111972));
#23889=CARTESIAN_POINT('Ctrl Pts',(-6.56268467749997,28.9782500034685,-5.80515448811441));
#23890=CARTESIAN_POINT('Ctrl Pts',(-6.56268467749993,28.8512500034686,-7.93750000000004));
#23891=CARTESIAN_POINT('Ctrl Pts',(-6.56268467750003,28.7242500034685,-10.0698455118856));
#23892=CARTESIAN_POINT('Ctrl Pts',(-5.30932343282159,28.5972500034687,-11.7949492688803));
#23893=CARTESIAN_POINT('Ctrl Pts',(-4.05596218814306,28.4702500034686,-13.5200530258749));
#23894=CARTESIAN_POINT('Ctrl Pts',(-2.0279810940716,28.3432500034687,-14.1789840269267));
#23895=CARTESIAN_POINT('Ctrl Pts',(1.1673575708729E-13,28.2162500034685,
-14.8379150279786));
#23896=CARTESIAN_POINT('Ctrl Pts',(2.0279810940716,28.0892500034687,-14.1789840269267));
#23897=CARTESIAN_POINT('Ctrl Pts',(4.05596218814324,27.9622500034685,-13.5200530258749));
#23898=CARTESIAN_POINT('Ctrl Pts',(5.30932343282159,27.8352500034685,-11.7949492688803));
#23899=CARTESIAN_POINT('Ctrl Pts',(6.56268467750003,27.7082500034685,-10.0698455118856));
#23900=CARTESIAN_POINT('Ctrl Pts',(6.5626846775001,27.5812500034686,-7.93750000000004));
#23901=CARTESIAN_POINT('Ctrl Pts',(6.56268467750004,30.7562500034686,-7.93750000000004));
#23902=CARTESIAN_POINT('Ctrl Pts',(6.56268467750003,30.6292500034685,-5.80515448811441));
#23903=CARTESIAN_POINT('Ctrl Pts',(5.30932343282159,30.5022500034686,-4.08005073111972));
#23904=CARTESIAN_POINT('Ctrl Pts',(4.05596218814312,30.3752500034686,-2.35494697412514));
#23905=CARTESIAN_POINT('Ctrl Pts',(2.02798109407154,30.2482500034685,-1.69601597307323));
#23906=CARTESIAN_POINT('Ctrl Pts',(0.,30.1212500034685,-1.0370849720215));
#23907=CARTESIAN_POINT('Ctrl Pts',(-2.02798109407154,29.9942500034686,-1.69601597307323));
#23908=CARTESIAN_POINT('Ctrl Pts',(-4.05596218814312,29.8672500034686,-2.35494697412503));
#23909=CARTESIAN_POINT('Ctrl Pts',(-5.30932343282148,29.7402500034687,-4.08005073111972));
#23910=CARTESIAN_POINT('Ctrl Pts',(-6.56268467750003,29.6132500034685,-5.80515448811441));
#23911=CARTESIAN_POINT('Ctrl Pts',(-6.56268467749993,29.4862500034685,-7.93750000000004));
#23912=CARTESIAN_POINT('Ctrl Pts',(-6.56268467749997,29.3592500034685,-10.0698455118856));
#23913=CARTESIAN_POINT('Ctrl Pts',(-5.30932343282159,29.2322500034685,-11.7949492688803));
#23914=CARTESIAN_POINT('Ctrl Pts',(-4.05596218814312,29.1052500034686,-13.5200530258749));
#23915=CARTESIAN_POINT('Ctrl Pts',(-2.02798109407148,28.9782500034687,-14.1789840269267));
#23916=CARTESIAN_POINT('Ctrl Pts',(0.,28.8512500034685,-14.8379150279786));
#23917=CARTESIAN_POINT('Ctrl Pts',(2.0279810940716,28.7242500034687,-14.1789840269267));
#23918=CARTESIAN_POINT('Ctrl Pts',(4.05596218814318,28.5972500034685,-13.5200530258749));
#23919=CARTESIAN_POINT('Ctrl Pts',(5.30932343282159,28.4702500034686,-11.7949492688803));
#23920=CARTESIAN_POINT('Ctrl Pts',(6.56268467750008,28.3432500034685,-10.0698455118856));
#23921=CARTESIAN_POINT('Ctrl Pts',(6.56268467749999,28.2162500034686,-7.93750000000004));
#23922=CARTESIAN_POINT('Origin',(-2.53888687851145E-9,74.888750003468,-7.9374999999999));
#23923=CARTESIAN_POINT('',(6.5626846775001,25.0412500034685,-7.93750000008384));
#23924=CARTESIAN_POINT('',(6.56268467749999,25.6762500034685,-7.93750000008277));
#23925=CARTESIAN_POINT('',(6.56268467242224,74.8887500034674,-7.93749999999981));
#23926=CARTESIAN_POINT('Ctrl Pts',(6.5626846775001,27.5812500034686,-7.93750000000004));
#23927=CARTESIAN_POINT('Ctrl Pts',(6.56268467750003,27.4542500034686,-5.80515448811441));
#23928=CARTESIAN_POINT('Ctrl Pts',(5.30932343282153,27.3272500034686,-4.08005073111972));
#23929=CARTESIAN_POINT('Ctrl Pts',(4.05596218814312,27.2002500034686,-2.35494697412514));
#23930=CARTESIAN_POINT('Ctrl Pts',(2.02798109407165,27.0732500034686,-1.69601597307323));
#23931=CARTESIAN_POINT('Ctrl Pts',(1.1673575708729E-13,26.9462500034685,
-1.0370849720215));
#23932=CARTESIAN_POINT('Ctrl Pts',(-2.02798109407148,26.8192500034686,-1.69601597307323));
#23933=CARTESIAN_POINT('Ctrl Pts',(-4.05596218814312,26.6922500034685,-2.35494697412503));
#23934=CARTESIAN_POINT('Ctrl Pts',(-5.30932343282159,26.5652500034685,-4.08005073111972));
#23935=CARTESIAN_POINT('Ctrl Pts',(-6.56268467750008,26.4382500034685,-5.80515448811441));
#23936=CARTESIAN_POINT('Ctrl Pts',(-6.56268467750004,26.3112500034686,-7.93750000000004));
#23937=CARTESIAN_POINT('Ctrl Pts',(-6.56268467749997,26.1842500034686,-10.0698455118856));
#23938=CARTESIAN_POINT('Ctrl Pts',(-5.30932343282159,26.0572500034686,-11.7949492688803));
#23939=CARTESIAN_POINT('Ctrl Pts',(-4.05596218814318,25.9302500034685,-13.5200530258749));
#23940=CARTESIAN_POINT('Ctrl Pts',(-2.0279810940716,25.8032500034687,-14.1789840269267));
#23941=CARTESIAN_POINT('Ctrl Pts',(0.,25.6762500034686,-14.8379150279786));
#23942=CARTESIAN_POINT('Ctrl Pts',(2.02798109407165,25.5492500034687,-14.1789840269267));
#23943=CARTESIAN_POINT('Ctrl Pts',(4.05596218814312,25.4222500034686,-13.5200530258749));
#23944=CARTESIAN_POINT('Ctrl Pts',(5.30932343282153,25.2952500034686,-11.7949492688803));
#23945=CARTESIAN_POINT('Ctrl Pts',(6.56268467750008,25.1682500034686,-10.0698455118856));
#23946=CARTESIAN_POINT('Ctrl Pts',(6.5626846775001,25.0412500034685,-7.93750000000004));
#23947=CARTESIAN_POINT('Ctrl Pts',(6.56268467749999,28.2162500034686,-7.93750000000004));
#23948=CARTESIAN_POINT('Ctrl Pts',(6.56268467749997,28.0892500034686,-5.80515448811441));
#23949=CARTESIAN_POINT('Ctrl Pts',(5.30932343282164,27.9622500034686,-4.08005073111972));
#23950=CARTESIAN_POINT('Ctrl Pts',(4.05596218814312,27.8352500034686,-2.35494697412514));
#23951=CARTESIAN_POINT('Ctrl Pts',(2.02798109407154,27.7082500034687,-1.69601597307323));
#23952=CARTESIAN_POINT('Ctrl Pts',(0.,27.5812500034685,-1.0370849720215));
#23953=CARTESIAN_POINT('Ctrl Pts',(-2.02798109407148,27.4542500034686,-1.69601597307323));
#23954=CARTESIAN_POINT('Ctrl Pts',(-4.05596218814312,27.3272500034686,-2.35494697412503));
#23955=CARTESIAN_POINT('Ctrl Pts',(-5.30932343282159,27.2002500034686,-4.08005073111972));
#23956=CARTESIAN_POINT('Ctrl Pts',(-6.56268467750003,27.0732500034685,-5.80515448811441));
#23957=CARTESIAN_POINT('Ctrl Pts',(-6.56268467749993,26.9462500034687,-7.93750000000004));
#23958=CARTESIAN_POINT('Ctrl Pts',(-6.56268467749991,26.8192500034686,-10.0698455118856));
#23959=CARTESIAN_POINT('Ctrl Pts',(-5.30932343282159,26.6922500034685,-11.7949492688803));
#23960=CARTESIAN_POINT('Ctrl Pts',(-4.05596218814312,26.5652500034685,-13.5200530258749));
#23961=CARTESIAN_POINT('Ctrl Pts',(-2.02798109407148,26.4382500034687,-14.1789840269267));
#23962=CARTESIAN_POINT('Ctrl Pts',(0.,26.3112500034686,-14.8379150279786));
#23963=CARTESIAN_POINT('Ctrl Pts',(2.02798109407165,26.1842500034687,-14.1789840269267));
#23964=CARTESIAN_POINT('Ctrl Pts',(4.05596218814318,26.0572500034686,-13.5200530258749));
#23965=CARTESIAN_POINT('Ctrl Pts',(5.30932343282159,25.9302500034686,-11.7949492688803));
#23966=CARTESIAN_POINT('Ctrl Pts',(6.56268467750003,25.8032500034686,-10.0698455118856));
#23967=CARTESIAN_POINT('Ctrl Pts',(6.56268467749999,25.6762500034685,-7.93750000000004));
#23968=CARTESIAN_POINT('Origin',(-2.53888687851145E-9,74.888750003468,-7.9374999999999));
#23969=CARTESIAN_POINT('',(6.5626846775001,22.5012500034686,-7.93750000008812));
#23970=CARTESIAN_POINT('',(6.56268467749999,23.1362500034686,-7.93750000008705));
#23971=CARTESIAN_POINT('',(6.56268467242224,74.8887500034674,-7.93749999999981));
#23972=CARTESIAN_POINT('Ctrl Pts',(6.5626846775001,25.0412500034685,-7.93750000000004));
#23973=CARTESIAN_POINT('Ctrl Pts',(6.56268467750003,24.9142500034686,-5.80515448811441));
#23974=CARTESIAN_POINT('Ctrl Pts',(5.30932343282153,24.7872500034686,-4.08005073111972));
#23975=CARTESIAN_POINT('Ctrl Pts',(4.05596218814324,24.6602500034686,-2.35494697412514));
#23976=CARTESIAN_POINT('Ctrl Pts',(2.02798109407171,24.5332500034686,-1.69601597307323));
#23977=CARTESIAN_POINT('Ctrl Pts',(0.,24.4062500034686,-1.0370849720215));
#23978=CARTESIAN_POINT('Ctrl Pts',(-2.0279810940716,24.2792500034685,-1.69601597307323));
#23979=CARTESIAN_POINT('Ctrl Pts',(-4.05596218814312,24.1522500034685,-2.35494697412503));
#23980=CARTESIAN_POINT('Ctrl Pts',(-5.30932343282159,24.0252500034685,-4.08005073111972));
#23981=CARTESIAN_POINT('Ctrl Pts',(-6.56268467749991,23.8982500034686,-5.80515448811441));
#23982=CARTESIAN_POINT('Ctrl Pts',(-6.56268467749999,23.7712500034686,-7.93750000000004));
#23983=CARTESIAN_POINT('Ctrl Pts',(-6.56268467749997,23.6442500034686,-10.0698455118856));
#23984=CARTESIAN_POINT('Ctrl Pts',(-5.30932343282164,23.5172500034686,-11.7949492688803));
#23985=CARTESIAN_POINT('Ctrl Pts',(-4.05596218814312,23.3902500034686,-13.5200530258749));
#23986=CARTESIAN_POINT('Ctrl Pts',(-2.02798109407154,23.2632500034686,-14.1789840269267));
#23987=CARTESIAN_POINT('Ctrl Pts',(0.,23.1362500034685,-14.8379150279786));
#23988=CARTESIAN_POINT('Ctrl Pts',(2.02798109407165,23.0092500034686,-14.1789840269267));
#23989=CARTESIAN_POINT('Ctrl Pts',(4.05596218814312,22.8822500034685,-13.5200530258749));
#23990=CARTESIAN_POINT('Ctrl Pts',(5.30932343282153,22.7552500034686,-11.7949492688803));
#23991=CARTESIAN_POINT('Ctrl Pts',(6.56268467749997,22.6282500034686,-10.0698455118856));
#23992=CARTESIAN_POINT('Ctrl Pts',(6.5626846775001,22.5012500034686,-7.93750000000004));
#23993=CARTESIAN_POINT('Ctrl Pts',(6.56268467749999,25.6762500034685,-7.93750000000004));
#23994=CARTESIAN_POINT('Ctrl Pts',(6.56268467749997,25.5492500034686,-5.80515448811441));
#23995=CARTESIAN_POINT('Ctrl Pts',(5.30932343282164,25.4222500034686,-4.08005073111972));
#23996=CARTESIAN_POINT('Ctrl Pts',(4.05596218814312,25.2952500034686,-2.35494697412514));
#23997=CARTESIAN_POINT('Ctrl Pts',(2.0279810940716,25.1682500034687,-1.69601597307323));
#23998=CARTESIAN_POINT('Ctrl Pts',(0.,25.0412500034686,-1.0370849720215));
#23999=CARTESIAN_POINT('Ctrl Pts',(-2.02798109407148,24.9142500034685,-1.69601597307323));
#24000=CARTESIAN_POINT('Ctrl Pts',(-4.05596218814318,24.7872500034685,-2.35494697412503));
#24001=CARTESIAN_POINT('Ctrl Pts',(-5.30932343282159,24.6602500034686,-4.08005073111972));
#24002=CARTESIAN_POINT('Ctrl Pts',(-6.56268467750003,24.5332500034686,-5.80515448811441));
#24003=CARTESIAN_POINT('Ctrl Pts',(-6.56268467749987,24.4062500034686,-7.93750000000004));
#24004=CARTESIAN_POINT('Ctrl Pts',(-6.56268467750003,24.2792500034686,-10.0698455118856));
#24005=CARTESIAN_POINT('Ctrl Pts',(-5.30932343282153,24.1522500034687,-11.7949492688803));
#24006=CARTESIAN_POINT('Ctrl Pts',(-4.05596218814324,24.0252500034686,-13.5200530258749));
#24007=CARTESIAN_POINT('Ctrl Pts',(-2.02798109407154,23.8982500034687,-14.1789840269267));
#24008=CARTESIAN_POINT('Ctrl Pts',(0.,23.7712500034685,-14.8379150279786));
#24009=CARTESIAN_POINT('Ctrl Pts',(2.02798109407154,23.6442500034687,-14.1789840269267));
#24010=CARTESIAN_POINT('Ctrl Pts',(4.05596218814318,23.5172500034685,-13.5200530258749));
#24011=CARTESIAN_POINT('Ctrl Pts',(5.30932343282164,23.3902500034686,-11.7949492688803));
#24012=CARTESIAN_POINT('Ctrl Pts',(6.56268467750003,23.2632500034686,-10.0698455118856));
#24013=CARTESIAN_POINT('Ctrl Pts',(6.56268467749999,23.1362500034686,-7.93750000000004));
#24014=CARTESIAN_POINT('Origin',(-2.53888687851145E-9,74.888750003468,-7.9374999999999));
#24015=CARTESIAN_POINT('',(6.56268467749999,19.9612500034686,-7.93750000009239));
#24016=CARTESIAN_POINT('',(6.56268467749999,20.5962500034686,-7.93750000009132));
#24017=CARTESIAN_POINT('',(6.56268467242224,74.8887500034674,-7.93749999999981));
#24018=CARTESIAN_POINT('Ctrl Pts',(6.5626846775001,22.5012500034686,-7.93750000000004));
#24019=CARTESIAN_POINT('Ctrl Pts',(6.56268467750003,22.3742500034686,-5.80515448811441));
#24020=CARTESIAN_POINT('Ctrl Pts',(5.30932343282159,22.2472500034686,-4.08005073111972));
#24021=CARTESIAN_POINT('Ctrl Pts',(4.05596218814312,22.1202500034686,-2.35494697412503));
#24022=CARTESIAN_POINT('Ctrl Pts',(2.0279810940716,21.9932500034685,-1.69601597307323));
#24023=CARTESIAN_POINT('Ctrl Pts',(0.,21.8662500034686,-1.0370849720215));
#24024=CARTESIAN_POINT('Ctrl Pts',(-2.0279810940716,21.7392500034686,-1.69601597307323));
#24025=CARTESIAN_POINT('Ctrl Pts',(-4.05596218814312,21.6122500034686,-2.35494697412503));
#24026=CARTESIAN_POINT('Ctrl Pts',(-5.30932343282153,21.4852500034687,-4.08005073111972));
#24027=CARTESIAN_POINT('Ctrl Pts',(-6.56268467750003,21.3582500034686,-5.80515448811441));
#24028=CARTESIAN_POINT('Ctrl Pts',(-6.56268467749999,21.2312500034685,-7.93750000000004));
#24029=CARTESIAN_POINT('Ctrl Pts',(-6.56268467749997,21.1042500034685,-10.0698455118856));
#24030=CARTESIAN_POINT('Ctrl Pts',(-5.30932343282164,20.9772500034686,-11.7949492688803));
#24031=CARTESIAN_POINT('Ctrl Pts',(-4.05596218814312,20.8502500034685,-13.5200530258749));
#24032=CARTESIAN_POINT('Ctrl Pts',(-2.02798109407154,20.7232500034687,-14.1789840269267));
#24033=CARTESIAN_POINT('Ctrl Pts',(0.,20.5962500034686,-14.8379150279786));
#24034=CARTESIAN_POINT('Ctrl Pts',(2.02798109407171,20.4692500034686,-14.1789840269267));
#24035=CARTESIAN_POINT('Ctrl Pts',(4.05596218814324,20.3422500034686,-13.5200530258749));
#24036=CARTESIAN_POINT('Ctrl Pts',(5.30932343282159,20.2152500034686,-11.7949492688803));
#24037=CARTESIAN_POINT('Ctrl Pts',(6.56268467750008,20.0882500034686,-10.0698455118856));
#24038=CARTESIAN_POINT('Ctrl Pts',(6.56268467749999,19.9612500034686,-7.93750000000004));
#24039=CARTESIAN_POINT('Ctrl Pts',(6.56268467749999,23.1362500034686,-7.93750000000004));
#24040=CARTESIAN_POINT('Ctrl Pts',(6.56268467750008,23.0092500034686,-5.80515448811441));
#24041=CARTESIAN_POINT('Ctrl Pts',(5.3093234328217,22.8822500034686,-4.08005073111972));
#24042=CARTESIAN_POINT('Ctrl Pts',(4.05596218814318,22.7552500034685,-2.35494697412503));
#24043=CARTESIAN_POINT('Ctrl Pts',(2.0279810940716,22.6282500034686,-1.69601597307323));
#24044=CARTESIAN_POINT('Ctrl Pts',(-1.1673575708729E-13,22.5012500034685,
-1.0370849720215));
#24045=CARTESIAN_POINT('Ctrl Pts',(-2.02798109407148,22.3742500034686,-1.69601597307323));
#24046=CARTESIAN_POINT('Ctrl Pts',(-4.05596218814306,22.2472500034686,-2.35494697412503));
#24047=CARTESIAN_POINT('Ctrl Pts',(-5.30932343282153,22.1202500034686,-4.08005073111972));
#24048=CARTESIAN_POINT('Ctrl Pts',(-6.56268467749997,21.9932500034685,-5.80515448811441));
#24049=CARTESIAN_POINT('Ctrl Pts',(-6.56268467749987,21.8662500034686,-7.93750000000004));
#24050=CARTESIAN_POINT('Ctrl Pts',(-6.56268467750003,21.7392500034685,-10.0698455118856));
#24051=CARTESIAN_POINT('Ctrl Pts',(-5.30932343282153,21.6122500034686,-11.7949492688803));
#24052=CARTESIAN_POINT('Ctrl Pts',(-4.05596218814318,21.4852500034685,-13.5200530258749));
#24053=CARTESIAN_POINT('Ctrl Pts',(-2.02798109407154,21.3582500034687,-14.1789840269267));
#24054=CARTESIAN_POINT('Ctrl Pts',(0.,21.2312500034686,-14.8379150279786));
#24055=CARTESIAN_POINT('Ctrl Pts',(2.02798109407154,21.1042500034687,-14.1789840269267));
#24056=CARTESIAN_POINT('Ctrl Pts',(4.05596218814312,20.9772500034685,-13.5200530258749));
#24057=CARTESIAN_POINT('Ctrl Pts',(5.30932343282164,20.8502500034686,-11.7949492688803));
#24058=CARTESIAN_POINT('Ctrl Pts',(6.56268467749991,20.7232500034686,-10.0698455118856));
#24059=CARTESIAN_POINT('Ctrl Pts',(6.56268467749999,20.5962500034686,-7.93750000000004));
#24060=CARTESIAN_POINT('Origin',(0.,-18.001,-7.93750000000004));
#24061=CARTESIAN_POINT('',(5.51611152846815E-15,22.3425000069372,-15.875));
#24062=CARTESIAN_POINT('',(-1.63067097993201E-14,22.0250000000001,-15.875));
#24063=CARTESIAN_POINT('',(-9.72063396823211E-16,-18.001,-15.875));
#24064=CARTESIAN_POINT('',(-4.09425652844336E-15,19.8025000069372,-15.875));
#24065=CARTESIAN_POINT('Ctrl Pts',(6.78623823802127E-14,22.3425000069372,
-15.875));
#24066=CARTESIAN_POINT('Ctrl Pts',(0.395040178672521,22.3220459769847,-15.875));
#24067=CARTESIAN_POINT('Ctrl Pts',(0.790420497079234,22.3015743355874,-15.8455096666082));
#24068=CARTESIAN_POINT('Ctrl Pts',(2.1991001059612,22.2286370080217,-15.6332224193839));
#24069=CARTESIAN_POINT('Ctrl Pts',(3.17598716825989,22.1790490668691,-15.2841499417528));
#24070=CARTESIAN_POINT('Ctrl Pts',(4.94518932437667,22.0728978141893,-14.23130929533));
#24071=CARTESIAN_POINT('Ctrl Pts',(5.7200870922735,22.0192899177241,-13.5364058840881));
#24072=CARTESIAN_POINT('Ctrl Pts',(6.97199703691789,21.9162606926934,-11.8741577819405));
#24073=CARTESIAN_POINT('Ctrl Pts',(7.43104000941119,21.8623942176982,-10.9184524179978));
#24074=CARTESIAN_POINT('Ctrl Pts',(7.94396663586668,21.7552586174882,-8.90945821440764));
#24075=CARTESIAN_POINT('Ctrl Pts',(8.00298850093494,21.7056272144354,-7.87818979799516));
#24076=CARTESIAN_POINT('Ctrl Pts',(7.7239878463525,21.6004972097071,-5.8339170308497));
#24077=CARTESIAN_POINT('Ctrl Pts',(7.38230828412897,21.5461497170984,-4.84127477607674));
#24078=CARTESIAN_POINT('Ctrl Pts',(6.33810938427407,21.4411549811571,-3.04837695866961));
#24079=CARTESIAN_POINT('Ctrl Pts',(5.64728214551277,21.3904042997954,-2.26446263971475));
#24080=CARTESIAN_POINT('Ctrl Pts',(4.01126411610705,21.2837505722391,-1.01179935196314));
#24081=CARTESIAN_POINT('Ctrl Pts',(3.08389896379364,21.2321753138586,-0.552044436971875));
#24082=CARTESIAN_POINT('Ctrl Pts',(1.0831538814182,21.128582560383,-0.00460559803268347));
#24083=CARTESIAN_POINT('Ctrl Pts',(0.0266016197439578,21.073877361334,0.0689460350682048));
#24084=CARTESIAN_POINT('Ctrl Pts',(-2.03128985394184,20.9673257341474,-0.196013908491485));
#24085=CARTESIAN_POINT('Ctrl Pts',(-3.0139353749126,20.9178982618204,-0.523126647845116));
#24086=CARTESIAN_POINT('Ctrl Pts',(-4.80649912410774,20.8119606880915,-1.53679171539507));
#24087=CARTESIAN_POINT('Ctrl Pts',(-5.59803512166624,20.7581284717844,-2.21616531313947));
#24088=CARTESIAN_POINT('Ctrl Pts',(-6.88378103002077,20.6545571854372,-3.84965336274376));
#24089=CARTESIAN_POINT('Ctrl Pts',(-7.36182078278323,20.6016562035522,-4.79095067020299));
#24090=CARTESIAN_POINT('Ctrl Pts',(-7.91952396519374,20.4946248469775,-6.78327916318912));
#24091=CARTESIAN_POINT('Ctrl Pts',(-8.00222222662397,20.4446754667674,-7.81281401194153));
#24092=CARTESIAN_POINT('Ctrl Pts',(-7.77007008099423,20.3398966932697,-9.86517616083676));
#24093=CARTESIAN_POINT('Ctrl Pts',(-7.45014540239196,20.2854176146861,-10.8675591854763));
#24094=CARTESIAN_POINT('Ctrl Pts',(-6.44616960099415,20.1799757855807,-12.6826056157578));
#24095=CARTESIAN_POINT('Ctrl Pts',(-5.77523755495239,20.1297467344383,-13.4796773377977));
#24096=CARTESIAN_POINT('Ctrl Pts',(-4.16975728145562,20.0232505572233,-14.7691954209118));
#24097=CARTESIAN_POINT('Ctrl Pts',(-3.25170674616548,19.9708639121129,-15.2508444363837));
#24098=CARTESIAN_POINT('Ctrl Pts',(-1.5302325047701,19.8817309894461,-15.7640055967039));
#24099=CARTESIAN_POINT('Ctrl Pts',(-0.766355811038719,19.8421796789287,
-15.875));
#24100=CARTESIAN_POINT('Ctrl Pts',(1.70696790036118E-14,19.8025000069371,
-15.875));
#24101=CARTESIAN_POINT('',(5.55111512312578E-14,18.0000000000001,-15.875));
#24102=CARTESIAN_POINT('',(-9.72063396823211E-16,-18.001,-15.875));
#24103=CARTESIAN_POINT('',(-4.29373077449685,18.819869818891,-14.6134105960265));
#24104=CARTESIAN_POINT('Ctrl Pts',(-9.72063396823211E-16,18.0000000000001,
-15.875));
#24105=CARTESIAN_POINT('Ctrl Pts',(-0.152276681747816,18.072084637752,-15.875));
#24106=CARTESIAN_POINT('Ctrl Pts',(-0.305855934339734,18.1421428142786,
-15.8706141374141));
#24107=CARTESIAN_POINT('Ctrl Pts',(-0.460325988668671,18.2094023441906,
-15.8616407252873));
#24108=CARTESIAN_POINT('Ctrl Pts',(-0.614082443016771,18.2763511575726,
-15.8527087673229));
#24109=CARTESIAN_POINT('Ctrl Pts',(-0.768721127003723,18.3405271222359,
-15.8392313687975));
#24110=CARTESIAN_POINT('Ctrl Pts',(-0.923815417265365,18.4011687051435,
-15.8210570223614));
#24111=CARTESIAN_POINT('Ctrl Pts',(-0.976648961750814,18.4218265240923,
-15.8148658522074));
#24112=CARTESIAN_POINT('Ctrl Pts',(-1.02953522580605,18.4420741943477,-15.8081300413038));
#24113=CARTESIAN_POINT('Ctrl Pts',(-1.08245691517555,18.4618816114692,-15.80084491656));
#24114=CARTESIAN_POINT('Ctrl Pts',(-1.21556599724492,18.5117013950516,-15.7825213090001));
#24115=CARTESIAN_POINT('Ctrl Pts',(-1.34862695113583,18.5587255077166,-15.7607646847442));
#24116=CARTESIAN_POINT('Ctrl Pts',(-1.4817395657411,18.6025368983511,-15.7354711534038));
#24117=CARTESIAN_POINT('Ctrl Pts',(-1.6130840260593,18.6457663358896,-15.7105135997317));
#24118=CARTESIAN_POINT('Ctrl Pts',(-1.74447921274838,18.6858678346499,-15.6821123226063));
#24119=CARTESIAN_POINT('Ctrl Pts',(-1.87600132923871,18.7224407429927,-15.650121166808));
#24120=CARTESIAN_POINT('Ctrl Pts',(-1.976037833142,18.7502583145603,-15.6257885034714));
#24121=CARTESIAN_POINT('Ctrl Pts',(-2.07614742951161,18.7760345210388,-15.5993780730588));
#24122=CARTESIAN_POINT('Ctrl Pts',(-2.17635351087789,18.7995930649607,-15.5708080407966));
#24123=CARTESIAN_POINT('Ctrl Pts',(-2.27056963336782,18.8217433639203,-15.5439458222321));
#24124=CARTESIAN_POINT('Ctrl Pts',(-2.36523835232703,18.8419415753925,-15.5150640314883));
#24125=CARTESIAN_POINT('Ctrl Pts',(-2.45994739338429,18.8598808531924,-15.4841923265615));
#24126=CARTESIAN_POINT('Ctrl Pts',(-2.55421906742611,18.8777372872817,-15.4534631873845));
#24127=CARTESIAN_POINT('Ctrl Pts',(-2.6485303701587,18.8933556030678,-15.4207624788507));
#24128=CARTESIAN_POINT('Ctrl Pts',(-2.74248535327406,18.9064331858182,-15.3861697025092));
#24129=CARTESIAN_POINT('Ctrl Pts',(-2.83620349346052,18.9194778024299,-15.3516641280828));
#24130=CARTESIAN_POINT('Ctrl Pts',(-2.92956679712358,18.9299944792857,-15.3152760826183));
#24131=CARTESIAN_POINT('Ctrl Pts',(-3.02219766183718,18.9376828843945,-15.2771340196761));
#24132=CARTESIAN_POINT('Ctrl Pts',(-3.10530581747077,18.9445809001944,-15.2429130662931));
#24133=CARTESIAN_POINT('Ctrl Pts',(-3.18782444335918,18.9492022622311,-15.207280908227));
#24134=CARTESIAN_POINT('Ctrl Pts',(-3.26949439648287,18.9513300675967,-15.1703633777618));
#24135=CARTESIAN_POINT('Ctrl Pts',(-3.42087322908613,18.9552740479707,-15.1019351192571));
#24136=CARTESIAN_POINT('Ctrl Pts',(-3.56980099384897,18.9508507374213,-15.0288961392634));
#24137=CARTESIAN_POINT('Ctrl Pts',(-3.71625969440135,18.936539439914,-14.9512949880053));
#24138=CARTESIAN_POINT('Ctrl Pts',(-3.74184003411462,18.9340398420711,-14.9377412434764));
#24139=CARTESIAN_POINT('Ctrl Pts',(-3.76734500463074,18.9312386033842,-14.9240482072849));
#24140=CARTESIAN_POINT('Ctrl Pts',(-3.79277444384613,18.9281276214137,-14.9102159893479));
#24141=CARTESIAN_POINT('Ctrl Pts',(-3.86447430656435,18.9193560170414,-14.8712152029456));
#24142=CARTESIAN_POINT('Ctrl Pts',(-3.93577353808586,18.9080524652382,-14.8309942492684));
#24143=CARTESIAN_POINT('Ctrl Pts',(-4.00627785537239,18.8940495030155,-14.7897729072588));
#24144=CARTESIAN_POINT('Ctrl Pts',(-4.07705725420642,18.8799919064573,-14.7483907349485));
#24145=CARTESIAN_POINT('Ctrl Pts',(-4.1470352971761,18.863213794202,-14.7060004943228));
#24146=CARTESIAN_POINT('Ctrl Pts',(-4.21584055455469,18.8435457354691,-14.6628694819372));
#24147=CARTESIAN_POINT('Ctrl Pts',(-4.24197933063924,18.8360739374871,-14.6464842242113));
#24148=CARTESIAN_POINT('Ctrl Pts',(-4.26794914936831,18.8281850617291,-14.6299925073087));
#24149=CARTESIAN_POINT('Ctrl Pts',(-4.29373077449686,18.819869818891,-14.6134105960265));
#24150=CARTESIAN_POINT('',(-4.29373077449685,18.8198698188908,-1.26158940397347));
#24151=CARTESIAN_POINT('Ctrl Pts',(-4.29373077449685,18.819869818891,-14.6134105960265));
#24152=CARTESIAN_POINT('Ctrl Pts',(-4.52296127969864,18.7459370342071,-14.4659769148109));
#24153=CARTESIAN_POINT('Ctrl Pts',(-4.74196146019457,18.6690215823314,-14.3087480538926));
#24154=CARTESIAN_POINT('Ctrl Pts',(-4.95124940477097,18.5902365316974,-14.1417968955388));
#24155=CARTESIAN_POINT('Ctrl Pts',(-5.16682135147801,18.5090859103801,-13.969832923681));
#24156=CARTESIAN_POINT('Ctrl Pts',(-5.37208902136478,18.4259511228614,-13.7875541699567));
#24157=CARTESIAN_POINT('Ctrl Pts',(-5.56758051682947,18.3420322638492,-13.5950037064242));
#24158=CARTESIAN_POINT('Ctrl Pts',(-5.64332797487214,18.3095160654493,-13.5203958155651));
#24159=CARTESIAN_POINT('Ctrl Pts',(-5.71760730096738,18.2768820318798,-13.4442453974143));
#24160=CARTESIAN_POINT('Ctrl Pts',(-5.79044777763095,18.2441996606711,-13.3665534898537));
#24161=CARTESIAN_POINT('Ctrl Pts',(-5.79212935934825,18.2434451615187,-13.3647599089037));
#24162=CARTESIAN_POINT('Ctrl Pts',(-5.79381016993235,18.2426906385331,-13.3629655109143));
#24163=CARTESIAN_POINT('Ctrl Pts',(-5.79549020982549,18.2419360925352,-13.3611702958253));
#24164=CARTESIAN_POINT('Ctrl Pts',(-5.94895048266734,18.1730134227974,-13.1971895484084));
#24165=CARTESIAN_POINT('Ctrl Pts',(-6.09643741101815,18.1036131389403,-13.0255265848449));
#24166=CARTESIAN_POINT('Ctrl Pts',(-6.23662479546188,18.0350900642456,-12.847493578081));
#24167=CARTESIAN_POINT('Ctrl Pts',(-6.29721400015929,18.0054742852249,-12.7705474367965));
#24168=CARTESIAN_POINT('Ctrl Pts',(-6.35643920688128,17.976022390356,-12.6924109203825));
#24169=CARTESIAN_POINT('Ctrl Pts',(-6.41419086511951,17.9468442552088,-12.6131882492251));
#24170=CARTESIAN_POINT('Ctrl Pts',(-6.41654032136253,17.9456572286563,-12.6099653080141));
#24171=CARTESIAN_POINT('Ctrl Pts',(-6.41888732415843,17.9444706625728,-12.6067405888829));
#24172=CARTESIAN_POINT('Ctrl Pts',(-6.42123186600278,17.9432845644396,-12.6035140991033));
#24173=CARTESIAN_POINT('Ctrl Pts',(-6.56679359836233,17.8696452308427,-12.4031963087054));
#24174=CARTESIAN_POINT('Ctrl Pts',(-6.70230659924676,17.7981518448594,-12.1970951577147));
#24175=CARTESIAN_POINT('Ctrl Pts',(-6.82801702228201,17.7297067509173,-11.9849986789165));
#24176=CARTESIAN_POINT('Ctrl Pts',(-6.86647149527177,17.7087695847482,-11.9201189488333));
#24177=CARTESIAN_POINT('Ctrl Pts',(-6.90400842021663,17.6881177916409,-11.8546780384769));
#24178=CARTESIAN_POINT('Ctrl Pts',(-6.94063408540422,17.6677776026631,-11.7886694036638));
#24179=CARTESIAN_POINT('Ctrl Pts',(-6.94307149280364,17.6664239800909,-11.7842765841997));
#24180=CARTESIAN_POINT('Ctrl Pts',(-6.94550485844196,17.665071741036,-11.7798812608693));
#24181=CARTESIAN_POINT('Ctrl Pts',(-6.94793418394148,17.6637208933711,-11.7754834321708));
#24182=CARTESIAN_POINT('Ctrl Pts',(-7.07457713217915,17.5932999757431,-11.5462206214354));
#24183=CARTESIAN_POINT('Ctrl Pts',(-7.19024425841544,17.5266506308609,-11.3101531082747));
#24184=CARTESIAN_POINT('Ctrl Pts',(-7.29463565879605,17.4650089179132,-11.0667676520206));
#24185=CARTESIAN_POINT('Ctrl Pts',(-7.31828389382657,17.4510449543094,-11.0116324928837));
#24186=CARTESIAN_POINT('Ctrl Pts',(-7.34135334430897,17.4373380947864,-10.956121694965));
#24187=CARTESIAN_POINT('Ctrl Pts',(-7.3638402765716,17.4239029374496,-10.9002291155016));
#24188=CARTESIAN_POINT('Ctrl Pts',(-7.36582071204233,17.4227196963639,-10.8953066278262));
#24189=CARTESIAN_POINT('Ctrl Pts',(-7.36779664658278,17.421538551103,-10.8903811356429));
#24190=CARTESIAN_POINT('Ctrl Pts',(-7.36976807627246,17.4203595125087,-10.8854526373327));
#24191=CARTESIAN_POINT('Ctrl Pts',(-7.44546738546979,17.3750865780631,-10.6962072792993));
#24192=CARTESIAN_POINT('Ctrl Pts',(-7.51472895154413,17.3327859329971,-10.5014874371513));
#24193=CARTESIAN_POINT('Ctrl Pts',(-7.57645236773666,17.29455943516,-10.3039688005431));
#24194=CARTESIAN_POINT('Ctrl Pts',(-7.61348923770643,17.2716217898201,-10.1854485935952));
#24195=CARTESIAN_POINT('Ctrl Pts',(-7.6478123110375,17.2501510470236,-10.0659218717069));
#24196=CARTESIAN_POINT('Ctrl Pts',(-7.67918843644889,17.2303836853404,-9.94597400456573));
#24197=CARTESIAN_POINT('Ctrl Pts',(-7.68031341058551,17.2296749371967,-9.94167333816705));
#24198=CARTESIAN_POINT('Ctrl Pts',(-7.68143460129582,17.2289683741076,-9.93737211336389));
#24199=CARTESIAN_POINT('Ctrl Pts',(-7.682551998173,17.2282640067415,-9.93307035593063));
#24200=CARTESIAN_POINT('Ctrl Pts',(-7.79057552082065,17.1601698088095,-9.51720111465524));
#24201=CARTESIAN_POINT('Ctrl Pts',(-7.86480882869604,17.1119590390803,-9.09494626559864));
#24202=CARTESIAN_POINT('Ctrl Pts',(-7.90422422557617,17.0860934798342,-8.66599267125661));
#24203=CARTESIAN_POINT('Ctrl Pts',(-7.92603246415529,17.07178226311,-8.42865591797634));
#24204=CARTESIAN_POINT('Ctrl Pts',(-7.9371813500848,17.064312408887,-8.1892683562573));
#24205=CARTESIAN_POINT('Ctrl Pts',(-7.93749334978002,17.0641067984408,-7.94777616176066));
#24206=CARTESIAN_POINT('Ctrl Pts',(-7.93749390429189,17.0641064330128,-7.94734696169487));
#24207=CARTESIAN_POINT('Ctrl Pts',(-7.93749442457205,17.0641060905316,-7.94691775513394));
#24208=CARTESIAN_POINT('Ctrl Pts',(-7.93749491061955,17.0641057709997,-7.94648854207958));
#24209=CARTESIAN_POINT('Ctrl Pts',(-7.93768655372469,17.0639797831163,-7.77725462647313));
#24210=CARTESIAN_POINT('Ctrl Pts',(-7.93239900403588,17.0674615298841,-7.60631918039094));
#24211=CARTESIAN_POINT('Ctrl Pts',(-7.92171494756793,17.0744688979786,-7.43716157505265));
#24212=CARTESIAN_POINT('Ctrl Pts',(-7.91102345406276,17.0814811438138,-7.2678862212346));
#24213=CARTESIAN_POINT('Ctrl Pts',(-7.89497393957298,17.0919932010127,-7.09996663012299));
#24214=CARTESIAN_POINT('Ctrl Pts',(-7.87374400759939,17.1058076114062,-6.93347731460257));
#24215=CARTESIAN_POINT('Ctrl Pts',(-7.87346433385428,17.1059895963459,-6.93128405790964));
#24216=CARTESIAN_POINT('Ctrl Pts',(-7.87318376431306,17.1061721542786,-6.92909104881785));
#24217=CARTESIAN_POINT('Ctrl Pts',(-7.87290229918002,17.1063552847221,-6.92689828753272));
#24218=CARTESIAN_POINT('Ctrl Pts',(-7.83036082814314,17.1340341605142,-6.59547787430953));
#24219=CARTESIAN_POINT('Ctrl Pts',(-7.76731445840906,17.174819812098,-6.26939293959585));
#24220=CARTESIAN_POINT('Ctrl Pts',(-7.68426407606719,17.2271865562986,-5.94853246399202));
#24221=CARTESIAN_POINT('Ctrl Pts',(-7.68326626852899,17.2278157157394,-5.9446774907548));
#24222=CARTESIAN_POINT('Ctrl Pts',(-7.68226543432046,17.2284466292013,-5.94082296302115));
#24223=CARTESIAN_POINT('Ctrl Pts',(-7.68126157924107,17.2290792899691,-5.93696889619287));
#24224=CARTESIAN_POINT('Ctrl Pts',(-7.62719229954297,17.2631554357352,-5.72938254075854));
#24225=CARTESIAN_POINT('Ctrl Pts',(-7.56432398380049,17.3023261324512,-5.52301181373151));
#24226=CARTESIAN_POINT('Ctrl Pts',(-7.4935763091711,17.345533282136,-5.32035620488053));
#24227=CARTESIAN_POINT('Ctrl Pts',(-7.45531251771263,17.3689018150767,-5.21075017195316));
#24228=CARTESIAN_POINT('Ctrl Pts',(-7.4147445062259,17.3934507919831,-5.10223040780266));
#24229=CARTESIAN_POINT('Ctrl Pts',(-7.37202153836157,17.4190115694052,-4.99518718727362));
#24230=CARTESIAN_POINT('Ctrl Pts',(-7.37020264317793,17.4200997984602,-4.99062991028669));
#24231=CARTESIAN_POINT('Ctrl Pts',(-7.36837989989909,17.4211898298956,-4.9860752064781));
#24232=CARTESIAN_POINT('Ctrl Pts',(-7.36655331157685,17.422281655205,-4.98152307439258));
#24233=CARTESIAN_POINT('Ctrl Pts',(-7.26791525719856,17.4812415877351,-4.73570224726818));
#24234=CARTESIAN_POINT('Ctrl Pts',(-7.15804389761601,17.5454461273167,-4.49732014145397));
#24235=CARTESIAN_POINT('Ctrl Pts',(-7.03725813864796,17.6136630597091,-4.26584946646392));
#24236=CARTESIAN_POINT('Ctrl Pts',(-7.00830992697048,17.6300123231965,-4.2103738693903));
#24237=CARTESIAN_POINT('Ctrl Pts',(-6.97873464011855,17.6465921971233,-4.1552953738361));
#24238=CARTESIAN_POINT('Ctrl Pts',(-6.94853637755767,17.6633859685258,-4.10060692620219));
#24239=CARTESIAN_POINT('Ctrl Pts',(-6.94626438275752,17.6646494637757,-4.09649238920185));
#24240=CARTESIAN_POINT('Ctrl Pts',(-6.94398886116032,17.6659141722406,-4.09238006080646));
#24241=CARTESIAN_POINT('Ctrl Pts',(-6.94170981151124,17.667180087461,-4.08826993972571));
#24242=CARTESIAN_POINT('Ctrl Pts',(-6.81695592055677,17.7364755718406,-3.86328423249227));
#24243=CARTESIAN_POINT('Ctrl Pts',(-6.68164503357455,17.8093783831497,-3.64493058249314));
#24244=CARTESIAN_POINT('Ctrl Pts',(-6.53553788058789,17.8848500923535,-3.43297205340694));
#24245=CARTESIAN_POINT('Ctrl Pts',(-6.49757915893022,17.9044576854394,-3.37790510668951));
#24246=CARTESIAN_POINT('Ctrl Pts',(-6.45889152043283,17.9242387878716,-3.32326994127638));
#24247=CARTESIAN_POINT('Ctrl Pts',(-6.41947032548397,17.944175414547,-3.26906268219969));
#24248=CARTESIAN_POINT('Ctrl Pts',(-6.26576753847862,18.0219080933118,-3.05770920073322));
#24249=CARTESIAN_POINT('Ctrl Pts',(-6.10302120078014,18.1009132292221,-2.8557968247366));
#24250=CARTESIAN_POINT('Ctrl Pts',(-5.93170231104313,18.1799349593124,-2.66313899571769));
#24251=CARTESIAN_POINT('Ctrl Pts',(-5.88659280047641,18.2007419559838,-2.61241078712826));
#24252=CARTESIAN_POINT('Ctrl Pts',(-5.84088875206301,18.2215501339755,-2.5623244032648));
#24253=CARTESIAN_POINT('Ctrl Pts',(-5.79459835582529,18.2423366010455,-2.51287686611627));
#24254=CARTESIAN_POINT('Ctrl Pts',(-5.79304324259939,18.2430349167327,-2.51121568960325));
#24255=CARTESIAN_POINT('Ctrl Pts',(-5.79148746488087,18.2437332148302,-2.50955520810606));
#24256=CARTESIAN_POINT('Ctrl Pts',(-5.78993102234963,18.2444314946615,-2.50789542163744));
#24257=CARTESIAN_POINT('Ctrl Pts',(-5.60237021560088,18.3285784682036,-2.30788104087095));
#24258=CARTESIAN_POINT('Ctrl Pts',(-5.40518143441788,18.4124500515875,-2.11798146925534));
#24259=CARTESIAN_POINT('Ctrl Pts',(-5.19781723817633,18.4948497478445,-1.93825471385303));
#24260=CARTESIAN_POINT('Ctrl Pts',(-4.9967832052399,18.5747340458648,-1.76401443939882));
#24261=CARTESIAN_POINT('Ctrl Pts',(-4.78618558233977,18.6532355453134,-1.59933547602871));
#24262=CARTESIAN_POINT('Ctrl Pts',(-4.56549139794203,18.7292531909103,-1.44430382682765));
#24263=CARTESIAN_POINT('Ctrl Pts',(-4.47655669487745,18.7598865615054,-1.38182962196841));
#24264=CARTESIAN_POINT('Ctrl Pts',(-4.38598200496235,18.7901164038823,-1.32092242551976));
#24265=CARTESIAN_POINT('Ctrl Pts',(-4.29373077449684,18.8198698188908,-1.2615894039735));
#24266=CARTESIAN_POINT('',(1.11022302462516E-13,18.,0.));
#24267=CARTESIAN_POINT('Ctrl Pts',(-4.29373077449681,18.8198698188908,-1.26158940397354));
#24268=CARTESIAN_POINT('Ctrl Pts',(-4.22582648941137,18.8417707121595,-1.21791555388257));
#24269=CARTESIAN_POINT('Ctrl Pts',(-4.15661453194584,18.86071388632,-1.17487038785831));
#24270=CARTESIAN_POINT('Ctrl Pts',(-4.08645576680373,18.8768690611168,-1.13273802650262));
#24271=CARTESIAN_POINT('Ctrl Pts',(-4.0166014010922,18.8929541430892,-1.09078846578175));
#24272=CARTESIAN_POINT('Ctrl Pts',(-3.9458086305145,18.9062753659277,-1.04974397568514));
#24273=CARTESIAN_POINT('Ctrl Pts',(-3.8744619443222,18.9170002498469,-1.00984160108927));
#24274=CARTESIAN_POINT('Ctrl Pts',(-3.84731136562865,18.9210815438826,-0.99465697767726));
#24275=CARTESIAN_POINT('Ctrl Pts',(-3.82008084867973,18.9247868516778,-0.97963728668364));
#24276=CARTESIAN_POINT('Ctrl Pts',(-3.79279256087207,18.9281254049619,-0.964793865349493));
#24277=CARTESIAN_POINT('Ctrl Pts',(-3.64719779704915,18.945938024073,-0.885597822024888));
#24278=CARTESIAN_POINT('Ctrl Pts',(-3.4991287754235,18.9535969347798,-0.81096042606437));
#24279=CARTESIAN_POINT('Ctrl Pts',(-3.34860693025952,18.952622880884,-0.740921793892792));
#24280=CARTESIAN_POINT('Ctrl Pts',(-3.32232346104453,18.9524527958338,-0.728691952898373));
#24281=CARTESIAN_POINT('Ctrl Pts',(-3.2959651551925,18.9520194863078,-0.716602450005113));
#24282=CARTESIAN_POINT('Ctrl Pts',(-3.26953206999634,18.9513310489586,-0.704653652035405));
#24283=CARTESIAN_POINT('Ctrl Pts',(-3.17850334583775,18.9489602483847,-0.663505075305149));
#24284=CARTESIAN_POINT('Ctrl Pts',(-3.086419875657,18.9434916030851,-0.623954084670512));
#24285=CARTESIAN_POINT('Ctrl Pts',(-2.99364161461572,18.9352254582242,-0.586172491771277));
#24286=CARTESIAN_POINT('Ctrl Pts',(-2.90078198108134,18.9269520634234,-0.548357761988755));
#24287=CARTESIAN_POINT('Ctrl Pts',(-2.80722663233826,18.9158762597357,-0.512315658170322));
#24288=CARTESIAN_POINT('Ctrl Pts',(-2.71335601231357,18.9022991832847,-0.478169909405996));
#24289=CARTESIAN_POINT('Ctrl Pts',(-2.61888384721301,18.8886351017252,-0.443805346629091));
#24290=CARTESIAN_POINT('Ctrl Pts',(-2.52409266754353,18.8724375871946,-0.411361617018201));
#24291=CARTESIAN_POINT('Ctrl Pts',(-2.42938551103078,18.8540136022487,-0.380913979263318));
#24292=CARTESIAN_POINT('Ctrl Pts',(-2.34490238900972,18.8375785636982,-0.353753291619269));
#24293=CARTESIAN_POINT('Ctrl Pts',(-2.26048649576891,18.8193718208331,-0.32818026897181));
#24294=CARTESIAN_POINT('Ctrl Pts',(-2.17643094124134,18.7996112684571,-0.304214036012625));
#24295=CARTESIAN_POINT('Ctrl Pts',(-2.04502170239041,18.7687183767071,-0.266746144104807));
#24296=CARTESIAN_POINT('Ctrl Pts',(-1.91377939287518,18.7340115684466,-0.232990701121492));
#24297=CARTESIAN_POINT('Ctrl Pts',(-1.78264791444894,18.6958884625523,-0.202768416867322));
#24298=CARTESIAN_POINT('Ctrl Pts',(-1.64965288012602,18.657223575694,-0.172116633024579));
#24299=CARTESIAN_POINT('Ctrl Pts',(-1.51677140832459,18.6150446008057,-0.14509896764463));
#24300=CARTESIAN_POINT('Ctrl Pts',(-1.38391902822724,18.5697663509261,-0.121575590609266));
#24301=CARTESIAN_POINT('Ctrl Pts',(-1.28346880481899,18.5355312825546,-0.103789469827784));
#24302=CARTESIAN_POINT('Ctrl Pts',(-1.18303463224986,18.499524379302,-0.088001977634254));
#24303=CARTESIAN_POINT('Ctrl Pts',(-1.08257270443572,18.4619249481095,-0.074171023694225));
#24304=CARTESIAN_POINT('Ctrl Pts',(-0.977468955166084,18.4225882434023,
-0.0597010135450861));
#24305=CARTESIAN_POINT('Ctrl Pts',(-0.872311892508873,18.3814503563709,
-0.0473752902949603));
#24306=CARTESIAN_POINT('Ctrl Pts',(-0.767497582476942,18.3388427147694,
-0.0371928090806906));
#24307=CARTESIAN_POINT('Ctrl Pts',(-0.690645617488946,18.307601933052,-0.0297268085934328));
#24308=CARTESIAN_POINT('Ctrl Pts',(-0.613978042670824,18.2755709939339,
-0.0234119367079837));
#24309=CARTESIAN_POINT('Ctrl Pts',(-0.537651063225293,18.2428805421956,
-0.0182299841328799));
#24310=CARTESIAN_POINT('Ctrl Pts',(-0.45595667868525,18.2078912585309,-0.0126836304134733));
#24311=CARTESIAN_POINT('Ctrl Pts',(-0.374796918314945,18.1722049684806,
-0.00843915814557654));
#24312=CARTESIAN_POINT('Ctrl Pts',(-0.293782657353165,18.1357422451802,
-0.00543860334920243));
#24313=CARTESIAN_POINT('Ctrl Pts',(-0.212550494340367,18.0991814489962,
-0.00242997803491511));
#24314=CARTESIAN_POINT('Ctrl Pts',(-0.131464343433757,18.0618400372384,
-0.000671975325032559));
#24315=CARTESIAN_POINT('Ctrl Pts',(-0.0501289083909383,18.0236379404196,
-0.000158294961541294));
#24316=CARTESIAN_POINT('Ctrl Pts',(-0.0334309211493575,18.0157951333461,
-5.28375043910101E-5));
#24317=CARTESIAN_POINT('Ctrl Pts',(-0.016722425025208,18.0079160508127,
-4.41750233939426E-14));
#24318=CARTESIAN_POINT('Ctrl Pts',(1.11022302462515E-13,18.,-4.44089209850063E-14));
#24319=CARTESIAN_POINT('',(4.29373077449696,18.8198698188909,-1.26158940397347));
#24320=CARTESIAN_POINT('Ctrl Pts',(1.11022302462515E-13,18.,-4.44089209850063E-14));
#24321=CARTESIAN_POINT('Ctrl Pts',(0.152276681653021,18.0720846377099,-4.65388243309537E-14));
#24322=CARTESIAN_POINT('Ctrl Pts',(0.305855934149367,18.1421428141949,-0.0043858625805328));
#24323=CARTESIAN_POINT('Ctrl Pts',(0.460325988382226,18.2094023440686,-0.0133592746961373));
#24324=CARTESIAN_POINT('Ctrl Pts',(0.614082442636275,18.2763511574133,-0.0222912326494619));
#24325=CARTESIAN_POINT('Ctrl Pts',(0.768721126528699,18.3405271220422,-0.0357686311582533));
#24326=CARTESIAN_POINT('Ctrl Pts',(0.923815416695544,18.4011687049212,-0.0539429775719302));
#24327=CARTESIAN_POINT('Ctrl Pts',(0.976648961370601,18.4218265239471,-0.0601341477443072));
#24328=CARTESIAN_POINT('Ctrl Pts',(1.02953522561586,18.4420741942768,-0.0668699586701339));
#24329=CARTESIAN_POINT('Ctrl Pts',(1.08245691517558,18.4618816114694,-0.0741550834401359));
#24330=CARTESIAN_POINT('Ctrl Pts',(1.21556599724415,18.5117013950515,-0.0924786909998602));
#24331=CARTESIAN_POINT('Ctrl Pts',(1.34862695113425,18.5587255077162,-0.114235315255648));
#24332=CARTESIAN_POINT('Ctrl Pts',(1.48173956573871,18.6025368983504,-0.139528846595817));
#24333=CARTESIAN_POINT('Ctrl Pts',(1.61308402605649,18.6457663358888,-0.164486400267772));
#24334=CARTESIAN_POINT('Ctrl Pts',(1.74447921274513,18.685867834649,-0.192887677393095));
#24335=CARTESIAN_POINT('Ctrl Pts',(1.87600132923503,18.7224407429918,-0.224878833191163));
#24336=CARTESIAN_POINT('Ctrl Pts',(1.97603783313957,18.7502583145597,-0.249211496528055));
#24337=CARTESIAN_POINT('Ctrl Pts',(2.07614742951043,18.7760345210385,-0.275621926940948));
#24338=CARTESIAN_POINT('Ctrl Pts',(2.17635351087795,18.7995930649607,-0.304191959203497));
#24339=CARTESIAN_POINT('Ctrl Pts',(2.27056963336781,18.8217433639203,-0.331054177768009));
#24340=CARTESIAN_POINT('Ctrl Pts',(2.36523835232694,18.8419415753925,-0.359935968511773));
#24341=CARTESIAN_POINT('Ctrl Pts',(2.45994739338413,18.8598808531924,-0.390807673438519));
#24342=CARTESIAN_POINT('Ctrl Pts',(2.55421906742605,18.8777372872817,-0.421536812615581));
#24343=CARTESIAN_POINT('Ctrl Pts',(2.64853037015873,18.8933556030678,-0.454237521149386));
#24344=CARTESIAN_POINT('Ctrl Pts',(2.74248535327419,18.9064331858182,-0.488830297490975));
#24345=CARTESIAN_POINT('Ctrl Pts',(2.83620349346067,18.9194778024299,-0.523335871917366));
#24346=CARTESIAN_POINT('Ctrl Pts',(2.92956679712376,18.9299944792857,-0.559723917381846));
#24347=CARTESIAN_POINT('Ctrl Pts',(3.02219766183738,18.9376828843945,-0.597865980324086));
#24348=CARTESIAN_POINT('Ctrl Pts',(3.10530581747092,18.9445809001944,-0.632086933707045));
#24349=CARTESIAN_POINT('Ctrl Pts',(3.18782444335928,18.949202262231,-0.667719091773169));
#24350=CARTESIAN_POINT('Ctrl Pts',(3.26949439648293,18.9513300675967,-0.704636622238322));
#24351=CARTESIAN_POINT('Ctrl Pts',(3.42087322908578,18.9552740479706,-0.773064880742814));
#24352=CARTESIAN_POINT('Ctrl Pts',(3.56980099384823,18.9508507374212,-0.846103860736343));
#24353=CARTESIAN_POINT('Ctrl Pts',(3.71625969440024,18.936539439914,-0.923705011994175));
#24354=CARTESIAN_POINT('Ctrl Pts',(3.74184003411389,18.9340398420711,-0.937258756523275));
#24355=CARTESIAN_POINT('Ctrl Pts',(3.7673450046304,18.9312386033841,-0.950951792714971));
#24356=CARTESIAN_POINT('Ctrl Pts',(3.79277444384618,18.9281276214136,-0.964784010652182));
#24357=CARTESIAN_POINT('Ctrl Pts',(3.86447430656453,18.9193560170413,-1.00378479705462));
#24358=CARTESIAN_POINT('Ctrl Pts',(3.93577353808618,18.9080524652381,-1.04400575073184));
#24359=CARTESIAN_POINT('Ctrl Pts',(4.00627785537283,18.8940495030153,-1.08522709274151));
#24360=CARTESIAN_POINT('Ctrl Pts',(4.07705725420683,18.8799919064571,-1.1266092650518));
#24361=CARTESIAN_POINT('Ctrl Pts',(4.14703529717648,18.8632137942018,-1.16899950567748));
#24362=CARTESIAN_POINT('Ctrl Pts',(4.21584055455503,18.8435457354689,-1.21213051806308));
#24363=CARTESIAN_POINT('Ctrl Pts',(4.24197933063947,18.8360739374869,-1.22851577578894));
#24364=CARTESIAN_POINT('Ctrl Pts',(4.26794914936844,18.828185061729,-1.24500749269148));
#24365=CARTESIAN_POINT('Ctrl Pts',(4.29373077449689,18.8198698188909,-1.26158940397359));
#24366=CARTESIAN_POINT('',(4.29373077449696,18.819869818891,-14.6134105960265));
#24367=CARTESIAN_POINT('Ctrl Pts',(4.29373077449695,18.8198698188909,-1.2615894039735));
#24368=CARTESIAN_POINT('Ctrl Pts',(4.52296127991311,18.7459370341897,-1.40902308532697));
#24369=CARTESIAN_POINT('Ctrl Pts',(4.74196146059745,18.6690215822512,-1.56625194639558));
#24370=CARTESIAN_POINT('Ctrl Pts',(4.95124940534233,18.5902365315365,-1.7332031049152));
#24371=CARTESIAN_POINT('Ctrl Pts',(5.16682135233816,18.5090859100929,-1.90516707703578));
#24372=CARTESIAN_POINT('Ctrl Pts',(5.37208902248157,18.4259511224268,-2.08744583105033));
#24373=CARTESIAN_POINT('Ctrl Pts',(5.56758051817822,18.3420322632787,-2.27999629490369));
#24374=CARTESIAN_POINT('Ctrl Pts',(5.64332797575349,18.3095160650655,-2.35460418533829));
#24375=CARTESIAN_POINT('Ctrl Pts',(5.71760730139922,18.2768820316859,-2.43075460304643));
#24376=CARTESIAN_POINT('Ctrl Pts',(5.79044777763098,18.244199660671,-2.5084465101464));
#24377=CARTESIAN_POINT('Ctrl Pts',(5.79212935934828,18.2434451615186,-2.51024009109646));
#24378=CARTESIAN_POINT('Ctrl Pts',(5.79381016993239,18.242690638533,-2.51203448908584));
#24379=CARTESIAN_POINT('Ctrl Pts',(5.79549020982554,18.2419360925351,-2.51382970417484));
#24380=CARTESIAN_POINT('Ctrl Pts',(5.94895048261904,18.1730134228195,-2.67781045154005));
#24381=CARTESIAN_POINT('Ctrl Pts',(6.0964374109252,18.1036131389842,-2.84947341504703));
#24382=CARTESIAN_POINT('Ctrl Pts',(6.23662479532932,18.0350900643106,-3.02750642175075));
#24383=CARTESIAN_POINT('Ctrl Pts',(6.29721400007292,18.0054742852681,-3.10445256308966));
#24384=CARTESIAN_POINT('Ctrl Pts',(6.3564392068392,17.9760223903775,-3.18258907955983));
#24385=CARTESIAN_POINT('Ctrl Pts',(6.41419086511958,17.9468442552091,-3.26181175077503));
#24386=CARTESIAN_POINT('Ctrl Pts',(6.41654032136261,17.9456572286566,-3.26503469198604));
#24387=CARTESIAN_POINT('Ctrl Pts',(6.41888732415851,17.9444706625731,-3.26825941111731));
#24388=CARTESIAN_POINT('Ctrl Pts',(6.42123186600286,17.9432845644399,-3.27148590089689));
#24389=CARTESIAN_POINT('Ctrl Pts',(6.56679359840251,17.8696452308231,-3.47180369134996));
#24390=CARTESIAN_POINT('Ctrl Pts',(6.70230659932144,17.7981518448203,-3.67790484239893));
#24391=CARTESIAN_POINT('Ctrl Pts',(6.82801702238586,17.7297067508609,-3.89000132125883));
#24392=CARTESIAN_POINT('Ctrl Pts',(6.86647149533936,17.7087695847111,-3.95488105128465));
#24393=CARTESIAN_POINT('Ctrl Pts',(6.90400842024961,17.6881177916226,-4.02032196158267));
#24394=CARTESIAN_POINT('Ctrl Pts',(6.94063408540424,17.6677776026631,-4.08633059633637));
#24395=CARTESIAN_POINT('Ctrl Pts',(6.94307149280366,17.6664239800909,-4.0907234158004));
#24396=CARTESIAN_POINT('Ctrl Pts',(6.94550485844198,17.6650717410359,-4.09511873913086));
#24397=CARTESIAN_POINT('Ctrl Pts',(6.9479341839415,17.6637208933711,-4.09951656782928));
#24398=CARTESIAN_POINT('Ctrl Pts',(7.07457713214333,17.5932999757631,-4.32877937849984));
#24399=CARTESIAN_POINT('Ctrl Pts',(7.19024425834999,17.5266506308987,-4.56484689159181));
#24400=CARTESIAN_POINT('Ctrl Pts',(7.29463565870743,17.4650089179656,-4.8082323477729));
#24401=CARTESIAN_POINT('Ctrl Pts',(7.31828389376895,17.4510449543436,-4.86336750697776));
#24402=CARTESIAN_POINT('Ctrl Pts',(7.3413533442809,17.4373380948032,-4.91887830496527));
#24403=CARTESIAN_POINT('Ctrl Pts',(7.36384027657162,17.4239029374496,-4.97477088449852));
#24404=CARTESIAN_POINT('Ctrl Pts',(7.36582071204235,17.4227196963639,-4.97969337217391));
#24405=CARTESIAN_POINT('Ctrl Pts',(7.3677966465828,17.421538551103,-4.98461886435727));
#24406=CARTESIAN_POINT('Ctrl Pts',(7.36976807627247,17.4203595125087,-4.98954736266744));
#24407=CARTESIAN_POINT('Ctrl Pts',(7.44546738549149,17.3750865780502,-5.17879272075504));
#24408=CARTESIAN_POINT('Ctrl Pts',(7.51472895158381,17.3327859329729,-5.37351256296032));
#24409=CARTESIAN_POINT('Ctrl Pts',(7.57645236778969,17.2945594351273,-5.57103119962675));
#24410=CARTESIAN_POINT('Ctrl Pts',(7.6134892377392,17.2716217897998,-5.68955140651901));
#24411=CARTESIAN_POINT('Ctrl Pts',(7.64781231105249,17.2501510470144,-5.80907812835044));
#24412=CARTESIAN_POINT('Ctrl Pts',(7.67918843644891,17.2303836853409,-5.92902599543444));
#24413=CARTESIAN_POINT('Ctrl Pts',(7.68031341058553,17.2296749371971,-5.93332666183312));
#24414=CARTESIAN_POINT('Ctrl Pts',(7.68143460129584,17.228968374108,-5.93762788663628));
#24415=CARTESIAN_POINT('Ctrl Pts',(7.68255199817302,17.2282640067419,-5.94192964406954));
#24416=CARTESIAN_POINT('Ctrl Pts',(7.79057552101168,17.1601698086902,-6.35779888608028));
#24417=CARTESIAN_POINT('Ctrl Pts',(7.86480882895862,17.1119590389104,-6.7800537358947));
#24418=CARTESIAN_POINT('Ctrl Pts',(7.90422422578528,17.0860934796973,-7.20900733101881));
#24419=CARTESIAN_POINT('Ctrl Pts',(7.92603246422657,17.0717822630624,-7.44634408355374));
#24420=CARTESIAN_POINT('Ctrl Pts',(7.9371813500858,17.0643124088864,-7.68573164451451));
#24421=CARTESIAN_POINT('Ctrl Pts',(7.93749334978002,17.0641067984408,-7.92722383823945));
#24422=CARTESIAN_POINT('Ctrl Pts',(7.93749390429189,17.0641064330128,-7.92765303830522));
#24423=CARTESIAN_POINT('Ctrl Pts',(7.93749442457205,17.0641060905316,-7.92808224486615));
#24424=CARTESIAN_POINT('Ctrl Pts',(7.93749491061955,17.0641057709997,-7.92851145792049));
#24425=CARTESIAN_POINT('Ctrl Pts',(7.93768655372469,17.0639797831163,-8.09774537352705));
#24426=CARTESIAN_POINT('Ctrl Pts',(7.93239900403588,17.0674615298841,-8.26868081960914));
#24427=CARTESIAN_POINT('Ctrl Pts',(7.92171494756793,17.0744688979786,-8.43783842494743));
#24428=CARTESIAN_POINT('Ctrl Pts',(7.91102345406277,17.0814811438138,-8.60711377876527));
#24429=CARTESIAN_POINT('Ctrl Pts',(7.89497393957297,17.0919932010127,-8.77503336987718));
#24430=CARTESIAN_POINT('Ctrl Pts',(7.87374400759939,17.1058076114061,-8.9415226853975));
#24431=CARTESIAN_POINT('Ctrl Pts',(7.87346433385428,17.1059895963459,-8.94371594209044));
#24432=CARTESIAN_POINT('Ctrl Pts',(7.87318376431306,17.1061721542786,-8.94590895118223));
#24433=CARTESIAN_POINT('Ctrl Pts',(7.87290229918002,17.1063552847221,-8.94810171246737));
#24434=CARTESIAN_POINT('Ctrl Pts',(7.83036082814314,17.1340341605142,-9.27952212569055));
#24435=CARTESIAN_POINT('Ctrl Pts',(7.76731445840908,17.1748198120981,-9.60560706040417));
#24436=CARTESIAN_POINT('Ctrl Pts',(7.6842640760672,17.2271865562987,-9.92646753600803));
#24437=CARTESIAN_POINT('Ctrl Pts',(7.68326626852899,17.2278157157395,-9.93032250924526));
#24438=CARTESIAN_POINT('Ctrl Pts',(7.68226543432046,17.2284466292013,-9.93417703697893));
#24439=CARTESIAN_POINT('Ctrl Pts',(7.68126157924107,17.2290792899692,-9.93803110380722));
#24440=CARTESIAN_POINT('Ctrl Pts',(7.6271922995878,17.2631554357069,-10.1456174590694));
#24441=CARTESIAN_POINT('Ctrl Pts',(7.56432398390477,17.3023261323862,-10.3519881859263));
#24442=CARTESIAN_POINT('Ctrl Pts',(7.49357630934712,17.3455332820285,-10.5546437946154));
#24443=CARTESIAN_POINT('Ctrl Pts',(7.45531251783705,17.3689018150015,-10.6642498277141));
#24444=CARTESIAN_POINT('Ctrl Pts',(7.41474450629143,17.3934507919441,-10.7727695920332));
#24445=CARTESIAN_POINT('Ctrl Pts',(7.37202153836162,17.4190115694055,-10.8798128127264));
#24446=CARTESIAN_POINT('Ctrl Pts',(7.37020264317797,17.4200997984605,-10.8843700897133));
#24447=CARTESIAN_POINT('Ctrl Pts',(7.36837989989913,17.4211898298959,-10.8889247935219));
#24448=CARTESIAN_POINT('Ctrl Pts',(7.36655331157689,17.4222816552053,-10.8934769256074));
#24449=CARTESIAN_POINT('Ctrl Pts',(7.26791525731588,17.4812415876656,-11.1392977524395));
#24450=CARTESIAN_POINT('Ctrl Pts',(7.15804389787725,17.5454461271643,-11.3776798579793));
#24451=CARTESIAN_POINT('Ctrl Pts',(7.03725813907874,17.6136630594658,-11.6091505327106));
#24452=CARTESIAN_POINT('Ctrl Pts',(7.00830992726388,17.6300123230318,-11.6646261300634));
#24453=CARTESIAN_POINT('Ctrl Pts',(6.97873464026834,17.6465921970398,-11.7197046258927));
#24454=CARTESIAN_POINT('Ctrl Pts',(6.94853637755767,17.6633859685255,-11.7743930737979));
#24455=CARTESIAN_POINT('Ctrl Pts',(6.94626438275751,17.6646494637754,-11.7785076107983));
#24456=CARTESIAN_POINT('Ctrl Pts',(6.94398886116031,17.6659141722403,-11.7826199391936));
#24457=CARTESIAN_POINT('Ctrl Pts',(6.94170981151122,17.6671800874607,-11.7867300602744));
#24458=CARTESIAN_POINT('Ctrl Pts',(6.81695592061704,17.7364755718065,-12.0117157673991));
#24459=CARTESIAN_POINT('Ctrl Pts',(6.6816450337051,17.8093783830793,-12.2300694172962));
#24460=CARTESIAN_POINT('Ctrl Pts',(6.53553788079947,17.884850092244,-12.4420279462862));
#24461=CARTESIAN_POINT('Ctrl Pts',(6.49757915907396,17.9044576853657,-12.4970948931076));
#24462=CARTESIAN_POINT('Ctrl Pts',(6.45889152050604,17.9242387878342,-12.551730058623));
#24463=CARTESIAN_POINT('Ctrl Pts',(6.41947032548394,17.9441754145465,-12.6059373178004));
#24464=CARTESIAN_POINT('Ctrl Pts',(6.26576753853644,18.0219080932814,-12.8172907991874));
#24465=CARTESIAN_POINT('Ctrl Pts',(6.10302120090262,18.1009132291616,-13.0192031751115));
#24466=CARTESIAN_POINT('Ctrl Pts',(5.93170231123652,18.1799349592224,-13.2118610040649));
#24467=CARTESIAN_POINT('Ctrl Pts',(5.88659280060703,18.2007419559236,-13.2625892127287));
#24468=CARTESIAN_POINT('Ctrl Pts',(5.84088875212914,18.2215501339452,-13.3126755966646));
#24469=CARTESIAN_POINT('Ctrl Pts',(5.79459835582526,18.2423366010449,-13.3621231338839));
#24470=CARTESIAN_POINT('Ctrl Pts',(5.79304324259934,18.2430349167321,-13.3637843103969));
#24471=CARTESIAN_POINT('Ctrl Pts',(5.79148746488082,18.2437332148296,-13.3654447918941));
#24472=CARTESIAN_POINT('Ctrl Pts',(5.78993102234957,18.2444314946609,-13.3671045783627));
#24473=CARTESIAN_POINT('Ctrl Pts',(5.60237021613349,18.3285784679638,-13.5671189585611));
#24474=CARTESIAN_POINT('Ctrl Pts',(5.40518143553207,18.4124500510806,-13.7570185296695));
#24475=CARTESIAN_POINT('Ctrl Pts',(5.19781723993319,18.4948497470905,-13.9367452846217));
#24476=CARTESIAN_POINT('Ctrl Pts',(4.99678320746859,18.5747340449313,-14.1109855587706));
#24477=CARTESIAN_POINT('Ctrl Pts',(4.78618558508331,18.653235544217,-14.2756645218748));
#24478=CARTESIAN_POINT('Ctrl Pts',(4.56549140125338,18.7292531897088,-14.4306961708455));
#24479=CARTESIAN_POINT('Ctrl Pts',(4.47655669712446,18.7598865607069,-14.4931703765203));
#24480=CARTESIAN_POINT('Ctrl Pts',(4.38598200610592,18.7901164034845,-14.5540775737448));
#24481=CARTESIAN_POINT('Ctrl Pts',(4.29373077449694,18.819869818891,-14.6134105960265));
#24482=CARTESIAN_POINT('Ctrl Pts',(4.29373077449694,18.819869818891,-14.6134105960265));
#24483=CARTESIAN_POINT('Ctrl Pts',(4.2258264894115,18.8417707121597,-14.6570844461174));
#24484=CARTESIAN_POINT('Ctrl Pts',(4.15661453194596,18.8607138863202,-14.7001296121417));
#24485=CARTESIAN_POINT('Ctrl Pts',(4.08645576680384,18.876869061117,-14.7422619734974));
#24486=CARTESIAN_POINT('Ctrl Pts',(4.01660140109238,18.8929541430893,-14.7842115342182));
#24487=CARTESIAN_POINT('Ctrl Pts',(3.94580863051476,18.9062753659278,-14.8252560243148));
#24488=CARTESIAN_POINT('Ctrl Pts',(3.87446194432254,18.9170002498469,-14.8651583989106));
#24489=CARTESIAN_POINT('Ctrl Pts',(3.84731136562891,18.9210815438826,-14.8803430223227));
#24490=CARTESIAN_POINT('Ctrl Pts',(3.82008084867992,18.9247868516778,-14.8953627133163));
#24491=CARTESIAN_POINT('Ctrl Pts',(3.79279256087219,18.9281254049619,-14.9102061346505));
#24492=CARTESIAN_POINT('Ctrl Pts',(3.64719779704913,18.9459380240731,-14.9894021779752));
#24493=CARTESIAN_POINT('Ctrl Pts',(3.49912877542333,18.9535969347799,-15.0640395739358));
#24494=CARTESIAN_POINT('Ctrl Pts',(3.34860693025921,18.952622880884,-15.1340782061074));
#24495=CARTESIAN_POINT('Ctrl Pts',(3.32232346104436,18.9524527958339,-15.1463080471018));
#24496=CARTESIAN_POINT('Ctrl Pts',(3.29596515519248,18.9520194863078,-15.158397549995));
#24497=CARTESIAN_POINT('Ctrl Pts',(3.26953206999647,18.9513310489587,-15.1703463479646));
#24498=CARTESIAN_POINT('Ctrl Pts',(3.17850334583779,18.9489602483847,-15.2114949246949));
#24499=CARTESIAN_POINT('Ctrl Pts',(3.08641987565695,18.9434916030852,-15.2510459153296));
#24500=CARTESIAN_POINT('Ctrl Pts',(2.99364161461558,18.9352254582242,-15.2888275082289));
#24501=CARTESIAN_POINT('Ctrl Pts',(2.90078198108108,18.9269520634234,-15.3266422380114));
#24502=CARTESIAN_POINT('Ctrl Pts',(2.80722663233789,18.9158762597357,-15.3626843418299));
#24503=CARTESIAN_POINT('Ctrl Pts',(2.71335601231308,18.9022991832847,-15.3968300905943));
#24504=CARTESIAN_POINT('Ctrl Pts',(2.61888384721251,18.8886351017251,-15.4311946533712));
#24505=CARTESIAN_POINT('Ctrl Pts',(2.52409266754301,18.8724375871946,-15.4636383829821));
#24506=CARTESIAN_POINT('Ctrl Pts',(2.42938551103024,18.8540136022486,-15.4940860207369));
#24507=CARTESIAN_POINT('Ctrl Pts',(2.34490238900942,18.8375785636981,-15.5212467083809));
#24508=CARTESIAN_POINT('Ctrl Pts',(2.26048649576885,18.8193718208331,-15.5468197310283));
#24509=CARTESIAN_POINT('Ctrl Pts',(2.17643094124152,18.7996112684571,-15.5707859639874));
#24510=CARTESIAN_POINT('Ctrl Pts',(2.04502170239011,18.7687183767071,-15.6082538558954));
#24511=CARTESIAN_POINT('Ctrl Pts',(1.91377939287443,18.7340115684464,-15.6420092988788));
#24512=CARTESIAN_POINT('Ctrl Pts',(1.78264791444772,18.6958884625519,-15.672231583133));
#24513=CARTESIAN_POINT('Ctrl Pts',(1.64965288012492,18.6572235756936,-15.7028833669757));
#24514=CARTESIAN_POINT('Ctrl Pts',(1.5167714083236,18.6150446008053,-15.7299010323556));
#24515=CARTESIAN_POINT('Ctrl Pts',(1.38391902822637,18.5697663509256,-15.753424409391));
#24516=CARTESIAN_POINT('Ctrl Pts',(1.28346880481848,18.5355312825542,-15.7712105301724));
#24517=CARTESIAN_POINT('Ctrl Pts',(1.18303463224972,18.4995243793018,-15.7869980223658));
#24518=CARTESIAN_POINT('Ctrl Pts',(1.08257270443595,18.4619249481094,-15.8008289763058));
#24519=CARTESIAN_POINT('Ctrl Pts',(0.977468955166276,18.4225882434021,-15.815298986455));
#24520=CARTESIAN_POINT('Ctrl Pts',(0.872311892509042,18.3814503563707,-15.8276247097051));
#24521=CARTESIAN_POINT('Ctrl Pts',(0.767497582477098,18.3388427147692,-15.8378071909194));
#24522=CARTESIAN_POINT('Ctrl Pts',(0.690645617489172,18.3076019330517,-15.8452731914066));
#24523=CARTESIAN_POINT('Ctrl Pts',(0.613978042671126,18.2755709939336,-15.8515880632921));
#24524=CARTESIAN_POINT('Ctrl Pts',(0.537651063225676,18.2428805421952,-15.8567700158672));
#24525=CARTESIAN_POINT('Ctrl Pts',(0.45595667868505,18.2078912585301,-15.8623163695866));
#24526=CARTESIAN_POINT('Ctrl Pts',(0.374796918314128,18.1722049684796,-15.8665608418546));
#24527=CARTESIAN_POINT('Ctrl Pts',(0.293782657351695,18.135742245179,-15.8695613966509));
#24528=CARTESIAN_POINT('Ctrl Pts',(0.212550494338228,18.0991814489947,-15.8725700219652));
#24529=CARTESIAN_POINT('Ctrl Pts',(0.131464343430913,18.0618400372367,-15.8743280246751));
#24530=CARTESIAN_POINT('Ctrl Pts',(0.0501289083873587,18.0236379404178,
-15.8748417050386));
#24531=CARTESIAN_POINT('Ctrl Pts',(0.0334309211470233,18.0157951333449,
-15.8749471624957));
#24532=CARTESIAN_POINT('Ctrl Pts',(0.0167224250241153,18.0079160508122,
-15.875));
#24533=CARTESIAN_POINT('Ctrl Pts',(4.32715606350417E-14,18.0000000000001,
-15.875));
#24534=CARTESIAN_POINT('',(4.52144207627622,18.7773513853136,-1.41366157655261));
#24535=CARTESIAN_POINT('Ctrl Pts',(1.73472347597681E-15,19.8025000069371,
-15.875));
#24536=CARTESIAN_POINT('Ctrl Pts',(0.28078511621843,19.7879617713667,-15.875));
#24537=CARTESIAN_POINT('Ctrl Pts',(0.561903033215541,19.7734063043411,-15.8601014606599));
#24538=CARTESIAN_POINT('Ctrl Pts',(1.86117102937661,19.7061339914361,-15.7214667453191));
#24539=CARTESIAN_POINT('Ctrl Pts',(2.84950805886979,19.6567506265481,-15.4164312891935));
#24540=CARTESIAN_POINT('Ctrl Pts',(4.6649970185884,19.5510594075386,-14.4424148382232));
#24541=CARTESIAN_POINT('Ctrl Pts',(5.47292612938169,19.497026701168,-13.7790166836516));
#24542=CARTESIAN_POINT('Ctrl Pts',(6.7922170125074,19.39294016586,-12.1747691802672));
#24543=CARTESIAN_POINT('Ctrl Pts',(7.28903180110871,19.340889707494,-11.2479079619773));
#24544=CARTESIAN_POINT('Ctrl Pts',(7.89112344354121,19.2339761464206,-9.27239428384591));
#24545=CARTESIAN_POINT('Ctrl Pts',(7.99733713518596,19.1835834316776,-8.2446715787786));
#24546=CARTESIAN_POINT('Ctrl Pts',(7.81173773313659,19.0791855521311,-6.18491852326425));
#24547=CARTESIAN_POINT('Ctrl Pts',(7.51360210287129,19.0246028887965,-5.17335226229376));
#24548=CARTESIAN_POINT('Ctrl Pts',(6.7337446239372,18.9389600978562,-3.68755396639768));
#24549=CARTESIAN_POINT('Ctrl Pts',(6.37318980270495,18.9081830882073,-3.16384313246412));
#24550=CARTESIAN_POINT('Ctrl Pts',(5.52988896127073,18.8437451698883,-2.20723351035506));
#24551=CARTESIAN_POINT('Ctrl Pts',(5.04878532190664,18.8105640618459,-1.77914455941684));
#24552=CARTESIAN_POINT('Ctrl Pts',(4.52144207733339,18.7773513820815,-1.41366157532098));
#24553=CARTESIAN_POINT('',(4.52144288377396,20.9998514252466,-1.41366213469196));
#24554=CARTESIAN_POINT('',(4.52144227190804,-18.001,-1.41366171017376));
#24555=CARTESIAN_POINT('Ctrl Pts',(4.52144288411286,20.9998514259562,-1.41366213447142));
#24556=CARTESIAN_POINT('Ctrl Pts',(4.5383926725966,21.0009189430859,-1.42540943753239));
#24557=CARTESIAN_POINT('Ctrl Pts',(4.55728556841932,21.0021118120135,-1.43860111654245));
#24558=CARTESIAN_POINT('Ctrl Pts',(4.59656734244123,21.0046012578358,-1.46633308801974));
#24559=CARTESIAN_POINT('Ctrl Pts',(4.61525107330043,21.0057890269683,-1.47964508784235));
#24560=CARTESIAN_POINT('Ctrl Pts',(4.67112900535412,21.0093524693881,-1.51982399655622));
#24561=CARTESIAN_POINT('Ctrl Pts',(4.70814823049889,21.0117281688305,-1.54693259872643));
#24562=CARTESIAN_POINT('Ctrl Pts',(4.81847839168823,21.0188535923946,-1.62920471299908));
#24563=CARTESIAN_POINT('Ctrl Pts',(4.89107015989642,21.0236021542917,-1.68531988610988));
#24564=CARTESIAN_POINT('Ctrl Pts',(5.10566975846148,21.0378234731235,-1.85723573883025));
#24565=CARTESIAN_POINT('Ctrl Pts',(5.24465837470424,21.0472815114198,-1.97670838228095));
#24566=CARTESIAN_POINT('Ctrl Pts',(5.64698140301046,21.0754192752053,-2.34751435539956));
#24567=CARTESIAN_POINT('Ctrl Pts',(5.89730544927446,21.0939623080549,-2.61226344399402));
#24568=CARTESIAN_POINT('Ctrl Pts',(6.58950342094494,21.1485522388563,-3.45326123482118));
#24569=CARTESIAN_POINT('Ctrl Pts',(6.97149805034829,21.1842837666164,-4.07379455621954));
#24570=CARTESIAN_POINT('Ctrl Pts',(7.68790162509451,21.2758275495856,-5.70004455898083));
#24571=CARTESIAN_POINT('Ctrl Pts',(7.9164252601042,21.3305618299046,-6.73730808732291));
#24572=CARTESIAN_POINT('Ctrl Pts',(7.9553382818272,21.4335563885068,-8.81622452353918));
#24573=CARTESIAN_POINT('Ctrl Pts',(7.77492400159749,21.4861693008238,-9.83763210663414));
#24574=CARTESIAN_POINT('Ctrl Pts',(7.03333162878123,21.5926233167573,-11.758487045622));
#24575=CARTESIAN_POINT('Ctrl Pts',(6.47786512863979,21.6427390970134,-12.6390947482521));
#24576=CARTESIAN_POINT('Ctrl Pts',(5.05339855943061,21.7482904710141,-14.1467122935227));
#24577=CARTESIAN_POINT('Ctrl Pts',(4.19490628033729,21.8027988640264,-14.7561464216009));
#24578=CARTESIAN_POINT('Ctrl Pts',(2.30914815337798,21.9074823693995,-15.6003340105396));
#24579=CARTESIAN_POINT('Ctrl Pts',(1.30300839224804,21.9575340202796,-15.8339134177512));
#24580=CARTESIAN_POINT('Ctrl Pts',(0.186818041394457,22.0153271058986,-15.8733523298983));
#24581=CARTESIAN_POINT('Ctrl Pts',(0.0933755231575857,22.0201652873541,
-15.875));
#24582=CARTESIAN_POINT('Ctrl Pts',(-6.13136191901172E-14,22.0250000000001,
-15.875));
#24583=CARTESIAN_POINT('Origin',(0.,-18.001,-7.93750000000004));
#24584=CARTESIAN_POINT('',(-1.46435436667273E-14,24.8825000069372,-15.875));
#24585=CARTESIAN_POINT('',(2.4976926802685E-15,24.565,-15.875));
#24586=CARTESIAN_POINT('',(-9.72063396823211E-16,-18.001,-15.875));
#24587=CARTESIAN_POINT('Ctrl Pts',(5.27355936696949E-15,24.8825000069372,
-15.875));
#24588=CARTESIAN_POINT('Ctrl Pts',(0.508585808332571,24.8561669149667,-15.875));
#24589=CARTESIAN_POINT('Ctrl Pts',(1.0172159760106,24.8298315261982,-15.8261195652966));
#24590=CARTESIAN_POINT('Ctrl Pts',(2.53199346929553,24.7514007591734,-15.5308196961735));
#24591=CARTESIAN_POINT('Ctrl Pts',(3.49697445619331,24.7011416007129,-15.1375440354767));
#24592=CARTESIAN_POINT('Ctrl Pts',(5.21784645322123,24.5946348231499,-14.006500726105));
#24593=CARTESIAN_POINT('Ctrl Pts',(5.9584541853683,24.542304507375,-13.2812058307267));
#24594=CARTESIAN_POINT('Ctrl Pts',(7.13587120049114,24.4391532565869,-11.5690297426178));
#24595=CARTESIAN_POINT('Ctrl Pts',(7.55349651279749,24.3844224072545,-10.593278748503));
#24596=CARTESIAN_POINT('Ctrl Pts',(7.97902505515585,24.2775641934729,-8.56152020560536));
#24597=CARTESIAN_POINT('Ctrl Pts',(7.99286614193217,24.2281815440205,-7.52720113107582));
#24598=CARTESIAN_POINT('Ctrl Pts',(7.6246493370653,24.1224735020145,-5.50017796733907));
#24599=CARTESIAN_POINT('Ctrl Pts',(7.2420712931667,24.0684529590819,-4.52746395914797));
#24600=CARTESIAN_POINT('Ctrl Pts',(6.1215593228575,23.9643987393829,-2.77846127714132));
#24601=CARTESIAN_POINT('Ctrl Pts',(5.39233178046772,23.9122970839216,-2.02040129161139));
#24602=CARTESIAN_POINT('Ctrl Pts',(3.69765257712498,23.8053755570064,-0.839678779680375));
#24603=CARTESIAN_POINT('Ctrl Pts',(2.75247326215505,23.7550150562583,-0.422476472920795));
#24604=CARTESIAN_POINT('Ctrl Pts',(0.735688572314485,23.6505918186215,0.0345284891707951));
#24605=CARTESIAN_POINT('Ctrl Pts',(-0.318384469253613,23.5960149863692,
0.0620656974416982));
#24606=CARTESIAN_POINT('Ctrl Pts',(-2.36232482748936,23.49018570731,-0.290032971156351));
#24607=CARTESIAN_POINT('Ctrl Pts',(-3.33346000867118,23.4403280501711,-0.660664150701976));
#24608=CARTESIAN_POINT('Ctrl Pts',(-5.07935293483514,23.3339880940002,-1.75178765582861));
#24609=CARTESIAN_POINT('Ctrl Pts',(-5.8375698374364,23.2807466706889,-2.46163280366343));
#24610=CARTESIAN_POINT('Ctrl Pts',(-7.05508863841836,23.1780879761606,-4.1507764548021));
#24611=CARTESIAN_POINT('Ctrl Pts',(-7.49477280115995,23.1233551647315,-5.11939993917488));
#24612=CARTESIAN_POINT('Ctrl Pts',(-7.96374159160696,23.0162032347313,-7.14300852639246));
#24613=CARTESIAN_POINT('Ctrl Pts',(-7.99972513178049,22.9667573095989,-8.175875293155));
#24614=CARTESIAN_POINT('Ctrl Pts',(-7.67519193208713,22.8613172543984,-10.2116499836502));
#24615=CARTESIAN_POINT('Ctrl Pts',(-7.31254814444144,22.8071240726913,-11.1943468829651));
#24616=CARTESIAN_POINT('Ctrl Pts',(-6.22935447415169,22.7025945863368,-12.9651264842601));
#24617=CARTESIAN_POINT('Ctrl Pts',(-5.5190149938795,22.6512135864572,-13.7359830183141));
#24618=CARTESIAN_POINT('Ctrl Pts',(-3.85314485337722,22.5444176707724,-14.9522304452467));
#24619=CARTESIAN_POINT('Ctrl Pts',(-2.91670240612869,22.4935183630391,-15.3904147002793));
#24620=CARTESIAN_POINT('Ctrl Pts',(-1.29256784029279,22.4094254052846,-15.7959532941412));
#24621=CARTESIAN_POINT('Ctrl Pts',(-0.646739751238422,22.3759863077173,
-15.875));
#24622=CARTESIAN_POINT('Ctrl Pts',(5.96744875736022E-14,22.3425000069372,
-15.875));
#24623=CARTESIAN_POINT('Ctrl Pts',(-6.36990460378684E-14,22.0250000000001,
-15.875));
#24624=CARTESIAN_POINT('Ctrl Pts',(-0.949477891510335,22.074161200001,-15.875));
#24625=CARTESIAN_POINT('Ctrl Pts',(-1.89208534878509,22.1218736784768,-15.7046193009312));
#24626=CARTESIAN_POINT('Ctrl Pts',(-3.75092248326721,22.22091379634,-15.0088096691342));
#24627=CARTESIAN_POINT('Ctrl Pts',(-4.63908363095019,22.2747999246053,-14.4606577314775));
#24628=CARTESIAN_POINT('Ctrl Pts',(-6.14924084972979,22.380677195981,-13.060274847696));
#24629=CARTESIAN_POINT('Ctrl Pts',(-6.75905812878465,22.4300820990418,-12.2236544338043));
#24630=CARTESIAN_POINT('Ctrl Pts',(-7.63659592255119,22.5367202762854,-10.343230987385));
#24631=CARTESIAN_POINT('Ctrl Pts',(-7.88743301566424,22.5914348158204,-9.31361842665414));
#24632=CARTESIAN_POINT('Ctrl Pts',(-7.97306761740581,22.6949093830429,-7.24013498608011));
#24633=CARTESIAN_POINT('Ctrl Pts',(-7.8163219568117,22.7466803925623,-6.21661270669918));
#24634=CARTESIAN_POINT('Ctrl Pts',(-7.11913434193015,22.8532950466548,-4.27806763088598));
#24635=CARTESIAN_POINT('Ctrl Pts',(-6.58228163977797,22.9039007232003,-3.38260125949016));
#24636=CARTESIAN_POINT('Ctrl Pts',(-5.19122591377799,23.0090123617593,-1.84344654635718));
#24637=CARTESIAN_POINT('Ctrl Pts',(-4.34864002346912,23.0633959832718,-1.21621891854341));
#24638=CARTESIAN_POINT('Ctrl Pts',(-2.48493043657753,23.1684396065758,-0.32985129266046));
#24639=CARTESIAN_POINT('Ctrl Pts',(-1.48444474350808,23.2181397744191,-0.0731761849580272));
#24640=CARTESIAN_POINT('Ctrl Pts',(0.584239367992702,23.3252502129597,0.0476526856448932));
#24641=CARTESIAN_POINT('Ctrl Pts',(1.63304041198226,23.3788605119783,-0.0993363107181023));
#24642=CARTESIAN_POINT('Ctrl Pts',(3.59655181222106,23.4820300205898,-0.786758499983969));
#24643=CARTESIAN_POINT('Ctrl Pts',(4.49450140548816,23.5356971537053,-1.31424201288508));
#24644=CARTESIAN_POINT('Ctrl Pts',(6.0349478213324,23.641797199696,-2.68025536507279));
#24645=CARTESIAN_POINT('Ctrl Pts',(6.6639671087408,23.6913334759273,-3.50458001374237));
#24646=CARTESIAN_POINT('Ctrl Pts',(7.58169225846245,23.7976250644636,-5.36490745307786));
#24647=CARTESIAN_POINT('Ctrl Pts',(7.85458790513208,23.8522936097784,-6.38641872853286));
#24648=CARTESIAN_POINT('Ctrl Pts',(7.98667256090725,23.9562149288905,-8.45388203717645));
#24649=CARTESIAN_POINT('Ctrl Pts',(7.85341991252846,24.007273438891,-9.47940961671702));
#24650=CARTESIAN_POINT('Ctrl Pts',(7.20039415369292,24.114034653206,-11.4352800183161));
#24651=CARTESIAN_POINT('Ctrl Pts',(6.68210414203887,24.1652456157174,-12.3454014227126));
#24652=CARTESIAN_POINT('Ctrl Pts',(5.32434865180305,24.269894965243,-13.9151999953278));
#24653=CARTESIAN_POINT('Ctrl Pts',(4.4977673852279,24.3241294065212,-14.5595543047395));
#24654=CARTESIAN_POINT('Ctrl Pts',(2.6562899853584,24.4294944312366,-15.4870825809801));
#24655=CARTESIAN_POINT('Ctrl Pts',(1.66143917596496,24.4789755181781,-15.7663991960582));
#24656=CARTESIAN_POINT('Ctrl Pts',(0.427422115449422,24.5428693276696,-15.8663795220757));
#24657=CARTESIAN_POINT('Ctrl Pts',(0.21358319137833,24.5539412843816,-15.875));
#24658=CARTESIAN_POINT('Ctrl Pts',(-4.76702011198427E-14,24.565,-15.875));
#24659=CARTESIAN_POINT('Origin',(0.,-18.001,-7.93750000000004));
#24660=CARTESIAN_POINT('',(7.49369629108171E-15,27.4225000069372,-15.875));
#24661=CARTESIAN_POINT('',(-5.16978508354899E-15,27.1050000000001,-15.875));
#24662=CARTESIAN_POINT('',(-9.72063396823211E-16,-18.001,-15.875));
#24663=CARTESIAN_POINT('Ctrl Pts',(9.5062846483529E-14,27.4225000069372,
-15.875));
#24664=CARTESIAN_POINT('Ctrl Pts',(0.624219539852169,27.3901797371156,-15.875));
#24665=CARTESIAN_POINT('Ctrl Pts',(1.24771112812793,27.3578971585064,-15.801362942656));
#24666=CARTESIAN_POINT('Ctrl Pts',(2.86701695199915,27.2740542189479,-15.4116256134532));
#24667=CARTESIAN_POINT('Ctrl Pts',(3.81924123505487,27.2226292642049,-14.9728242497032));
#24668=CARTESIAN_POINT('Ctrl Pts',(5.48912016231564,27.1158247420042,-13.7618116498142));
#24669=CARTESIAN_POINT('Ctrl Pts',(6.19410644258195,27.064964283629,-13.0056376260485));
#24670=CARTESIAN_POINT('Ctrl Pts',(7.28947994752642,26.9609089493055,-11.2484443263014));
#24671=CARTESIAN_POINT('Ctrl Pts',(7.6619928698852,26.9062603168654,-10.2597050461275));
#24672=CARTESIAN_POINT('Ctrl Pts',(7.99903184162878,26.800083823255,-8.21303851826056));
#24673=CARTESIAN_POINT('Ctrl Pts',(7.96746790208441,26.7504816783959,-7.17601383432028));
#24674=CARTESIAN_POINT('Ctrl Pts',(7.51002828234806,26.644317832783,-5.16872469739288));
#24675=CARTESIAN_POINT('Ctrl Pts',(7.08732731533967,26.5907251275606,-4.21773572336723));
#24676=CARTESIAN_POINT('Ctrl Pts',(5.89088422543125,26.487731585604,-2.51494425079395));
#24677=CARTESIAN_POINT('Ctrl Pts',(5.12254957469675,26.4337992857223,-1.78392039090943));
#24678=CARTESIAN_POINT('Ctrl Pts',(3.36848207149392,26.326657480458,-0.677700912351653));
#24679=CARTESIAN_POINT('Ctrl Pts',(2.40535199885269,26.2770421281866,-0.304304727598297));
#24680=CARTESIAN_POINT('Ctrl Pts',(0.374502057938519,26.1718906328122,0.0590295397115103));
#24681=CARTESIAN_POINT('Ctrl Pts',(-0.67495984682772,26.1175525517943,0.0392916743172318));
#24682=CARTESIAN_POINT('Ctrl Pts',(-2.70220537666353,26.0125876823283,-0.402670233429265));
#24683=CARTESIAN_POINT('Ctrl Pts',(-3.66081284174792,25.9617990422184,-0.818931376977721));
#24684=CARTESIAN_POINT('Ctrl Pts',(-5.35605729947494,25.8551355586809,-1.99039704350108));
#24685=CARTESIAN_POINT('Ctrl Pts',(-6.07871747524366,25.8036085570719,-2.73131110334026));
#24686=CARTESIAN_POINT('Ctrl Pts',(-7.21494557234268,25.6999861967515,-4.46643733006872));
#24687=CARTESIAN_POINT('Ctrl Pts',(-7.6099153643053,25.6452836412246,-5.44897497305318));
#24688=CARTESIAN_POINT('Ctrl Pts',(-7.99095461069713,25.5387542472933,-7.48851146161607));
#24689=CARTESIAN_POINT('Ctrl Pts',(-7.98202232718952,25.4893198157644,-8.52423487824865));
#24690=CARTESIAN_POINT('Ctrl Pts',(-7.56898602067955,25.3833672804673,-10.5416603459946));
#24691=CARTESIAN_POINT('Ctrl Pts',(-7.16614950446568,25.3295490005744,-11.5036845246756));
#24692=CARTESIAN_POINT('Ctrl Pts',(-6.00744541886707,25.2260123198636,-13.2297679230054));
#24693=CARTESIAN_POINT('Ctrl Pts',(-5.25866306136744,25.1730517413319,-13.9744047651811));
#24694=CARTESIAN_POINT('Ctrl Pts',(-3.53424516529992,25.0660131501615,-15.1180419981786));
#24695=CARTESIAN_POINT('Ctrl Pts',(-2.58006791475045,25.0160884094762,-15.5134055519264));
#24696=CARTESIAN_POINT('Ctrl Pts',(-1.05678757155941,24.9372173896464,-15.8222328513334));
#24697=CARTESIAN_POINT('Ctrl Pts',(-0.528417728937034,24.9098599379989,
-15.875));
#24698=CARTESIAN_POINT('Ctrl Pts',(8.18789480661053E-15,24.8825000069372,
-15.875));
#24699=CARTESIAN_POINT('Ctrl Pts',(-1.17961196366423E-14,24.565,-15.875));
#24700=CARTESIAN_POINT('Ctrl Pts',(-0.836467978306689,24.6083098758209,
-15.875));
#24701=CARTESIAN_POINT('Ctrl Pts',(-1.66901604868968,24.6513687341673,-15.7427642526738));
#24702=CARTESIAN_POINT('Ctrl Pts',(-3.44503997400206,24.7434340320891,-15.162152007294));
#24703=CARTESIAN_POINT('Ctrl Pts',(-4.35204519100589,24.796865006184,-14.6548922502149));
#24704=CARTESIAN_POINT('Ctrl Pts',(-5.92144264644372,24.9031505594052,-13.3226311528391));
#24705=CARTESIAN_POINT('Ctrl Pts',(-6.56905306265197,24.952925693415,-12.5103214269728));
#24706=CARTESIAN_POINT('Ctrl Pts',(-7.52528735905546,25.0588559665969,-10.6698437725775));
#24707=CARTESIAN_POINT('Ctrl Pts',(-7.81923854442363,25.1134553691784,-9.65657797110715));
#24708=CARTESIAN_POINT('Ctrl Pts',(-7.99593679652942,25.2177768367742,-7.59548449089693));
#24709=CARTESIAN_POINT('Ctrl Pts',(-7.88522677580753,25.2682687366265,-6.56811852720181));
#24710=CARTESIAN_POINT('Ctrl Pts',(-7.27465739000588,25.3751581999211,-4.59584880005299));
#24711=CARTESIAN_POINT('Ctrl Pts',(-6.77426313425,25.4270586590243,-3.67176122202902));
#24712=CARTESIAN_POINT('Ctrl Pts',(-5.44856714317156,25.5312410147699,-2.07318110685299));
#24713=CARTESIAN_POINT('Ctrl Pts',(-4.63752074881183,25.5853094391607,-1.41289989536927));
#24714=CARTESIAN_POINT('Ctrl Pts',(-2.81768173593427,25.6909496227162,-0.446547711794352));
#24715=CARTESIAN_POINT('Ctrl Pts',(-1.82825937663462,25.7403380540275,-0.1457641783938));
#24716=CARTESIAN_POINT('Ctrl Pts',(0.237099502352091,25.8472763217129,0.065844563319637));
#24717=CARTESIAN_POINT('Ctrl Pts',(1.29420484576369,25.9020101577234,-0.0359189862404865));
#24718=CARTESIAN_POINT('Ctrl Pts',(3.28397585660572,26.0050347057353,-0.638538942803915));
#24719=CARTESIAN_POINT('Ctrl Pts',(4.2002099962157,26.0575929837782,-1.12442905110605));
#24720=CARTESIAN_POINT('Ctrl Pts',(5.79974737504025,26.1640571208062,-2.42107404430918));
#24721=CARTESIAN_POINT('Ctrl Pts',(6.46681553222913,26.2141991661854,-3.22068377432052));
#24722=CARTESIAN_POINT('Ctrl Pts',(7.46292553316076,26.319724597504,-5.03998370845816));
#24723=CARTESIAN_POINT('Ctrl Pts',(7.77858166455462,26.3742261613421,-6.0442102870369));
#24724=CARTESIAN_POINT('Ctrl Pts',(8.00158613360409,26.4789325838569,-8.09807543001832));
#24725=CARTESIAN_POINT('Ctrl Pts',(7.91426666814584,26.5289590715126,-9.12726125824446));
#24726=CARTESIAN_POINT('Ctrl Pts',(7.34783370140172,26.6359683838815,-11.1163056100658));
#24727=CARTESIAN_POINT('Ctrl Pts',(6.86609704238139,26.6886935677963,-12.0547755141607));
#24728=CARTESIAN_POINT('Ctrl Pts',(5.57375337988629,26.792367957767,-13.6825703331671));
#24729=CARTESIAN_POINT('Ctrl Pts',(4.77898461373321,26.8462413617665,-14.3588477598749));
#24730=CARTESIAN_POINT('Ctrl Pts',(2.98189317687904,26.9521332238845,-15.3647789989823));
#24731=CARTESIAN_POINT('Ctrl Pts',(1.99812686687186,27.0015428100985,-15.6875743213914));
#24732=CARTESIAN_POINT('Ctrl Pts',(0.654344113010902,27.0711199675143,-15.8547946639326));
#24733=CARTESIAN_POINT('Ctrl Pts',(0.326990712642387,27.0880693732141,-15.875));
#24734=CARTESIAN_POINT('Ctrl Pts',(-5.25968157916168E-14,27.1050000000001,
-15.875));
#24735=CARTESIAN_POINT('Origin',(0.,-18.001,-7.93750000000004));
#24736=CARTESIAN_POINT('',(-1.32535964816009E-14,29.9625000069372,-15.875));
#24737=CARTESIAN_POINT('',(-4.26571593994078E-14,29.645,-15.875));
#24738=CARTESIAN_POINT('',(-9.72063396823211E-16,-18.001,-15.875));
#24739=CARTESIAN_POINT('Ctrl Pts',(-4.48252546192407E-14,29.9625000069372,
-15.875));
#24740=CARTESIAN_POINT('Ctrl Pts',(0.736573960655214,29.924362352423,-15.875));
#24741=CARTESIAN_POINT('Ctrl Pts',(1.47105355996765,29.8863331378396,-15.772465740066));
#24742=CARTESIAN_POINT('Ctrl Pts',(3.18774470741065,29.7974478698477,-15.2816389743965));
#24743=CARTESIAN_POINT('Ctrl Pts',(4.12686094412051,29.7444249917232,-14.7980669295615));
#24744=CARTESIAN_POINT('Ctrl Pts',(5.74561976414415,29.6373789620042,-13.5087580372874));
#24745=CARTESIAN_POINT('Ctrl Pts',(6.41526615853753,29.5874791981015,-12.7224187313828));
#24746=CARTESIAN_POINT('Ctrl Pts',(7.42815971898147,29.4826519431958,-10.9227503105544));
#24747=CARTESIAN_POINT('Ctrl Pts',(7.75543374230582,29.4281887458617,-9.92307774094497));
#24748=CARTESIAN_POINT('Ctrl Pts',(8.00402649279823,29.3228044342571,-7.86376051477762));
#24749=CARTESIAN_POINT('Ctrl Pts',(7.92659261093737,29.2725134828056,-6.82440623067985));
#24750=CARTESIAN_POINT('Ctrl Pts',(7.37956520218366,29.1659957601636,-4.83903957989797));
#24751=CARTESIAN_POINT('Ctrl Pts',(6.91725543998198,29.1137233616627,-3.91137218888092));
#24752=CARTESIAN_POINT('Ctrl Pts',(5.65038778333555,29.0105394930011,-2.26463030061079));
#24753=CARTESIAN_POINT('Ctrl Pts',(4.85053034642538,28.9558097104299,-1.56721777465549));
#24754=CARTESIAN_POINT('Ctrl Pts',(3.04827483309507,28.8489726456425,-0.537336623884139));
#24755=CARTESIAN_POINT('Ctrl Pts',(2.06829346615786,28.7995902189997,-0.205969067278297));
#24756=CARTESIAN_POINT('Ctrl Pts',(0.0263597995014314,28.6938648405862,
0.0671743779869568));
#24757=CARTESIAN_POINT('Ctrl Pts',(-1.01672316573496,28.6398570424794,0.0023935713156336));
#24758=CARTESIAN_POINT('Ctrl Pts',(-3.02573001584092,28.5358365187321,-0.525708220472481));
#24759=CARTESIAN_POINT('Ctrl Pts',(-3.97158882065666,28.4836811578961,-0.986505905423148));
#24760=CARTESIAN_POINT('Ctrl Pts',(-5.61647909717162,28.3767514102684,-2.23602711384972));
#24761=CARTESIAN_POINT('Ctrl Pts',(-6.3041434221088,28.3264238453969,-3.00704397924283));
#24762=CARTESIAN_POINT('Ctrl Pts',(-7.35921305036772,28.2219743844626,-4.7853365210284));
#24763=CARTESIAN_POINT('Ctrl Pts',(-7.70959913301805,28.1674037307671,-5.77968169536413));
#24764=CARTESIAN_POINT('Ctrl Pts',(-8.003354843952,28.0616011386154,-7.83281881041147));
#24765=CARTESIAN_POINT('Ctrl Pts',(-7.94941043789711,28.0117206267662,-8.87103382953876));
#24766=CARTESIAN_POINT('Ctrl Pts',(-7.44817485664906,27.9053692493889,-10.8679010937008));
#24767=CARTESIAN_POINT('Ctrl Pts',(-7.00603971353237,27.8521917627398,-11.8075725102872));
#24768=CARTESIAN_POINT('Ctrl Pts',(-5.77352473680867,27.74949960399,-13.4854401062041));
#24769=CARTESIAN_POINT('Ctrl Pts',(-4.9872689275275,27.6947661372597,-14.2016947213343));
#24770=CARTESIAN_POINT('Ctrl Pts',(-3.20621013981998,27.5876327327036,-15.2704878517884));
#24771=CARTESIAN_POINT('Ctrl Pts',(-2.23447144379235,27.5381944307113,-15.6225282357278));
#24772=CARTESIAN_POINT('Ctrl Pts',(-0.817251851957353,27.4648149276997,
-15.8434703725885));
#24773=CARTESIAN_POINT('Ctrl Pts',(-0.408470071868316,27.4436493976466,
-15.875));
#24774=CARTESIAN_POINT('Ctrl Pts',(7.08461067588928E-14,27.4225000069372,
-15.875));
#24775=CARTESIAN_POINT('Ctrl Pts',(-5.10702591327572E-14,27.1050000000001,
-15.875));
#24776=CARTESIAN_POINT('Ctrl Pts',(-0.717914112981769,27.1421715019459,
-15.875));
#24777=CARTESIAN_POINT('Ctrl Pts',(-1.43407996200344,27.1792524838758,-15.7775953996811));
#24778=CARTESIAN_POINT('Ctrl Pts',(-3.11674440141664,27.2663759480241,-15.309192321087));
#24779=CARTESIAN_POINT('Ctrl Pts',(-4.0423031180092,27.3180994138876,-14.8451723426533));
#24780=CARTESIAN_POINT('Ctrl Pts',(-5.67239094602482,27.4247234872727,-13.58532121545));
#24781=CARTESIAN_POINT('Ctrl Pts',(-6.35934945246318,27.47536311323,-12.7988363573248));
#24782=CARTESIAN_POINT('Ctrl Pts',(-7.39576329636799,27.5804469591558,-11.0015994225818));
#24783=CARTESIAN_POINT('Ctrl Pts',(-7.73324216548751,27.6348220956183,-10.0070309028449));
#24784=CARTESIAN_POINT('Ctrl Pts',(-8.00316616355678,27.7398865875611,-7.96113935087222));
#24785=CARTESIAN_POINT('Ctrl Pts',(-7.93955543190281,27.7895695346163,-6.93019976657644));
#24786=CARTESIAN_POINT('Ctrl Pts',(-7.41794390221256,27.8966860832206,-4.92441434922844));
#24787=CARTESIAN_POINT('Ctrl Pts',(-6.95521173491136,27.9503570671105,-3.97149099523772));
#24788=CARTESIAN_POINT('Ctrl Pts',(-5.69674018400867,28.0534931347906,-2.31476351275529));
#24789=CARTESIAN_POINT('Ctrl Pts',(-4.91860850865424,28.1071462184412,-1.62282642394335));
#24790=CARTESIAN_POINT('Ctrl Pts',(-3.14485764138248,28.213258720227,-0.577519825724921));
#24791=CARTESIAN_POINT('Ctrl Pts',(-2.16685228936275,28.262806699111,-0.232682623541554));
#24792=CARTESIAN_POINT('Ctrl Pts',(-0.114404512256726,28.3690764675427,
0.067930054342613));
#24793=CARTESIAN_POINT('Ctrl Pts',(0.94137007018476,28.4237414006258,0.0132189985048882));
#24794=CARTESIAN_POINT('Ctrl Pts',(2.94896136887821,28.5276886312436,-0.497265377597983));
#24795=CARTESIAN_POINT('Ctrl Pts',(3.88366732438073,28.5787082396742,-0.93959406668474));
#24796=CARTESIAN_POINT('Ctrl Pts',(5.54382016817213,28.6854778532263,-2.16284643685243));
#24797=CARTESIAN_POINT('Ctrl Pts',(6.25041788147492,28.7367289402747,-2.93621935226714));
#24798=CARTESIAN_POINT('Ctrl Pts',(7.32616862873122,28.8413496814412,-4.71127046121473));
#24799=CARTESIAN_POINT('Ctrl Pts',(7.68482120007732,28.8955743650117,-5.69590390880756));
#24800=CARTESIAN_POINT('Ctrl Pts',(8.00065474910145,29.0009575889456,-7.73335118728829));
#24801=CARTESIAN_POINT('Ctrl Pts',(7.96026661063342,29.0504295279356,-8.76591919118594));
#24802=CARTESIAN_POINT('Ctrl Pts',(7.48263755651254,29.1576366540103,-10.787834781398));
#24803=CARTESIAN_POINT('Ctrl Pts',(7.03861107572573,29.2123372659245,-11.7547821623659));
#24804=CARTESIAN_POINT('Ctrl Pts',(5.81335784329496,29.314924048782,-13.4391822302741));
#24805=CARTESIAN_POINT('Ctrl Pts',(5.05163085685929,29.3683402581132,-14.1459151738609));
#24806=CARTESIAN_POINT('Ctrl Pts',(3.30099691448562,29.4746358794488,-15.2290564673484));
#24807=CARTESIAN_POINT('Ctrl Pts',(2.32866255484483,29.5244286348141,-15.5952242616502));
#24808=CARTESIAN_POINT('Ctrl Pts',(0.87846121798129,29.5995158365285,-15.838565031241));
#24809=CARTESIAN_POINT('Ctrl Pts',(0.439095759214256,29.6222649003928,-15.875));
#24810=CARTESIAN_POINT('Ctrl Pts',(-3.99680288865056E-14,29.645,-15.875));
#24811=CARTESIAN_POINT('Origin',(0.,-18.001,-7.93750000000004));
#24812=CARTESIAN_POINT('',(3.05280419258108E-15,32.5025000069372,-15.875));
#24813=CARTESIAN_POINT('',(2.84491558808815E-14,32.1850000000001,-15.875));
#24814=CARTESIAN_POINT('',(-9.72063396823211E-16,-18.001,-15.875));
#24815=CARTESIAN_POINT('Ctrl Pts',(-1.01307850997046E-14,32.5025000069372,
-15.875));
#24816=CARTESIAN_POINT('Ctrl Pts',(0.849805888356549,32.4584995329788,-15.875));
#24817=CARTESIAN_POINT('Ctrl Pts',(1.69524300201692,32.414903306185,-15.7385137921434));
#24818=CARTESIAN_POINT('Ctrl Pts',(3.50299454566702,32.3208921513219,-15.137633521164));
#24819=CARTESIAN_POINT('Ctrl Pts',(4.42623973950424,32.2661581245547,-14.6099102164331));
#24820=CARTESIAN_POINT('Ctrl Pts',(5.99104322325474,32.1590439672215,-13.2440996243987));
#24821=CARTESIAN_POINT('Ctrl Pts',(6.6249795417268,32.1096130241932,-12.4277417526968));
#24822=CARTESIAN_POINT('Ctrl Pts',(7.55362584166265,32.0041354131546,-10.5874926427543));
#24823=CARTESIAN_POINT('Ctrl Pts',(7.83491766257849,31.9499639421575,-9.57880377695661));
#24824=CARTESIAN_POINT('Ctrl Pts',(7.99369332499519,31.8454964233445,-7.50892096202494));
#24825=CARTESIAN_POINT('Ctrl Pts',(7.86907943675707,31.7940255725315,-6.46765050687525));
#24826=CARTESIAN_POINT('Ctrl Pts',(7.23036751456396,31.6872122133539,-4.5060703270135));
#24827=CARTESIAN_POINT('Ctrl Pts',(6.72774208091398,31.6363913721743,-3.60271706817703));
#24828=CARTESIAN_POINT('Ctrl Pts',(5.39283838888249,31.5323085621847,-2.02008115994509));
#24829=CARTESIAN_POINT('Ctrl Pts',(4.56677207757762,31.4776643982301,-1.36155532801674));
#24830=CARTESIAN_POINT('Ctrl Pts',(2.72309872699471,31.3715122044493,-0.411184564370692));
#24831=CARTESIAN_POINT('Ctrl Pts',(1.72653338920418,31.3218948775435,-0.122146758303137));
#24832=CARTESIAN_POINT('Ctrl Pts',(-0.324117470713751,31.2157181482505,
0.0600801418958527));
#24833=CARTESIAN_POINT('Ctrl Pts',(-1.35887810786185,31.1621412560545,-0.0495340621609275));
#24834=CARTESIAN_POINT('Ctrl Pts',(-3.34733525420087,31.0591847361201,-0.664081986129089));
#24835=CARTESIAN_POINT('Ctrl Pts',(-4.27954278064386,31.0051838630904,-1.17043135315008));
#24836=CARTESIAN_POINT('Ctrl Pts',(-5.87188660873315,30.8980357025591,-2.49945319684862));
#24837=CARTESIAN_POINT('Ctrl Pts',(-6.52342049862927,30.8484363956693,-3.30107633199719));
#24838=CARTESIAN_POINT('Ctrl Pts',(-7.49368309383774,30.7432628065576,-5.12162956841538));
#24839=CARTESIAN_POINT('Ctrl Pts',(-7.79765378547948,30.6889345839556,-6.12613285266895));
#24840=CARTESIAN_POINT('Ctrl Pts',(-8.00073138203963,30.5840007572664,-8.19109063495698));
#24841=CARTESIAN_POINT('Ctrl Pts',(-7.89947037271715,30.5331722793238,-9.23147753227341));
#24842=CARTESIAN_POINT('Ctrl Pts',(-7.30609195072424,30.4264987511991,-11.2049478427975));
#24843=CARTESIAN_POINT('Ctrl Pts',(-6.82338854754,30.3750211664139,-12.1203695415557));
#24844=CARTESIAN_POINT('Ctrl Pts',(-5.52199240182528,30.2713682810967,-13.7349980822292));
#24845=CARTESIAN_POINT('Ctrl Pts',(-4.70870678348807,30.2166685819792,-14.4129398140733));
#24846=CARTESIAN_POINT('Ctrl Pts',(-2.8853352338182,30.1101623486631,-15.4028867093612));
#24847=CARTESIAN_POINT('Ctrl Pts',(-1.8969813878097,30.0607201785052,-15.7130135095793));
#24848=CARTESIAN_POINT('Ctrl Pts',(-0.585223021794811,29.9928011506256,
-15.8588382366372));
#24849=CARTESIAN_POINT('Ctrl Pts',(-0.292446435800955,29.9776420316737,
-15.875));
#24850=CARTESIAN_POINT('Ctrl Pts',(-5.87030424270552E-14,29.9625000069372,
-15.875));
#24851=CARTESIAN_POINT('Ctrl Pts',(-4.53803661315533E-14,29.645,-15.875));
#24852=CARTESIAN_POINT('Ctrl Pts',(-0.60076652805944,29.6761059411745,-15.875));
#24853=CARTESIAN_POINT('Ctrl Pts',(-1.20102819352252,29.7071857420343,-15.8067928930804));
#24854=CARTESIAN_POINT('Ctrl Pts',(-2.78647271976851,29.7892754422182,-15.4399982407669));
#24855=CARTESIAN_POINT('Ctrl Pts',(-3.72985706541699,29.8397374734669,-15.0184674546151));
#24856=CARTESIAN_POINT('Ctrl Pts',(-5.4186118431039,29.946634128663,-13.8304079101059));
#24857=CARTESIAN_POINT('Ctrl Pts',(-6.14395063807967,29.998578603021,-13.0697001623927));
#24858=CARTESIAN_POINT('Ctrl Pts',(-7.25681384791781,30.1027326597859,-11.3161848081354));
#24859=CARTESIAN_POINT('Ctrl Pts',(-7.63531699691702,30.1567905903446,-10.3413875378226));
#24860=CARTESIAN_POINT('Ctrl Pts',(-7.99457161687568,30.2624460277761,-8.31252065008465));
#24861=CARTESIAN_POINT('Ctrl Pts',(-7.97618389438668,30.31183249889,-7.27849297393089));
#24862=CARTESIAN_POINT('Ctrl Pts',(-7.54174953490999,30.4187531380881,-5.24836040346573));
#24863=CARTESIAN_POINT('Ctrl Pts',(-7.11959642041862,30.4734864628244,-4.2740303122445));
#24864=CARTESIAN_POINT('Ctrl Pts',(-5.93394869755091,30.576539362472,-2.56652580710964));
#24865=CARTESIAN_POINT('Ctrl Pts',(-5.18973799987701,30.6290462253603,-1.84438178734286));
#24866=CARTESIAN_POINT('Ctrl Pts',(-3.46373674247435,30.7355199208385,-0.721485316793999));
#24867=CARTESIAN_POINT('Ctrl Pts',(-2.49748880602533,30.7856873032105,-0.332835461595449));
#24868=CARTESIAN_POINT('Ctrl Pts',(-0.459893950304063,30.8911880306299,
0.0549386168117478));
#24869=CARTESIAN_POINT('Ctrl Pts',(0.592598519303625,30.9456830254692,0.0461972746405091));
#24870=CARTESIAN_POINT('Ctrl Pts',(2.61526999568577,31.0504110637688,-0.373671127574245));
#24871=CARTESIAN_POINT('Ctrl Pts',(3.56762371680106,31.1004141393016,-0.773479665864678));
#24872=CARTESIAN_POINT('Ctrl Pts',(5.28600956243452,31.2074300555214,-1.92467424608267));
#24873=CARTESIAN_POINT('Ctrl Pts',(6.03082090822791,31.2602070115457,-2.67205198013382));
#24874=CARTESIAN_POINT('Ctrl Pts',(7.18180568473254,31.363850874488,-4.40282013516036));
#24875=CARTESIAN_POINT('Ctrl Pts',(7.58055982035965,31.4177121364128,-5.36704361649729));
#24876=CARTESIAN_POINT('Ctrl Pts',(7.98452790924092,31.5236177119233,-7.38646189178608));
#24877=CARTESIAN_POINT('Ctrl Pts',(7.98884729936329,31.5730321441085,-8.42190857812903));
#24878=CARTESIAN_POINT('Ctrl Pts',(7.59881305327393,31.6796302915114,-10.4599186239401));
#24879=CARTESIAN_POINT('Ctrl Pts',(7.19925811072238,31.7343407022857,-11.4411259814758));
#24880=CARTESIAN_POINT('Ctrl Pts',(6.05469257606037,31.8378705213091,-13.1716639298901));
#24881=CARTESIAN_POINT('Ctrl Pts',(5.32841029609977,31.889549405654,-13.9094359049476));
#24882=CARTESIAN_POINT('Ctrl Pts',(3.62798333001476,31.9961823518139,-15.0727650575699));
#24883=CARTESIAN_POINT('Ctrl Pts',(2.66808101180657,32.0468545356208,-15.4843950802912));
#24884=CARTESIAN_POINT('Ctrl Pts',(1.11053836543475,32.127499557725,-15.8167122830523));
#24885=CARTESIAN_POINT('Ctrl Pts',(0.555369956406371,32.1562445610946,-15.875));
#24886=CARTESIAN_POINT('Ctrl Pts',(1.24483756636096E-13,32.1850000000001,
-15.875));
#24887=CARTESIAN_POINT('Origin',(0.,-18.001,-7.93750000000004));
#24888=CARTESIAN_POINT('',(1.4501979134028E-14,35.0425000069372,-15.875));
#24889=CARTESIAN_POINT('',(-1.66564366207583E-15,34.7250000000001,-15.875));
#24890=CARTESIAN_POINT('',(-9.72063396823211E-16,-18.001,-15.875));
#24891=CARTESIAN_POINT('Ctrl Pts',(-9.99200722162641E-15,35.0425000069372,
-15.875));
#24892=CARTESIAN_POINT('Ctrl Pts',(0.970090933462564,34.9922715236566,-15.875));
#24893=CARTESIAN_POINT('Ctrl Pts',(1.93248681409951,34.9437065644586,-15.6971471683423));
#24894=CARTESIAN_POINT('Ctrl Pts',(3.81822285928236,34.8427334070056,-14.9748445200943));
#24895=CARTESIAN_POINT('Ctrl Pts',(4.71329600152565,34.7880367669905,-14.4095741740582));
#24896=CARTESIAN_POINT('Ctrl Pts',(6.21605595886414,34.6815544612065,-12.9791294950926));
#24897=CARTESIAN_POINT('Ctrl Pts',(6.81519863680074,34.6321037804164,-12.1339790477124));
#24898=CARTESIAN_POINT('Ctrl Pts',(7.66110176306296,34.5261202464978,-10.2565710316361));
#24899=CARTESIAN_POINT('Ctrl Pts',(7.89755691956149,34.472331596896,-9.24108798867198));
#24900=CARTESIAN_POINT('Ctrl Pts',(7.96862631735271,34.3688680419953,-7.16309565896684));
#24901=CARTESIAN_POINT('Ctrl Pts',(7.79726863331709,34.3157805716978,-6.12047324327451));
#24902=CARTESIAN_POINT('Ctrl Pts',(7.06808748209868,34.2087269605643,-4.18340938579211));
#24903=CARTESIAN_POINT('Ctrl Pts',(6.5257636328328,34.1588522707425,-3.30441334610998));
#24904=CARTESIAN_POINT('Ctrl Pts',(5.12486611018882,34.0539998585826,-1.78732241538885));
#24905=CARTESIAN_POINT('Ctrl Pts',(4.27441882470329,33.9995451690497,-1.16857990293053));
#24906=CARTESIAN_POINT('Ctrl Pts',(2.3913441993438,33.8941911946945,-0.298668390678644));
#24907=CARTESIAN_POINT('Ctrl Pts',(1.37834973008372,33.8438669417104,-0.0526791921381577));
#24908=CARTESIAN_POINT('Ctrl Pts',(-0.679103325210624,33.7373380145512,
0.0372729376288422));
#24909=CARTESIAN_POINT('Ctrl Pts',(-1.70386196214072,33.6851246449656,-0.117350434261928));
#24910=CARTESIAN_POINT('Ctrl Pts',(-3.66013477795052,33.5819073436672,-0.816306061666204));
#24911=CARTESIAN_POINT('Ctrl Pts',(-4.5696032899542,33.527178784434,-1.36281168890308));
#24912=CARTESIAN_POINT('Ctrl Pts',(-6.1038472063139,33.4203636326017,-2.76085913608331));
#24913=CARTESIAN_POINT('Ctrl Pts',(-6.7206167227976,33.3709808813071,-3.59148092125172));
#24914=CARTESIAN_POINT('Ctrl Pts',(-7.60850475049445,33.2652377919484,-5.45036439257499));
#24915=CARTESIAN_POINT('Ctrl Pts',(-7.86766437450084,33.2112432397888,-6.46265166913726));
#24916=CARTESIAN_POINT('Ctrl Pts',(-7.98317485724195,33.1072575635412,-8.53680718435962));
#24917=CARTESIAN_POINT('Ctrl Pts',(-7.83559071200281,33.0550463207417,-9.57881433209888));
#24918=CARTESIAN_POINT('Ctrl Pts',(-7.15237728567606,32.9481081623779,-11.5284694538581));
#24919=CARTESIAN_POINT('Ctrl Pts',(-6.63021560611076,32.8978139630681,-12.4198874319169));
#24920=CARTESIAN_POINT('Ctrl Pts',(-5.2626962307764,32.7933376145242,-13.9705626696936));
#24921=CARTESIAN_POINT('Ctrl Pts',(-4.4244432838421,32.7387734553081,-14.6096862254101));
#24922=CARTESIAN_POINT('Ctrl Pts',(-2.56119712677316,32.6329985178308,-15.5207213710765));
#24923=CARTESIAN_POINT('Ctrl Pts',(-1.55655463281693,32.5830938725771,-15.788746995707));
#24924=CARTESIAN_POINT('Ctrl Pts',(-0.35252362084797,32.5207526533491,-15.8691352102942));
#24925=CARTESIAN_POINT('Ctrl Pts',(-0.176167739284417,32.5116214594135,
-15.875));
#24926=CARTESIAN_POINT('Ctrl Pts',(-5.48172618408671E-15,32.5025000069372,
-15.875));
#24927=CARTESIAN_POINT('Ctrl Pts',(1.19348975147204E-13,32.1850000000001,
-15.875));
#24928=CARTESIAN_POINT('Ctrl Pts',(-0.479821973824826,32.2098437843904,
-15.875));
#24929=CARTESIAN_POINT('Ctrl Pts',(-0.95979439088142,32.2346953582927,-15.8314925177406));
#24930=CARTESIAN_POINT('Ctrl Pts',(-2.44052190888781,32.3113631167635,-15.559514895666));
#24931=CARTESIAN_POINT('Ctrl Pts',(-3.4018624930967,32.3610302127626,-15.1817084661653));
#24932=CARTESIAN_POINT('Ctrl Pts',(-5.14999927583338,32.4681524913806,-14.067967661525));
#24933=CARTESIAN_POINT('Ctrl Pts',(-5.91441854190448,32.521881254785,-13.3342017457131));
#24934=CARTESIAN_POINT('Ctrl Pts',(-7.10334001050634,32.6249856054144,-11.6267161052087));
#24935=CARTESIAN_POINT('Ctrl Pts',(-7.52209463175434,32.6786253221975,-10.6734901993414));
#24936=CARTESIAN_POINT('Ctrl Pts',(-7.97067507649972,32.7847494926242,-8.66412824505769));
#24937=CARTESIAN_POINT('Ctrl Pts',(-7.99771737810506,32.834308928385,-7.6273558962722));
#24938=CARTESIAN_POINT('Ctrl Pts',(-7.65190541526759,32.9405579782968,-5.58206645029218));
#24939=CARTESIAN_POINT('Ctrl Pts',(-7.27491157723585,32.9952194098341,-4.5945231904542));
#24940=CARTESIAN_POINT('Ctrl Pts',(-6.1713828811108,33.0991910219691,-2.84167985969742));
#24941=CARTESIAN_POINT('Ctrl Pts',(-5.46287826007856,33.1501742885371,-2.08853424230292));
#24942=CARTESIAN_POINT('Ctrl Pts',(-3.78793941754756,33.2569517942899,-0.885373730014236));
#24943=CARTESIAN_POINT('Ctrl Pts',(-2.83443565213759,33.3082411768288,-0.451051786516673));
#24944=CARTESIAN_POINT('Ctrl Pts',(-0.814360119641338,33.4128348047143,
0.02603283564326));
#24945=CARTESIAN_POINT('Ctrl Pts',(0.23273205517928,33.4670501880172,0.0641746315103381));
#24946=CARTESIAN_POINT('Ctrl Pts',(2.268387340936,33.5724504901527,-0.262433230432161));
#24947=CARTESIAN_POINT('Ctrl Pts',(3.23842845507517,33.6219142003453,-0.618703479819044));
#24948=CARTESIAN_POINT('Ctrl Pts',(5.0150716781271,33.7291050467692,-1.69546154969738));
#24949=CARTESIAN_POINT('Ctrl Pts',(5.79848012757925,33.7838360999378,-2.41555591413844));
#24950=CARTESIAN_POINT('Ctrl Pts',(7.02387583415542,33.8864233216061,-4.09977430173718));
#24951=CARTESIAN_POINT('Ctrl Pts',(7.46184247993154,33.9398022270509,-5.04191207434748));
#24952=CARTESIAN_POINT('Ctrl Pts',(7.95362461121147,34.0461177491235,-7.04112281968223));
#24953=CARTESIAN_POINT('Ctrl Pts',(8.00272599438934,34.0959286274556,-8.0790886997892));
#24954=CARTESIAN_POINT('Ctrl Pts',(7.69962425601701,34.2018141938604,-10.1308741045105));
#24955=CARTESIAN_POINT('Ctrl Pts',(7.3444580136891,34.2564037662479,-11.1240503017925));
#24956=CARTESIAN_POINT('Ctrl Pts',(6.28067601693568,34.3607707854692,-12.8978378399292));
#24957=CARTESIAN_POINT('Ctrl Pts',(5.58927625729154,34.4112031799623,-13.6656632453394));
#24958=CARTESIAN_POINT('Ctrl Pts',(3.93898630872078,34.5181070255036,-14.9069013469801));
#24959=CARTESIAN_POINT('Ctrl Pts',(2.99174533661782,34.5700961395091,-15.362963791741));
#24960=CARTESIAN_POINT('Ctrl Pts',(1.33422262317561,34.6559178383083,-15.7907462141402));
#24961=CARTESIAN_POINT('Ctrl Pts',(0.667699158686123,34.6904284821436,-15.875));
#24962=CARTESIAN_POINT('Ctrl Pts',(1.29063426612674E-14,34.7250000000001,
-15.875));
#24963=CARTESIAN_POINT('Origin',(0.,-18.001,-7.93750000000004));
#24964=CARTESIAN_POINT('',(-5.69020212634203E-15,37.5825000069372,-15.875));
#24965=CARTESIAN_POINT('',(7.63247416915985E-15,37.2650000000001,-15.875));
#24966=CARTESIAN_POINT('',(-9.72063396823211E-16,-18.001,-15.875));
#24967=CARTESIAN_POINT('Ctrl Pts',(-6.14559781626452E-14,37.5825000069372,
-15.875));
#24968=CARTESIAN_POINT('Ctrl Pts',(0.0648007681039002,37.5791448118879,
-15.875));
#24969=CARTESIAN_POINT('Ctrl Pts',(0.12963596222447,37.5757878343597,-15.8742064650826));
#24970=CARTESIAN_POINT('Ctrl Pts',(1.21770299726839,37.5194508921281,-15.8475377204892));
#24971=CARTESIAN_POINT('Ctrl Pts',(2.22646116209439,37.4691901787736,-15.624785921622));
#24972=CARTESIAN_POINT('Ctrl Pts',(4.12233564784132,37.364686501604,-14.8004311361088));
#24973=CARTESIAN_POINT('Ctrl Pts',(4.98813466023159,37.3101291116282,-14.1994439118828));
#24974=CARTESIAN_POINT('Ctrl Pts',(6.42806682210644,37.204382590406,-12.7067007433853));
#24975=CARTESIAN_POINT('Ctrl Pts',(6.99215060066927,37.1544526769673,-11.8330247778842));
#24976=CARTESIAN_POINT('Ctrl Pts',(7.75433965280672,37.0480776373944,-9.92046591662647));
#24977=CARTESIAN_POINT('Ctrl Pts',(7.94574814392369,36.9950319317637,-8.90007367658115));
#24978=CARTESIAN_POINT('Ctrl Pts',(7.92850355379243,36.8922703274921,-6.81884745579795));
#24979=CARTESIAN_POINT('Ctrl Pts',(7.71036723229586,36.8375358499281,-5.77820487914458));
#24980=CARTESIAN_POINT('Ctrl Pts',(6.89216633471838,36.7304415224441,-3.86923844409522));
#24981=CARTESIAN_POINT('Ctrl Pts',(6.31035446161657,36.6810175743866,-3.01488271303926));
#24982=CARTESIAN_POINT('Ctrl Pts',(4.84503125674973,36.5755206401467,-1.56528829467365));
#24983=CARTESIAN_POINT('Ctrl Pts',(3.97191179476745,36.5213606287323,-0.987433946974345));
#24984=CARTESIAN_POINT('Ctrl Pts',(2.05118100985973,36.4169255320887,-0.199544354491347));
#24985=CARTESIAN_POINT('Ctrl Pts',(1.02182551332679,36.3654071560936,0.00222508803780422));
#24986=CARTESIAN_POINT('Ctrl Pts',(-1.04129465620275,36.2585848022639,-0.00223011638187775));
#24987=CARTESIAN_POINT('Ctrl Pts',(-2.05539139111777,36.2078039963006,-0.202636926533077));
#24988=CARTESIAN_POINT('Ctrl Pts',(-3.97169591767539,36.1036931728616,-0.985963708951519));
#24989=CARTESIAN_POINT('Ctrl Pts',(-4.85226215942494,36.0490537047291,-1.56932252571176));
#24990=CARTESIAN_POINT('Ctrl Pts',(-6.32370333397671,35.9429265413702,-3.03120447219226));
#24991=CARTESIAN_POINT('Ctrl Pts',(-6.90535534830421,35.893293126359,-3.89064945096875));
#24992=CARTESIAN_POINT('Ctrl Pts',(-7.70949343749074,35.7871033330414,-5.78581635903722));
#24993=CARTESIAN_POINT('Ctrl Pts',(-7.92346919040345,35.733542764425,-6.80397165270648));
#24994=CARTESIAN_POINT('Ctrl Pts',(-7.95045596877978,35.6306243345731,-8.88521717713868));
#24995=CARTESIAN_POINT('Ctrl Pts',(-7.75532755669859,35.5765526174918,-9.92829577969207));
#24996=CARTESIAN_POINT('Ctrl Pts',(-6.98027194086661,35.4693980056103,-11.8525051908394));
#24997=CARTESIAN_POINT('Ctrl Pts',(-6.41784131115587,35.4198145663908,-12.719006969005));
#24998=CARTESIAN_POINT('Ctrl Pts',(-4.9839729914452,35.3146184605473,-14.2020106446483));
#24999=CARTESIAN_POINT('Ctrl Pts',(-4.12177453714119,35.2603004795952,-14.8000870636612));
#25000=CARTESIAN_POINT('Ctrl Pts',(-2.21932381032028,35.1553986501384,-15.6284729951544));
#25001=CARTESIAN_POINT('Ctrl Pts',(-1.1979951139365,35.1045287049437,-15.8521240368318));
#25002=CARTESIAN_POINT('Ctrl Pts',(-0.108359865597093,35.0481105651948,
-15.8744455157375));
#25003=CARTESIAN_POINT('Ctrl Pts',(-0.0541678346537001,35.0453046596593,
-15.875));
#25004=CARTESIAN_POINT('Ctrl Pts',(-4.55229467871315E-15,35.0425000069372,
-15.875));
#25005=CARTESIAN_POINT('Ctrl Pts',(1.11022302462516E-15,34.7250000000001,
-15.875));
#25006=CARTESIAN_POINT('Ctrl Pts',(-0.363509860640991,34.7438214819125,
-15.875));
#25007=CARTESIAN_POINT('Ctrl Pts',(-0.727368191051986,34.7626610065743,
-15.850029402379));
#25008=CARTESIAN_POINT('Ctrl Pts',(-2.10401211480627,34.8339396196637,-15.6593567340553));
#25009=CARTESIAN_POINT('Ctrl Pts',(-3.08223203909142,34.8833245093867,-15.3235523334587));
#25010=CARTESIAN_POINT('Ctrl Pts',(-4.87999195226312,34.9902273372992,-14.2853226623512));
#25011=CARTESIAN_POINT('Ctrl Pts',(-5.67697430303928,35.0449600603399,-13.5838563013009));
#25012=CARTESIAN_POINT('Ctrl Pts',(-6.93653105482265,35.1480413436088,-11.9304225865429));
#25013=CARTESIAN_POINT('Ctrl Pts',(-7.39453834961942,35.2004969651798,-11.0001859168604));
#25014=CARTESIAN_POINT('Ctrl Pts',(-7.93179481923721,35.3069802201514,-9.01234444706242));
#25015=CARTESIAN_POINT('Ctrl Pts',(-8.00421237791695,35.3571734658315,-7.97322362338979));
#25016=CARTESIAN_POINT('Ctrl Pts',(-7.74599857552462,35.462649286388,-5.91517415017933));
#25017=CARTESIAN_POINT('Ctrl Pts',(-7.41379961298889,35.5171375939901,-4.91659186403143));
#25018=CARTESIAN_POINT('Ctrl Pts',(-6.39191085395918,35.6218872236836,-3.12142253291469));
#25019=CARTESIAN_POINT('Ctrl Pts',(-5.71843033335381,35.6718672305716,-2.33833386040319));
#25020=CARTESIAN_POINT('Ctrl Pts',(-4.09409882353876,35.7788897281313,-1.05746834187355));
#25021=CARTESIAN_POINT('Ctrl Pts',(-3.15353713284373,35.8317190314962,-0.578733174653649));
#25022=CARTESIAN_POINT('Ctrl Pts',(-1.15239837642726,35.935332168267,-0.0163885496313035));
#25023=CARTESIAN_POINT('Ctrl Pts',(-0.112382454211418,35.9891811638186,
0.0662013203635666));
#25024=CARTESIAN_POINT('Ctrl Pts',(1.93329509262871,36.0951003894446,-0.170977548322487));
#25025=CARTESIAN_POINT('Ctrl Pts',(2.91988456334042,36.1445200830762,-0.485602244766304));
#25026=CARTESIAN_POINT('Ctrl Pts',(4.73884062868974,36.2510985537357,-1.48400012152621));
#25027=CARTESIAN_POINT('Ctrl Pts',(5.54932921408693,36.3058068135178,-2.16607292692184));
#25028=CARTESIAN_POINT('Ctrl Pts',(6.84347895779032,36.4093634168762,-3.78751163298749));
#25029=CARTESIAN_POINT('Ctrl Pts',(7.32189173198879,36.4609980264526,-4.70551888221592));
#25030=CARTESIAN_POINT('Ctrl Pts',(7.9055134476158,36.5676398241248,-6.68151497324313));
#25031=CARTESIAN_POINT('Ctrl Pts',(8.0017547186586,36.6183450548568,-7.72169504645281));
#25032=CARTESIAN_POINT('Ctrl Pts',(7.78911407750309,36.7233759385058,-9.78551658956596));
#25033=CARTESIAN_POINT('Ctrl Pts',(7.48024700718692,36.777734724559,-10.7890496106528));
#25034=CARTESIAN_POINT('Ctrl Pts',(6.50101684593399,36.8828384077115,-12.6052694942955));
#25035=CARTESIAN_POINT('Ctrl Pts',(5.84568059562513,36.9324900533354,-13.4036939864018));
#25036=CARTESIAN_POINT('Ctrl Pts',(4.24777912829267,37.0396180231976,-14.724402966992));
#25037=CARTESIAN_POINT('Ctrl Pts',(3.31411010317857,37.093405030739,-15.2259808346506));
#25038=CARTESIAN_POINT('Ctrl Pts',(1.55990245202554,37.1842327940314,-15.7596126746479));
#25039=CARTESIAN_POINT('Ctrl Pts',(0.781373958260331,37.2245427320836,-15.875));
#25040=CARTESIAN_POINT('Ctrl Pts',(6.1478599988618E-14,37.2650000000001,
-15.875));
#25041=CARTESIAN_POINT('Origin',(0.,-18.001,-7.93750000000004));
#25042=CARTESIAN_POINT('',(1.80380328987778E-15,40.1225000069372,-15.875));
#25043=CARTESIAN_POINT('',(1.84571486592551E-14,39.805,-15.875));
#25044=CARTESIAN_POINT('',(-9.72063396823211E-16,-18.001,-15.875));
#25045=CARTESIAN_POINT('Ctrl Pts',(5.9986737799278E-14,40.1225000069372,
-15.875));
#25046=CARTESIAN_POINT('Ctrl Pts',(0.185867297990525,40.1128763395597,-15.875));
#25047=CARTESIAN_POINT('Ctrl Pts',(0.371944385759047,40.103241809879,-15.8684716342223));
#25048=CARTESIAN_POINT('Ctrl Pts',(1.57889074635526,40.0407496423896,-15.7834306632627));
#25049=CARTESIAN_POINT('Ctrl Pts',(2.57638491518406,39.9911817245374,-15.5146893568303));
#25050=CARTESIAN_POINT('Ctrl Pts',(4.42832218354737,39.8859628737238,-14.6063608649745));
#25051=CARTESIAN_POINT('Ctrl Pts',(5.26242841254009,39.8316554417827,-13.9699654363925));
#25052=CARTESIAN_POINT('Ctrl Pts',(6.63580409260786,39.7267863109672,-12.4144445942834));
#25053=CARTESIAN_POINT('Ctrl Pts',(7.16280366634182,39.6758735707267,-11.5111784728837));
#25054=CARTESIAN_POINT('Ctrl Pts',(7.83653466399014,39.5691794174613,-9.56339745218134));
#25055=CARTESIAN_POINT('Ctrl Pts',(7.98079626566829,39.5178024314015,-8.53879810000055));
#25056=CARTESIAN_POINT('Ctrl Pts',(7.87048579900228,39.414086729212,-6.46843549020098));
#25057=CARTESIAN_POINT('Ctrl Pts',(7.60791398256985,39.3593933345895,-5.4430651721184));
#25058=CARTESIAN_POINT('Ctrl Pts',(6.70901558264553,39.2529355379743,-3.57324528354891));
#25059=CARTESIAN_POINT('Ctrl Pts',(6.08901666201518,39.2034756052062,-2.7431306233325));
#25060=CARTESIAN_POINT('Ctrl Pts',(4.5627511221141,39.0974762991203,-1.36090910126765));
#25061=CARTESIAN_POINT('Ctrl Pts',(3.66934538919467,39.0437031321698,-0.823687420761977));
#25062=CARTESIAN_POINT('Ctrl Pts',(1.71380952697431,38.9402775522919,-0.116873805681974));
#25063=CARTESIAN_POINT('Ctrl Pts',(0.668706479971726,38.8871236809561,0.0407489814137206));
#25064=CARTESIAN_POINT('Ctrl Pts',(-1.39902799814106,38.7800624116666,-0.057539562425789));
#25065=CARTESIAN_POINT('Ctrl Pts',(-2.40219030683038,38.7302126473264,-0.303329135149752));
#25066=CARTESIAN_POINT('Ctrl Pts',(-4.27637136753711,38.6253347448599,-1.16983872628206));
#25067=CARTESIAN_POINT('Ctrl Pts',(-5.12650815803909,38.5708888676778,-1.78871904048554));
#25068=CARTESIAN_POINT('Ctrl Pts',(-6.53338217014492,38.4655659817784,-3.3130429568106));
#25069=CARTESIAN_POINT('Ctrl Pts',(-7.07904785220948,38.4152071427341,-4.20149410445223));
#25070=CARTESIAN_POINT('Ctrl Pts',(-7.79724476709036,38.3086668457171,-6.13170283999069));
#25071=CARTESIAN_POINT('Ctrl Pts',(-7.965183003106,38.2565131010932,-7.15423708406995));
#25072=CARTESIAN_POINT('Ctrl Pts',(-7.90165369156493,38.1532618300973,-9.23036838493943));
#25073=CARTESIAN_POINT('Ctrl Pts',(-7.66135886518496,38.0985346504455,-10.2636630247046));
#25074=CARTESIAN_POINT('Ctrl Pts',(-6.80297851111757,37.9917420113679,-12.1534478313711));
#25075=CARTESIAN_POINT('Ctrl Pts',(-6.20224707983457,37.9423583482901,-12.995846776573));
#25076=CARTESIAN_POINT('Ctrl Pts',(-4.70655188507403,37.8365973253077,-14.412315216426));
#25077=CARTESIAN_POINT('Ctrl Pts',(-3.82317267607415,37.7826164241643,-14.9701629936973));
#25078=CARTESIAN_POINT('Ctrl Pts',(-1.94551186050395,37.6819123589154,-15.6947383580089));
#25079=CARTESIAN_POINT('Ctrl Pts',(-0.976631580980323,37.6330671458976,
-15.875));
#25080=CARTESIAN_POINT('Ctrl Pts',(-5.87030424270552E-14,37.5825000069372,
-15.875));
#25081=CARTESIAN_POINT('Ctrl Pts',(5.28743715477731E-14,37.2650000000001,
-15.875));
#25082=CARTESIAN_POINT('Ctrl Pts',(-0.246325470798439,37.2777540154896,
-15.875));
#25083=CARTESIAN_POINT('Ctrl Pts',(-0.492933725020677,37.2905226726808,
-15.8635338979502));
#25084=CARTESIAN_POINT('Ctrl Pts',(-1.76216030317954,37.3562395284532,-15.7448462700579));
#25085=CARTESIAN_POINT('Ctrl Pts',(-2.75701869450834,37.4058108170844,-15.4514028738958));
#25086=CARTESIAN_POINT('Ctrl Pts',(-4.59650542976917,37.5120390370243,-14.4927716462837));
#25087=CARTESIAN_POINT('Ctrl Pts',(-5.41994727147877,37.566696878774,-13.8301841142049));
#25088=CARTESIAN_POINT('Ctrl Pts',(-6.74791495111436,37.6706927887025,-12.2408569830228));
#25089=CARTESIAN_POINT('Ctrl Pts',(-7.24640490395248,37.7216400948249,-11.3349899794204));
#25090=CARTESIAN_POINT('Ctrl Pts',(-7.87570224164693,37.82842545482,-9.37091940849076));
#25091=CARTESIAN_POINT('Ctrl Pts',(-7.99546242012346,37.8797535284719,-8.32982170422263));
#25092=CARTESIAN_POINT('Ctrl Pts',(-7.82750474973192,37.9843199465854,-6.26091390886392));
#25093=CARTESIAN_POINT('Ctrl Pts',(-7.54151344243943,38.0385259457425,-5.25305081879688));
#25094=CARTESIAN_POINT('Ctrl Pts',(-6.60423189572394,38.1439432223175,-3.41683271158838));
#25095=CARTESIAN_POINT('Ctrl Pts',(-5.96665031585442,38.1933991011947,-2.60351775144321));
#25096=CARTESIAN_POINT('Ctrl Pts',(-4.39537345261552,38.3005734616406,-1.24463883631588));
#25097=CARTESIAN_POINT('Ctrl Pts',(-3.46923623280529,38.3553053237183,-0.720967191637942));
#25098=CARTESIAN_POINT('Ctrl Pts',(-1.48988927923936,38.4579230202483,-0.0734723203727779));
#25099=CARTESIAN_POINT('Ctrl Pts',(-0.458829348094782,38.5112431526314,
0.0532894238835631));
#25100=CARTESIAN_POINT('Ctrl Pts',(1.59470343952526,38.6175690997477,-0.0939780982895629));
#25101=CARTESIAN_POINT('Ctrl Pts',(2.59754266809464,38.667399587462,-0.366719226636373));
#25102=CARTESIAN_POINT('Ctrl Pts',(4.45645307465599,38.7732612712922,-1.28657234944641));
#25103=CARTESIAN_POINT('Ctrl Pts',(5.29201868124709,38.8278454869227,-1.93005372939396));
#25104=CARTESIAN_POINT('Ctrl Pts',(6.65228551138309,38.9322365117142,-3.48790765481004));
#25105=CARTESIAN_POINT('Ctrl Pts',(7.17008966563123,38.9826379953507,-4.38199638047202));
#25106=CARTESIAN_POINT('Ctrl Pts',(7.84337351461919,39.0895494003904,-6.33433452486375));
#25107=CARTESIAN_POINT('Ctrl Pts',(7.98582844272044,39.1415861421795,-7.37618898469444));
#25108=CARTESIAN_POINT('Ctrl Pts',(7.86068429551567,39.2456813681751,-9.44943901200891));
#25109=CARTESIAN_POINT('Ctrl Pts',(7.59659859145796,39.2997173356786,-10.4609667494475));
#25110=CARTESIAN_POINT('Ctrl Pts',(6.69962519227849,39.4054039973125,-12.3157522996759));
#25111=CARTESIAN_POINT('Ctrl Pts',(6.07903425107462,39.4547876391827,-13.1432083713512));
#25112=CARTESIAN_POINT('Ctrl Pts',(4.53797774525617,39.561671536427,-14.5341379436891));
#25113=CARTESIAN_POINT('Ctrl Pts',(3.62542075252794,39.6164035277038,-15.0765054126516));
#25114=CARTESIAN_POINT('Ctrl Pts',(1.78672925347056,39.7131060004465,-15.7232323347485));
#25115=CARTESIAN_POINT('Ctrl Pts',(0.896114797452721,39.7586017855968,-15.875));
#25116=CARTESIAN_POINT('Ctrl Pts',(7.2025718722557E-14,39.805,-15.875));
#25117=CARTESIAN_POINT('Origin',(0.,-18.001,-7.93750000000004));
#25118=CARTESIAN_POINT('',(-2.65762727771028E-14,42.6625000069372,-15.875));
#25119=CARTESIAN_POINT('',(-6.2616496713002E-9,42.3450000006485,-15.875));
#25120=CARTESIAN_POINT('',(-9.72063396823211E-16,-18.001,-15.875));
#25121=CARTESIAN_POINT('Ctrl Pts',(-1.21430643318376E-14,42.6625000069372,
-15.875));
#25122=CARTESIAN_POINT('Ctrl Pts',(0.300454544332103,42.6469433456635,-15.875));
#25123=CARTESIAN_POINT('Ctrl Pts',(0.60125822561139,42.6313686070956,-15.8579410296588));
#25124=CARTESIAN_POINT('Ctrl Pts',(1.91951584091607,42.5631130670159,-15.7073371473094));
#25125=CARTESIAN_POINT('Ctrl Pts',(2.90591665428349,42.5137278838793,-15.3947491935123));
#25126=CARTESIAN_POINT('Ctrl Pts',(4.7136267695739,42.4079488643821,-14.4071411162044));
#25127=CARTESIAN_POINT('Ctrl Pts',(5.51598669608921,42.3539819098442,-13.7382381235893));
#25128=CARTESIAN_POINT('Ctrl Pts',(6.82385615017907,42.2500682907801,-12.1239520873497));
#25129=CARTESIAN_POINT('Ctrl Pts',(7.31428406470129,42.1977404128448,-11.1921586784889));
#25130=CARTESIAN_POINT('Ctrl Pts',(7.9012607442347,42.0907851526947,-9.21088704799251));
#25131=CARTESIAN_POINT('Ctrl Pts',(7.99946203179922,42.0405577307008,-8.18253679286367));
#25132=CARTESIAN_POINT('Ctrl Pts',(7.79800018427309,41.9360265225012,-6.12523018922354));
#25133=CARTESIAN_POINT('Ctrl Pts',(7.4924218338955,41.8814761264338,-5.11673748152932));
#25134=CARTESIAN_POINT('Ctrl Pts',(6.514850757226,41.7757585515474,-3.28751193389603));
#25135=CARTESIAN_POINT('Ctrl Pts',(5.85685564858871,41.7258024157269,-2.4819637473802));
#25136=CARTESIAN_POINT('Ctrl Pts',(4.27128902936751,41.6194153347666,-1.16862157650717));
#25137=CARTESIAN_POINT('Ctrl Pts',(3.35932997630399,41.5664363295322,-0.672786206102429));
#25138=CARTESIAN_POINT('Ctrl Pts',(1.37395363649707,41.4636393247877,-0.0492519434039022));
#25139=CARTESIAN_POINT('Ctrl Pts',(0.31682951160224,41.4089045163267,0.0632246299822857));
#25140=CARTESIAN_POINT('Ctrl Pts',(-1.75115225875815,41.3018304429648,-0.128128031572477));
#25141=CARTESIAN_POINT('Ctrl Pts',(-2.74309856090656,41.2524130366757,-0.418972246627263));
#25142=CARTESIAN_POINT('Ctrl Pts',(-4.57302366092601,41.146896637977,-1.36737477531151));
#25143=CARTESIAN_POINT('Ctrl Pts',(-5.39130545400732,41.0927483743506,-2.02032068794153));
#25144=CARTESIAN_POINT('Ctrl Pts',(-6.73190329291471,40.9883463181676,-3.60560912888532));
#25145=CARTESIAN_POINT('Ctrl Pts',(-7.24061972766324,40.9367791529986,-4.52322227145597));
#25146=CARTESIAN_POINT('Ctrl Pts',(-7.87091814714441,40.829947725114,-6.48790309398654));
#25147=CARTESIAN_POINT('Ctrl Pts',(-7.99209826798352,40.7792070067401,-7.5144255662737));
#25148=CARTESIAN_POINT('Ctrl Pts',(-7.83612457682176,40.6750678728088,-9.57855012710422));
#25149=CARTESIAN_POINT('Ctrl Pts',(-7.55193763598935,40.6204332959951,-10.5957028239988));
#25150=CARTESIAN_POINT('Ctrl Pts',(-6.61358117058684,40.5143316941337,-12.4454685917169));
#25151=CARTESIAN_POINT('Ctrl Pts',(-5.9746255177841,40.4646813857368,-13.2633856477434));
#25152=CARTESIAN_POINT('Ctrl Pts',(-4.41865875031456,40.3584784649879,-14.6114173473667));
#25153=CARTESIAN_POINT('Ctrl Pts',(-3.51581695525116,40.3049346026081,-15.1281168683531));
#25154=CARTESIAN_POINT('Ctrl Pts',(-1.72020503836694,40.2112659530537,-15.7344517960849));
#25155=CARTESIAN_POINT('Ctrl Pts',(-0.862352704592977,40.1671501184995,
-15.875));
#25156=CARTESIAN_POINT('Ctrl Pts',(5.37070388162419E-14,40.1225000069372,
-15.875));
#25157=CARTESIAN_POINT('Ctrl Pts',(9.09688990802238E-14,39.805,-15.875));
#25158=CARTESIAN_POINT('Ctrl Pts',(-0.128923461931392,39.8116752813873,
-15.875));
#25159=CARTESIAN_POINT('Ctrl Pts',(-0.257961433384957,39.818356491744,-15.8718590127514));
#25160=CARTESIAN_POINT('Ctrl Pts',(-1.41780723665423,39.8784099295488,-15.8152422530517));
#25161=CARTESIAN_POINT('Ctrl Pts',(-2.42896253760847,39.9286309487171,-15.5643717670732));
#25162=CARTESIAN_POINT('Ctrl Pts',(-4.30770635463342,40.0340803549818,-14.6853636882796));
#25163=CARTESIAN_POINT('Ctrl Pts',(-5.15550411383657,40.0885615010144,-14.0621051029345));
#25164=CARTESIAN_POINT('Ctrl Pts',(-6.54908111448641,40.1933338099745,-12.5375703846111));
#25165=CARTESIAN_POINT('Ctrl Pts',(-7.08696717242735,40.2432899324377,-11.6558310944197));
#25166=CARTESIAN_POINT('Ctrl Pts',(-7.80602747190267,40.3503193264008,-9.71597056259306));
#25167=CARTESIAN_POINT('Ctrl Pts',(-7.97214689114645,40.4032043066804,-8.67347038615789));
#25168=CARTESIAN_POINT('Ctrl Pts',(-7.89131535184402,40.506784913823,-6.59627293232724));
#25169=CARTESIAN_POINT('Ctrl Pts',(-7.64987601671947,40.5606208742748,-5.58144858297681));
#25170=CARTESIAN_POINT('Ctrl Pts',(-6.79474000294826,40.6665543857725,-3.70805634326503));
#25171=CARTESIAN_POINT('Ctrl Pts',(-6.19172517110699,40.7159800649546,-2.86608687083622));
#25172=CARTESIAN_POINT('Ctrl Pts',(-4.68204147809769,40.8225376748708,-1.44269753865027));
#25173=CARTESIAN_POINT('Ctrl Pts',(-3.78378584066279,40.8772435685726,-0.881503462017499));
#25174=CARTESIAN_POINT('Ctrl Pts',(-1.84302089740972,40.980828303655,-0.149129868455843));
#25175=CARTESIAN_POINT('Ctrl Pts',(-0.822435479458738,41.0324166861016,
0.0236067096783087));
#25176=CARTESIAN_POINT('Ctrl Pts',(1.23737684193968,41.1390677691886,-0.029027715532643));
#25177=CARTESIAN_POINT('Ctrl Pts',(2.25689579584603,41.1898082845221,-0.25756096921839));
#25178=CARTESIAN_POINT('Ctrl Pts',(4.15517361440018,41.2948110684688,-1.09500759847268));
#25179=CARTESIAN_POINT('Ctrl Pts',(5.0148559220807,41.3491610847678,-1.69759981986668));
#25180=CARTESIAN_POINT('Ctrl Pts',(6.44159243080683,41.4542852588518,-3.18805604346756));
#25181=CARTESIAN_POINT('Ctrl Pts',(6.99965655552302,41.5039210909783,-4.05728027463741));
#25182=CARTESIAN_POINT('Ctrl Pts',(7.76474742221403,41.6110550038067,-5.98430708342086));
#25183=CARTESIAN_POINT('Ctrl Pts',(7.95470864438124,41.6649037667633,-7.02730052722785));
#25184=CARTESIAN_POINT('Ctrl Pts',(7.91816984828705,41.7679426179726,-9.10788786739275));
#25185=CARTESIAN_POINT('Ctrl Pts',(7.69932733321596,41.8215546040985,-10.1255060142777));
#25186=CARTESIAN_POINT('Ctrl Pts',(6.8861293697943,41.9277024299275,-12.0168769367812));
#25187=CARTESIAN_POINT('Ctrl Pts',(6.30068628876214,41.9772866121413,-12.8732340780505));
#25188=CARTESIAN_POINT('Ctrl Pts',(4.82245152923863,42.0834928057278,-14.3283622475923));
#25189=CARTESIAN_POINT('Ctrl Pts',(3.93872346358835,42.1381467768533,-14.9078457292674));
#25190=CARTESIAN_POINT('Ctrl Pts',(2.02470881339383,42.2418073226377,-15.6795289453528));
#25191=CARTESIAN_POINT('Ctrl Pts',(1.01703327273241,42.292340979105,-15.8750000016047));
#25192=CARTESIAN_POINT('Ctrl Pts',(-1.25233615144715E-8,42.3450000006485,
-15.875));
#25193=CARTESIAN_POINT('Origin',(0.,-18.001,-7.93750000000004));
#25194=CARTESIAN_POINT('',(-2.92477469301071E-14,45.2025000069372,-15.875));
#25195=CARTESIAN_POINT('',(8.46514143762872E-15,44.885,-15.875));
#25196=CARTESIAN_POINT('',(-9.72063396823211E-16,-18.001,-15.875));
#25197=CARTESIAN_POINT('Ctrl Pts',(-1.83186799063151E-14,45.2025000069372,
-15.875));
#25198=CARTESIAN_POINT('Ctrl Pts',(0.414093089374723,45.1810594727575,-15.875));
#25199=CARTESIAN_POINT('Ctrl Pts',(0.828501962723747,45.1596025882034,-15.842596332934));
#25200=CARTESIAN_POINT('Ctrl Pts',(2.25518995910534,45.0857328387799,-15.6170597446468));
#25201=CARTESIAN_POINT('Ctrl Pts',(3.2301180397819,45.0360649594813,-15.2606023136635));
#25202=CARTESIAN_POINT('Ctrl Pts',(4.99133973839858,44.9298489672139,-14.19465028386));
#25203=CARTESIAN_POINT('Ctrl Pts',(5.76057075917527,44.8763220528392,-13.4946081896136));
#25204=CARTESIAN_POINT('Ctrl Pts',(7.0009989017113,44.7734817570966,-11.8227646179266));
#25205=CARTESIAN_POINT('Ctrl Pts',(7.45357972913763,44.7192638026932,-10.8622051736005));
#25206=CARTESIAN_POINT('Ctrl Pts',(7.95130601089794,44.6120962317578,-8.84762283372994));
#25207=CARTESIAN_POINT('Ctrl Pts',(8.00230032536853,44.5625433313465,-7.81578750250976));
#25208=CARTESIAN_POINT('Ctrl Pts',(7.70742658653592,44.4573017101486,-5.77440556374169));
#25209=CARTESIAN_POINT('Ctrl Pts',(7.35841791020113,44.4030050483682,-4.78517692857907));
#25210=CARTESIAN_POINT('Ctrl Pts',(6.30061393659308,44.298169040757,-2.99992304014986));
#25211=CARTESIAN_POINT('Ctrl Pts',(5.60300453270788,44.2472125238532,-2.22052955071996));
#25212=CARTESIAN_POINT('Ctrl Pts',(3.9565996009202,44.1405079699132,-0.980492544419229));
#25213=CARTESIAN_POINT('Ctrl Pts',(3.02607306041202,44.0891812569913,-0.52822382645339));
#25214=CARTESIAN_POINT('Ctrl Pts',(1.02234021118214,43.9854338056496,0.00335437628450272));
#25215=CARTESIAN_POINT('Ctrl Pts',(-0.03391822241176,43.930743820163,0.0688139935690083));
#25216=CARTESIAN_POINT('Ctrl Pts',(-2.08951685814976,43.8243109094478,-0.21145543413736));
#25217=CARTESIAN_POINT('Ctrl Pts',(-3.07018109632898,43.7748410382994,-0.546165898899786));
#25218=CARTESIAN_POINT('Ctrl Pts',(-4.85472481487504,43.6688259661318,-1.5734160504032));
#25219=CARTESIAN_POINT('Ctrl Pts',(-5.6405408372536,43.6150685612002,-2.25820435184308));
#25220=CARTESIAN_POINT('Ctrl Pts',(-6.91463230239517,43.5116814811785,-3.9016806791066));
#25221=CARTESIAN_POINT('Ctrl Pts',(-7.3861361833161,43.4584599442885,-4.84795809196937));
#25222=CARTESIAN_POINT('Ctrl Pts',(-7.92841842210969,43.3513910090069,-6.84606028214751));
#25223=CARTESIAN_POINT('Ctrl Pts',(-8.00295760332611,43.3015657794211,-7.8762028670668));
#25224=CARTESIAN_POINT('Ctrl Pts',(-7.75465683012312,43.1966622791342,-9.9258508957005));
#25225=CARTESIAN_POINT('Ctrl Pts',(-7.42721296297431,43.1422254493468,-10.9249328212549));
#25226=CARTESIAN_POINT('Ctrl Pts',(-6.40936083873474,43.036934144788,-12.7324137865624));
#25227=CARTESIAN_POINT('Ctrl Pts',(-5.73159127342935,42.9865397015636,-13.5249806950076));
#25228=CARTESIAN_POINT('Ctrl Pts',(-4.11560421824636,42.8799879692098,-14.8018628753267));
#25229=CARTESIAN_POINT('Ctrl Pts',(-3.1943453937713,42.8278939083433,-15.2759982468382));
#25230=CARTESIAN_POINT('Ctrl Pts',(-1.48929540753733,42.7396113857753,-15.7699023313494));
#25231=CARTESIAN_POINT('Ctrl Pts',(-0.745723087441236,42.7011113765908,
-15.875));
#25232=CARTESIAN_POINT('Ctrl Pts',(-5.41233724504764E-15,42.6625000069372,
-15.875));
#25233=CARTESIAN_POINT('Ctrl Pts',(-1.2523352834363E-8,42.3450000006485,
-15.875));
#25234=CARTESIAN_POINT('Ctrl Pts',(-0.00718283073825684,42.3453719060567,
-15.8749999999887));
#25235=CARTESIAN_POINT('Ctrl Pts',(-0.0143661199379798,42.3457438358511,
-15.8749902501427));
#25236=CARTESIAN_POINT('Ctrl Pts',(-1.05976660879513,42.3998716285815,-15.8721520368392));
#25237=CARTESIAN_POINT('Ctrl Pts',(-2.08740291424895,42.4512408187044,-15.6656635511861));
#25238=CARTESIAN_POINT('Ctrl Pts',(-4.00424958390844,42.5557785175246,-14.8690566104206));
#25239=CARTESIAN_POINT('Ctrl Pts',(-4.87506285028589,42.6099745573722,-14.2868442275217));
#25240=CARTESIAN_POINT('Ctrl Pts',(-6.3336727297779,42.7154095731031,-12.8300442398946));
#25241=CARTESIAN_POINT('Ctrl Pts',(-6.91133069430021,42.7648576448598,-11.9730766733429));
#25242=CARTESIAN_POINT('Ctrl Pts',(-7.72065890152763,42.8720145680178,-10.0599561659786));
#25243=CARTESIAN_POINT('Ctrl Pts',(-7.93389431393028,42.9267471830165,-9.01775901144047));
#25244=CARTESIAN_POINT('Ctrl Pts',(-7.94093188920756,43.0293967969897,-6.93549057135042));
#25245=CARTESIAN_POINT('Ctrl Pts',(-7.74434012355705,43.0826556176578,-5.91558444175416));
#25246=CARTESIAN_POINT('Ctrl Pts',(-6.97244712715683,43.1889924725656,-4.00695401748261));
#25247=CARTESIAN_POINT('Ctrl Pts',(-6.40430688532385,43.2388440334976,-3.13655229747144));
#25248=CARTESIAN_POINT('Ctrl Pts',(-4.95709627578438,43.344680517238,-1.65087104682534));
#25249=CARTESIAN_POINT('Ctrl Pts',(-4.08787156469548,43.3992590024194,-1.05390574198236));
#25250=CARTESIAN_POINT('Ctrl Pts',(-2.18725613219509,43.5036751134421,-0.238953575351402));
#25251=CARTESIAN_POINT('Ctrl Pts',(-1.17726529609476,43.5540446315884,-0.0213287807175966));
#25252=CARTESIAN_POINT('Ctrl Pts',(0.887727052590154,43.6609639214022,0.0186985187400757));
#25253=CARTESIAN_POINT('Ctrl Pts',(1.9231168137452,43.7130511158005,-0.1663580163584));
#25254=CARTESIAN_POINT('Ctrl Pts',(3.85734793065473,43.8171144439488,-0.923450354424346));
#25255=CARTESIAN_POINT('Ctrl Pts',(4.73841970608408,43.8711384211649,-1.48588944352097));
#25256=CARTESIAN_POINT('Ctrl Pts',(6.22720874915739,43.9768417410447,-2.90996736593318));
#25257=CARTESIAN_POINT('Ctrl Pts',(6.82361929704801,44.0262245421741,-3.75510591832266));
#25258=CARTESIAN_POINT('Ctrl Pts',(7.67285742027115,44.1330884659885,-5.64930882929789));
#25259=CARTESIAN_POINT('Ctrl Pts',(7.90811583243183,44.1878195838756,-6.68431987487908));
#25260=CARTESIAN_POINT('Ctrl Pts',(7.96110460463708,44.2909619682184,-8.76166479094792));
#25261=CARTESIAN_POINT('Ctrl Pts',(7.78782588199072,44.3433080827685,-9.7837200503708));
#25262=CARTESIAN_POINT('Ctrl Pts',(7.05961136102939,44.4498118828499,-11.7099327075577));
#25263=CARTESIAN_POINT('Ctrl Pts',(6.50974743990282,44.5000625170366,-12.5950293995893));
#25264=CARTESIAN_POINT('Ctrl Pts',(5.09533745588943,44.6054841178605,-14.1122245346181));
#25265=CARTESIAN_POINT('Ctrl Pts',(4.24161592094833,44.6599576487681,-14.7270795228757));
#25266=CARTESIAN_POINT('Ctrl Pts',(2.36246672704688,44.7647535910512,-15.5840580016538));
#25267=CARTESIAN_POINT('Ctrl Pts',(1.35802910142151,44.814685208198,-15.8246308207638));
#25268=CARTESIAN_POINT('Ctrl Pts',(0.22371140399614,44.8734168750292,-15.8726375525265));
#25269=CARTESIAN_POINT('Ctrl Pts',(0.111809721412583,44.8792108182554,-15.875));
#25270=CARTESIAN_POINT('Ctrl Pts',(-1.18655085756814E-14,44.885,-15.875));
#25271=CARTESIAN_POINT('Origin',(0.,-18.001,-7.93750000000004));
#25272=CARTESIAN_POINT('',(6.78245966593122E-15,47.7425000069373,-15.875));
#25273=CARTESIAN_POINT('',(1.23509220238168E-14,47.425,-15.875));
#25274=CARTESIAN_POINT('',(-9.72063396823211E-16,-18.001,-15.875));
#25275=CARTESIAN_POINT('Ctrl Pts',(1.346145417358E-14,47.7425000069373,
-15.875));
#25276=CARTESIAN_POINT('Ctrl Pts',(0.536131078723344,47.7147407010877,-15.875));
#25277=CARTESIAN_POINT('Ctrl Pts',(1.07217525151894,47.686985894974,-15.8206810031299));
#25278=CARTESIAN_POINT('Ctrl Pts',(2.60215309102455,47.6077680982907,-15.5058499602607));
#25279=CARTESIAN_POINT('Ctrl Pts',(3.55518708976509,47.5577948449748,-15.1076985008461));
#25280=CARTESIAN_POINT('Ctrl Pts',(5.27582292987373,47.4507704060872,-13.9593207328677));
#25281=CARTESIAN_POINT('Ctrl Pts',(6.022115217456,47.3979255158128,-13.2129642659173));
#25282=CARTESIAN_POINT('Ctrl Pts',(7.17598098299624,47.2943215013235,-11.4839414226786));
#25283=CARTESIAN_POINT('Ctrl Pts',(7.5762594799151,47.2404761561679,-10.5205364658375));
#25284=CARTESIAN_POINT('Ctrl Pts',(7.98361143601375,47.1345529072572,-8.50185877341769));
#25285=CARTESIAN_POINT('Ctrl Pts',(7.98965182749404,47.0851315780006,-7.46630839809705));
#25286=CARTESIAN_POINT('Ctrl Pts',(7.60565637182131,46.9792981093663,-5.44186492991381));
#25287=CARTESIAN_POINT('Ctrl Pts',(7.21598333391762,46.9253452773936,-4.47283126405295));
#25288=CARTESIAN_POINT('Ctrl Pts',(6.08212765812418,46.821468256998,-2.73176268627033));
#25289=CARTESIAN_POINT('Ctrl Pts',(5.34609413436768,46.7690805884849,-1.97835371905176));
#25290=CARTESIAN_POINT('Ctrl Pts',(3.64105459911015,46.6621167900168,-0.810502013748309));
#25291=CARTESIAN_POINT('Ctrl Pts',(2.69273834198521,46.6119221560619,-0.400886571937467));
#25292=CARTESIAN_POINT('Ctrl Pts',(0.67333747039778,46.5073634601534,0.0399305255073528));
#25293=CARTESIAN_POINT('Ctrl Pts',(-0.380086693244262,46.4528202249105,
0.0592665995938344));
#25294=CARTESIAN_POINT('Ctrl Pts',(-2.42130517369179,46.347131876756,-0.308390799253155));
#25295=CARTESIAN_POINT('Ctrl Pts',(-3.39032224405438,46.2971487774006,-0.686865161060566));
#25296=CARTESIAN_POINT('Ctrl Pts',(-5.12757382038213,46.190749656441,-1.79182651200148));
#25297=CARTESIAN_POINT('Ctrl Pts',(-5.87969960599913,46.1378370944241,-2.50703017682195));
#25298=CARTESIAN_POINT('Ctrl Pts',(-7.08338280256676,46.0350046517945,-4.20419767461094));
#25299=CARTESIAN_POINT('Ctrl Pts',(-7.51545706022845,45.9802696389798,-5.17533847162807));
#25300=CARTESIAN_POINT('Ctrl Pts',(-7.96942443679653,45.8732160711656,-7.20182382545928));
#25301=CARTESIAN_POINT('Ctrl Pts',(-7.99777112386962,45.8238046792999,-8.23520088124158));
#25302=CARTESIAN_POINT('Ctrl Pts',(-7.65816151419308,45.7182688493223,-10.2680218936531));
#25303=CARTESIAN_POINT('Ctrl Pts',(-7.28861749067,45.6641325228415,-11.2473221839934));
#25304=CARTESIAN_POINT('Ctrl Pts',(-6.19253387136322,45.5597638414915,-13.0106480423953));
#25305=CARTESIAN_POINT('Ctrl Pts',(-5.47569444764857,45.5081470312241,-13.7771188700226));
#25306=CARTESIAN_POINT('Ctrl Pts',(-3.79990067038661,45.4013065309656,-14.9811725513299));
#25307=CARTESIAN_POINT('Ctrl Pts',(-2.86044627530179,45.3506055844234,-15.4121480385549));
#25308=CARTESIAN_POINT('Ctrl Pts',(-1.25297119627631,45.2673752063774,-15.8007416130287));
#25309=CARTESIAN_POINT('Ctrl Pts',(-0.62684741416668,45.2349563404374,-15.875));
#25310=CARTESIAN_POINT('Ctrl Pts',(-9.71445146547012E-15,45.2025000069372,
-15.875));
#25311=CARTESIAN_POINT('Ctrl Pts',(-3.73312492030209E-14,44.885,-15.875));
#25312=CARTESIAN_POINT('Ctrl Pts',(-0.932020445293405,44.9332573042782,
-15.875));
#25313=CARTESIAN_POINT('Ctrl Pts',(-1.85769971369281,44.980244432192,-15.7108256257695));
#25314=CARTESIAN_POINT('Ctrl Pts',(-3.70421023799222,45.0782119619776,-15.0332931782654));
#25315=CARTESIAN_POINT('Ctrl Pts',(-4.59539439428895,45.1320341721975,-14.4914022865744));
#25316=CARTESIAN_POINT('Ctrl Pts',(-6.11480378672683,45.2379825132159,-13.1014187072022));
#25317=CARTESIAN_POINT('Ctrl Pts',(-6.73046087154675,45.2874149370191,-12.2685259637988));
#25318=CARTESIAN_POINT('Ctrl Pts',(-7.62026450762139,45.3939505954988,-10.3941698289853));
#25319=CARTESIAN_POINT('Ctrl Pts',(-7.87784267286048,45.4486539057136,-9.36697561457017));
#25320=CARTESIAN_POINT('Ctrl Pts',(-7.97764310122838,45.5522679542267,-7.29526241641956));
#25321=CARTESIAN_POINT('Ctrl Pts',(-7.82806540607513,45.6038084711587,-6.27111851809931));
#25322=CARTESIAN_POINT('Ctrl Pts',(-7.1443428831817,45.7104692171442,-4.32726235844925));
#25323=CARTESIAN_POINT('Ctrl Pts',(-6.61314452286045,45.7612471334107,-3.42731431463647));
#25324=CARTESIAN_POINT('Ctrl Pts',(-5.2322356449816,45.8662204115536,-1.87873993665991));
#25325=CARTESIAN_POINT('Ctrl Pts',(-4.39451134392497,45.9205611496417,-1.24622997719547));
#25326=CARTESIAN_POINT('Ctrl Pts',(-2.53754931859762,46.0257066178352,-0.347228690382674));
#25327=CARTESIAN_POINT('Ctrl Pts',(-1.53878048653146,46.07532642789,-0.0836158856518243));
#25328=CARTESIAN_POINT('Ctrl Pts',(0.530475862045332,46.1824664951999,0.0515848033244231));
#25329=CARTESIAN_POINT('Ctrl Pts',(1.58161651110608,46.2363802475909,-0.0886182285104546));
#25330=CARTESIAN_POINT('Ctrl Pts',(3.55013587705037,46.3393838294781,-0.763695491740995));
#25331=CARTESIAN_POINT('Ctrl Pts',(4.4509168543477,46.3929808139443,-1.28497698088934));
#25332=CARTESIAN_POINT('Ctrl Pts',(6.0003125392266,46.4991411338195,-2.6406532119956));
#25333=CARTESIAN_POINT('Ctrl Pts',(6.63505294201067,46.5487392394636,-3.46129238829061));
#25334=CARTESIAN_POINT('Ctrl Pts',(7.56467089723176,46.6549223179508,-5.31555205511408));
#25335=CARTESIAN_POINT('Ctrl Pts',(7.84407828082769,46.7095721457825,-6.33456743405312));
#25336=CARTESIAN_POINT('Ctrl Pts',(7.98993006677436,46.8136199865895,-8.40012686786143));
#25337=CARTESIAN_POINT('Ctrl Pts',(7.8636353537285,46.8644913094592,-9.42623077416332));
#25338=CARTESIAN_POINT('Ctrl Pts',(7.22812604754061,46.9705556607606,-11.3736410838175));
#25339=CARTESIAN_POINT('Ctrl Pts',(6.72492600108043,47.0213593418421,-12.2766447124189));
#25340=CARTESIAN_POINT('Ctrl Pts',(5.38905941843051,47.125454127982,-13.8583488300923));
#25341=CARTESIAN_POINT('Ctrl Pts',(4.56262965766865,47.1800963018128,-14.5163090248842));
#25342=CARTESIAN_POINT('Ctrl Pts',(2.71837576444638,47.2862378264649,-15.4655301718279));
#25343=CARTESIAN_POINT('Ctrl Pts',(1.72157316290845,47.3358619554654,-15.7539546713386));
#25344=CARTESIAN_POINT('Ctrl Pts',(0.465187531251854,47.4009139444253,-15.8647882769727));
#25345=CARTESIAN_POINT('Ctrl Pts',(0.232461311524967,47.4129638303003,-15.875));
#25346=CARTESIAN_POINT('Ctrl Pts',(-9.85322934354826E-15,47.425,-15.875));
#25347=CARTESIAN_POINT('Origin',(0.,-18.001,-7.93750000000004));
#25348=CARTESIAN_POINT('',(-2.25170198433171E-14,50.2825000069373,-15.875));
#25349=CARTESIAN_POINT('',(1.77632592688644E-14,49.965,-15.875));
#25350=CARTESIAN_POINT('',(-9.72063396823211E-16,-18.001,-15.875));
#25351=CARTESIAN_POINT('Ctrl Pts',(-5.81479309147426E-14,50.2825000069373,
-15.875));
#25352=CARTESIAN_POINT('Ctrl Pts',(0.653807280817845,50.2486477700587,-15.875));
#25353=CARTESIAN_POINT('Ctrl Pts',(1.30663150140665,50.2148464331757,-15.7942160326749));
#25354=CARTESIAN_POINT('Ctrl Pts',(2.9366542847825,50.1304486006657,-15.38259096553));
#25355=CARTESIAN_POINT('Ctrl Pts',(3.87202354333085,50.0794754540483,-14.9418443569599));
#25356=CARTESIAN_POINT('Ctrl Pts',(5.53435991943361,49.9726957425407,-13.7212655606029));
#25357=CARTESIAN_POINT('Ctrl Pts',(6.24238641304659,49.9213955529466,-12.9488528088023));
#25358=CARTESIAN_POINT('Ctrl Pts',(7.32098116949546,49.816809543527,-11.1754310887501));
#25359=CARTESIAN_POINT('Ctrl Pts',(7.68115940712471,49.7625967825885,-10.1915354788068));
#25360=CARTESIAN_POINT('Ctrl Pts',(8.00031667494626,49.6571917112352,-8.15472447597427));
#25361=CARTESIAN_POINT('Ctrl Pts',(7.96161114636959,49.6077302366269,-7.12204195811604));
#25362=CARTESIAN_POINT('Ctrl Pts',(7.48729083246518,49.500544002672,-5.09947555936591));
#25363=CARTESIAN_POINT('Ctrl Pts',(7.04489407564157,49.4458127135795,-4.13176436505925));
#25364=CARTESIAN_POINT('Ctrl Pts',(5.82244293327038,49.3432169360504,-2.44550101455162));
#25365=CARTESIAN_POINT('Ctrl Pts',(5.06205045206097,49.2898545540075,-1.73757352754138));
#25366=CARTESIAN_POINT('Ctrl Pts',(3.3130744950487,49.1835361040814,-0.651400106710352));
#25367=CARTESIAN_POINT('Ctrl Pts',(2.34118543823385,49.1337197705541,-0.283572948588524));
#25368=CARTESIAN_POINT('Ctrl Pts',(0.296287131399293,49.0278408917062,0.0629522337464999));
#25369=CARTESIAN_POINT('Ctrl Pts',(-0.75800313893461,48.9732528119812,0.0324758551607617));
#25370=CARTESIAN_POINT('Ctrl Pts',(-2.77383231753296,48.8688790479336,-0.43032492871163));
#25371=CARTESIAN_POINT('Ctrl Pts',(-3.71788481900124,48.8184553700188,-0.850245570831606));
#25372=CARTESIAN_POINT('Ctrl Pts',(-5.40884456344841,48.7115493990853,-2.03557633726835));
#25373=CARTESIAN_POINT('Ctrl Pts',(-6.1356304108929,48.6595469669848,-2.79529963316335));
#25374=CARTESIAN_POINT('Ctrl Pts',(-7.25134190837716,48.5554299408883,-4.54713752306414));
#25375=CARTESIAN_POINT('Ctrl Pts',(-7.63136315832352,48.5013858118147,-5.52116125907929));
#25376=CARTESIAN_POINT('Ctrl Pts',(-7.99395463249854,48.3957106443432,-7.54934460457188));
#25377=CARTESIAN_POINT('Ctrl Pts',(-7.9772594876316,48.3463261487214,-8.58348117451226));
#25378=CARTESIAN_POINT('Ctrl Pts',(-7.54614137792062,48.2394286218675,-10.6142219063534));
#25379=CARTESIAN_POINT('Ctrl Pts',(-7.12567396603874,48.1846960942229,-11.5890835286308));
#25380=CARTESIAN_POINT('Ctrl Pts',(-5.94309054125989,48.0816064135481,-13.2983306145831));
#25381=CARTESIAN_POINT('Ctrl Pts',(-5.20022189354574,48.0291659070723,-14.0216488963176));
#25382=CARTESIAN_POINT('Ctrl Pts',(-3.47613061226199,47.922679825768,-15.1475811993493));
#25383=CARTESIAN_POINT('Ctrl Pts',(-2.51035411875744,47.8724788321516,-15.5379545432278));
#25384=CARTESIAN_POINT('Ctrl Pts',(-1.00241195566267,47.794401978617,-15.8275351151833));
#25385=CARTESIAN_POINT('Ctrl Pts',(-0.501168007523581,47.7684490267852,
-15.875));
#25386=CARTESIAN_POINT('Ctrl Pts',(2.04003480774873E-14,47.7425000069373,
-15.875));
#25387=CARTESIAN_POINT('Ctrl Pts',(-1.56819002228303E-14,47.425,-15.875));
#25388=CARTESIAN_POINT('Ctrl Pts',(-0.794856362164506,47.466155347525,-15.875));
#25389=CARTESIAN_POINT('Ctrl Pts',(-1.58661550937941,47.5071503302801,-15.7555961361419));
#25390=CARTESIAN_POINT('Ctrl Pts',(-3.35195554599498,47.5985544960704,-15.2088091003677));
#25391=CARTESIAN_POINT('Ctrl Pts',(-4.28395883803311,47.652585540312,-14.701794946948));
#25392=CARTESIAN_POINT('Ctrl Pts',(-5.87552731412188,47.7597364624359,-13.3716151818296));
#25393=CARTESIAN_POINT('Ctrl Pts',(-6.52653109150684,47.8093289243409,-12.5695465207045));
#25394=CARTESIAN_POINT('Ctrl Pts',(-7.4955427314391,47.9145121408912,-10.7483913152514));
#25395=CARTESIAN_POINT('Ctrl Pts',(-7.79883064150281,47.9688360087522,-9.74375461563591));
#25396=CARTESIAN_POINT('Ctrl Pts',(-8.00057468876214,48.0737561993779,-7.67864045101106));
#25397=CARTESIAN_POINT('Ctrl Pts',(-7.8986131005827,48.1246022992544,-6.63822515393834));
#25398=CARTESIAN_POINT('Ctrl Pts',(-7.30387333168754,48.2312802090904,-4.66510819031687));
#25399=CARTESIAN_POINT('Ctrl Pts',(-6.82057134758887,48.282736323223,-3.75004758489364));
#25400=CARTESIAN_POINT('Ctrl Pts',(-5.51816506889115,48.386402537996,-2.13637139113658));
#25401=CARTESIAN_POINT('Ctrl Pts',(-4.70449046280344,48.4411009476239,-1.45900742530222));
#25402=CARTESIAN_POINT('Ctrl Pts',(-2.8805040993486,48.5475969906744,-0.47024158232038));
#25403=CARTESIAN_POINT('Ctrl Pts',(-1.89190398115398,48.5970427217612,-0.160743512346776));
#25404=CARTESIAN_POINT('Ctrl Pts',(0.154842771348392,48.7030173077424,0.065423053042827));
#25405=CARTESIAN_POINT('Ctrl Pts',(1.19386045451051,48.756814617383,-0.0226010476609183));
#25406=CARTESIAN_POINT('Ctrl Pts',(3.19252183340366,48.8602994827606,-0.595418601074552));
#25407=CARTESIAN_POINT('Ctrl Pts',(4.13143524810454,48.913349841068,-1.07966736250788));
#25408=CARTESIAN_POINT('Ctrl Pts',(5.74941340285591,49.0203991123348,-2.37015725975462));
#25409=CARTESIAN_POINT('Ctrl Pts',(6.41852304397825,49.070288107611,-3.15695120719297));
#25410=CARTESIAN_POINT('Ctrl Pts',(7.43015648945349,49.1751261096768,-4.95724731194615));
#25411=CARTESIAN_POINT('Ctrl Pts',(7.75674079541332,49.2295856951343,-5.95707063619724));
#25412=CARTESIAN_POINT('Ctrl Pts',(8.00398623965225,49.3349570883735,-8.01656328924397));
#25413=CARTESIAN_POINT('Ctrl Pts',(7.92584933507523,49.3852621659541,-9.05594985543086));
#25414=CARTESIAN_POINT('Ctrl Pts',(7.37745291223851,49.4917846730923,-11.0409688476393));
#25415=CARTESIAN_POINT('Ctrl Pts',(6.91454042622445,49.5440318327638,-11.9682759154278));
#25416=CARTESIAN_POINT('Ctrl Pts',(5.64664929693399,49.6472299724739,-13.6140780353494));
#25417=CARTESIAN_POINT('Ctrl Pts',(4.84639023667935,49.701959249045,-14.3109211479442));
#25418=CARTESIAN_POINT('Ctrl Pts',(3.04350605084262,49.8087869894479,-15.339630622804));
#25419=CARTESIAN_POINT('Ctrl Pts',(2.06327777697,49.858169485716,-15.6703754064018));
#25420=CARTESIAN_POINT('Ctrl Pts',(0.699355133000662,49.928789427987,-15.8519168472916));
#25421=CARTESIAN_POINT('Ctrl Pts',(0.349501826097301,49.9469038133199,-15.875));
#25422=CARTESIAN_POINT('Ctrl Pts',(2.98372437868011E-14,49.965,-15.875));
#25423=CARTESIAN_POINT('Origin',(0.,-18.001,-7.93750000000004));
#25424=CARTESIAN_POINT('',(3.23349364670696E-14,52.8225000069373,-15.875));
#25425=CARTESIAN_POINT('',(-1.58903761650857E-14,52.505,-15.875));
#25426=CARTESIAN_POINT('',(-9.72063396823211E-16,-18.001,-15.875));
#25427=CARTESIAN_POINT('Ctrl Pts',(6.45317133063372E-14,52.8225000069373,
-15.875));
#25428=CARTESIAN_POINT('Ctrl Pts',(0.773569576646692,52.7824468271716,-15.875));
#25429=CARTESIAN_POINT('Ctrl Pts',(1.54453904921656,52.7425282732227,-15.7619059751812));
#25430=CARTESIAN_POINT('Ctrl Pts',(3.27171771156026,52.6530999922527,-15.2419447488513));
#25431=CARTESIAN_POINT('Ctrl Pts',(4.18864284441362,52.6006075124872,-14.757666944871));
#25432=CARTESIAN_POINT('Ctrl Pts',(5.79044053510198,52.4941311371167,-13.463730874213));
#25433=CARTESIAN_POINT('Ctrl Pts',(6.45897797152374,52.4439565573702,-12.665085600608));
#25434=CARTESIAN_POINT('Ctrl Pts',(7.45808107910025,52.3384627919826,-10.8474012410675));
#25435=CARTESIAN_POINT('Ctrl Pts',(7.77536200962594,52.2839696599145,-9.84387381973884));
#25436=CARTESIAN_POINT('Ctrl Pts',(8.00184684110837,52.1792355660142,-7.7905775789266));
#25437=CARTESIAN_POINT('Ctrl Pts',(7.91628553375303,52.1292389925771,-6.76125855492272));
#25438=CARTESIAN_POINT('Ctrl Pts',(7.35317347218804,52.0222212289997,-4.77096355284263));
#25439=CARTESIAN_POINT('Ctrl Pts',(6.87284289780254,51.9694296557435,-3.8314173847343));
#25440=CARTESIAN_POINT('Ctrl Pts',(5.58300909250724,51.8657943866653,-2.20145348555862));
#25441=CARTESIAN_POINT('Ctrl Pts',(4.78946963612395,51.8119365510112,-1.52399560683276));
#25442=CARTESIAN_POINT('Ctrl Pts',(2.99409950398244,51.7060271422976,-0.515118645584527));
#25443=CARTESIAN_POINT('Ctrl Pts',(2.01075948761862,51.6566112771505,-0.190679533404238));
#25444=CARTESIAN_POINT('Ctrl Pts',(-0.0479242187475715,51.5500186304629,
0.0688836502428259));
#25445=CARTESIAN_POINT('Ctrl Pts',(-1.10456567771461,51.4953088130379,-0.00752102230742142));
#25446=CARTESIAN_POINT('Ctrl Pts',(-3.1042403601309,51.391771481755,-0.56054811777542));
#25447=CARTESIAN_POINT('Ctrl Pts',(-4.03048770719061,51.3401050408273,-1.02294329308526));
#25448=CARTESIAN_POINT('Ctrl Pts',(-5.66283575348142,51.2334696110068,-2.28005664868103));
#25449=CARTESIAN_POINT('Ctrl Pts',(-6.35126848200509,51.1827882120263,-3.06556267474446));
#25450=CARTESIAN_POINT('Ctrl Pts',(-7.39065099008283,51.0777381993738,-4.86114796347009));
#25451=CARTESIAN_POINT('Ctrl Pts',(-7.7297322817676,51.0233734807042,-5.85498426542378));
#25452=CARTESIAN_POINT('Ctrl Pts',(-8.00311693857964,50.9182838662122,-7.90026155689908));
#25453=CARTESIAN_POINT('Ctrl Pts',(-7.94125568753201,50.868621142215,-8.93132691420704));
#25454=CARTESIAN_POINT('Ctrl Pts',(-7.42295486627348,50.7614972641422,-10.9383368889781));
#25455=CARTESIAN_POINT('Ctrl Pts',(-6.96162877025295,50.7077522190565,-11.8923214807642));
#25456=CARTESIAN_POINT('Ctrl Pts',(-5.7056586211759,50.604656784673,-13.5511567107216));
#25457=CARTESIAN_POINT('Ctrl Pts',(-4.92875937155118,50.5510208328049,-14.2442271685858));
#25458=CARTESIAN_POINT('Ctrl Pts',(-3.15674152402518,50.4448934073684,-15.2924094280659));
#25459=CARTESIAN_POINT('Ctrl Pts',(-2.17916238406381,50.3953306886788,-15.6388624867812));
#25460=CARTESIAN_POINT('Ctrl Pts',(-0.776895600253733,50.3227253985187,
-15.8465111808394));
#25461=CARTESIAN_POINT('Ctrl Pts',(-0.388274448369631,50.3026037270789,
-15.875));
#25462=CARTESIAN_POINT('Ctrl Pts',(-6.26582119522823E-14,50.2825000069373,
-15.875));
#25463=CARTESIAN_POINT('Ctrl Pts',(2.23432383705813E-14,49.965,-15.875));
#25464=CARTESIAN_POINT('Ctrl Pts',(-0.681261075343724,50.0002737144038,
-15.875));
#25465=CARTESIAN_POINT('Ctrl Pts',(-1.361186693817,50.03547828274,-15.7872884588347));
#25466=CARTESIAN_POINT('Ctrl Pts',(-3.03049655359253,50.121910285648,-15.3473599347427));
#25467=CARTESIAN_POINT('Ctrl Pts',(-3.97616063868438,50.1740893961102,-14.885896974024));
#25468=CARTESIAN_POINT('Ctrl Pts',(-5.62029138243705,50.2810227358729,-13.6352123273661));
#25469=CARTESIAN_POINT('Ctrl Pts',(-6.30743060757244,50.3313360092099,-12.8637472404363));
#25470=CARTESIAN_POINT('Ctrl Pts',(-7.36127462030046,50.4357969462637,-11.0848234209427));
#25471=CARTESIAN_POINT('Ctrl Pts',(-7.71098839802158,50.4903648478974,-10.0903156889372));
#25472=CARTESIAN_POINT('Ctrl Pts',(-8.00342981178138,50.5961556729552,-8.03699049288612));
#25473=CARTESIAN_POINT('Ctrl Pts',(-7.94880387175336,50.6460463980019,-6.99874079620579));
#25474=CARTESIAN_POINT('Ctrl Pts',(-7.44623828915304,50.7524027784839,-5.00220407522544));
#25475=CARTESIAN_POINT('Ctrl Pts',(-7.00351678260699,50.8055523242616,-4.06287997598149));
#25476=CARTESIAN_POINT('Ctrl Pts',(-5.77000092114518,50.9082591534721,-2.38590793487282));
#25477=CARTESIAN_POINT('Ctrl Pts',(-4.98334557363517,50.9629928732215,-1.67019492318765));
#25478=CARTESIAN_POINT('Ctrl Pts',(-3.20166662664349,51.0701180942583,-0.602524264433342));
#25479=CARTESIAN_POINT('Ctrl Pts',(-2.22968898315318,51.1195531981091,-0.251080012551294));
#25480=CARTESIAN_POINT('Ctrl Pts',(-0.192751057308643,51.2250199116128,
0.0651712897973573));
#25481=CARTESIAN_POINT('Ctrl Pts',(0.853616143887715,51.2791977578927,0.0218546860159068));
#25482=CARTESIAN_POINT('Ctrl Pts',(2.87160605675112,51.3836833984677,-0.465122895034999));
#25483=CARTESIAN_POINT('Ctrl Pts',(3.82364940164646,51.4351278390047,-0.904556148837716));
#25484=CARTESIAN_POINT('Ctrl Pts',(5.49281377843064,51.5419361314569,-2.11667612674403));
#25485=CARTESIAN_POINT('Ctrl Pts',(6.19730349890426,51.5927796532965,-2.87327719099847));
#25486=CARTESIAN_POINT('Ctrl Pts',(7.29152515539215,51.696846704379,-4.63108268685891));
#25487=CARTESIAN_POINT('Ctrl Pts',(7.66340527550933,51.7514934477553,-5.61998921481477));
#25488=CARTESIAN_POINT('Ctrl Pts',(7.99920554623815,51.8576596089564,-7.66684839583198));
#25489=CARTESIAN_POINT('Ctrl Pts',(7.96700279068472,51.9072681563388,-8.70390841509103));
#25490=CARTESIAN_POINT('Ctrl Pts',(7.50831207286596,52.013437504532,-10.7109027891529));
#25491=CARTESIAN_POINT('Ctrl Pts',(7.08505449358577,52.0670234901091,-11.6615744498179));
#25492=CARTESIAN_POINT('Ctrl Pts',(5.88754951617242,52.170001284794,-13.3637011068002));
#25493=CARTESIAN_POINT('Ctrl Pts',(5.11866135152908,52.223962717717,-14.0943366610575));
#25494=CARTESIAN_POINT('Ctrl Pts',(3.36375569476365,52.3311072364392,-15.1994916795358));
#25495=CARTESIAN_POINT('Ctrl Pts',(2.40037277456299,52.3807156884826,-15.5722639209813));
#25496=CARTESIAN_POINT('Ctrl Pts',(0.931959596462894,52.4567458462968,-15.833983701258));
#25497=CARTESIAN_POINT('Ctrl Pts',(0.465883173992151,52.4808779260702,-15.875));
#25498=CARTESIAN_POINT('Ctrl Pts',(-3.24740234702858E-14,52.505,-15.875));
#25499=CARTESIAN_POINT('Origin',(0.,-18.001,-7.93750000000004));
#25500=CARTESIAN_POINT('',(-2.46333824840088E-14,55.3625000069373,-15.875));
#25501=CARTESIAN_POINT('',(2.44592918861349E-14,55.045,-15.875));
#25502=CARTESIAN_POINT('',(-9.72063396823211E-16,-18.001,-15.875));
#25503=CARTESIAN_POINT('Ctrl Pts',(-2.52575738102223E-14,55.3625000069373,
-15.875));
#25504=CARTESIAN_POINT('Ctrl Pts',(0.88761857172687,55.3165417023581,-15.875));
#25505=CARTESIAN_POINT('Ctrl Pts',(1.77011756769855,55.2713889565383,-15.7260946063877));
#25506=CARTESIAN_POINT('Ctrl Pts',(3.58449937240897,55.1761581973968,-15.0942661122647));
#25507=CARTESIAN_POINT('Ctrl Pts',(4.48318907247908,55.1225090905112,-14.5683935783575));
#25508=CARTESIAN_POINT('Ctrl Pts',(6.02596616795313,55.0163930988054,-13.2050641840642));
#25509=CARTESIAN_POINT('Ctrl Pts',(6.65647325827018,54.9668417440083,-12.3816969617684));
#25510=CARTESIAN_POINT('Ctrl Pts',(7.57729478212815,54.8605781437163,-10.5229439661176));
#25511=CARTESIAN_POINT('Ctrl Pts',(7.85188655635563,54.8059142458295,-9.50207817347011));
#25512=CARTESIAN_POINT('Ctrl Pts',(7.98755464789972,54.7019597341018,-7.43510513527449));
#25513=CARTESIAN_POINT('Ctrl Pts',(7.85611325111853,54.6509510053513,-6.40942676133224));
#25514=CARTESIAN_POINT('Ctrl Pts',(7.20649584389212,54.5441790337993,-4.45223046677657));
#25515=CARTESIAN_POINT('Ctrl Pts',(6.68964065097011,54.4929165656096,-3.54098331751992));
#25516=CARTESIAN_POINT('Ctrl Pts',(5.33445751776623,54.3883039015244,-1.96884961653697));
#25517=CARTESIAN_POINT('Ctrl Pts',(4.50911833992717,54.3340819831997,-1.32319720029189));
#25518=CARTESIAN_POINT('Ctrl Pts',(2.66936874471942,54.2286936544334,-0.392525075909464));
#25519=CARTESIAN_POINT('Ctrl Pts',(1.67495331423129,54.1792242114812,-0.111474355579484));
#25520=CARTESIAN_POINT('Ctrl Pts',(-0.395625268275944,54.0720156827491,
0.0598698134383127));
#25521=CARTESIAN_POINT('Ctrl Pts',(-1.45258479174199,54.017296838446,-0.0632474876637047));
#25522=CARTESIAN_POINT('Ctrl Pts',(-3.43343402764324,53.9147195090952,-0.707348252054608));
#25523=CARTESIAN_POINT('Ctrl Pts',(-4.34111091272081,53.861307471052,-1.21306133286519));
#25524=CARTESIAN_POINT('Ctrl Pts',(-5.91269534406702,53.755009034774,-2.54273563012737));
#25525=CARTESIAN_POINT('Ctrl Pts',(-6.56172013952658,53.7052112496336,-3.35412661619982));
#25526=CARTESIAN_POINT('Ctrl Pts',(-7.52086783897476,53.5993094898124,-5.19307861402896));
#25527=CARTESIAN_POINT('Ctrl Pts',(-7.81640836407917,53.5447163268471,-6.20570129682935));
#25528=CARTESIAN_POINT('Ctrl Pts',(-7.99648604030202,53.4403657138208,-8.26628860586363));
#25529=CARTESIAN_POINT('Ctrl Pts',(-7.88748313012729,53.3899120148144,-9.29379040068007));
#25530=CARTESIAN_POINT('Ctrl Pts',(-7.28013210091988,53.2830133436423,-11.2672928240728));
#25531=CARTESIAN_POINT('Ctrl Pts',(-6.78109645907326,53.2310564179884,-12.1924339505509));
#25532=CARTESIAN_POINT('Ctrl Pts',(-5.45783190275612,53.1269103387079,-13.7931686694191));
#25533=CARTESIAN_POINT('Ctrl Pts',(-4.64796834669153,53.0728553747377,-14.4546356330282));
#25534=CARTESIAN_POINT('Ctrl Pts',(-2.82977960591002,52.9671956648927,-15.4239008199022));
#25535=CARTESIAN_POINT('Ctrl Pts',(-1.84076920880454,52.9178096755865,-15.7262998319337));
#25536=CARTESIAN_POINT('Ctrl Pts',(-0.54814992503158,52.8508816136455,-15.8608219119256));
#25537=CARTESIAN_POINT('Ctrl Pts',(-0.273911963877,52.8366823706966,-15.875));
#25538=CARTESIAN_POINT('Ctrl Pts',(6.85562717706034E-14,52.8225000069373,
-15.875));
#25539=CARTESIAN_POINT('Ctrl Pts',(-3.42781358853017E-14,52.505,-15.875));
#25540=CARTESIAN_POINT('Ctrl Pts',(-0.568805192377397,52.5344510762958,
-15.875));
#25541=CARTESIAN_POINT('Ctrl Pts',(-1.13732232065543,52.5638872374713,-15.8138577872502));
#25542=CARTESIAN_POINT('Ctrl Pts',(-2.70703094247271,52.6451621783525,-15.4706097604538));
#25543=CARTESIAN_POINT('Ctrl Pts',(-3.66545458389885,52.6959677070125,-15.0536927628113));
#25544=CARTESIAN_POINT('Ctrl Pts',(-5.35996431105652,52.8026354726181,-13.8810751253922));
#25545=CARTESIAN_POINT('Ctrl Pts',(-6.08211127948475,52.8541413740709,-13.139716279437));
#25546=CARTESIAN_POINT('Ctrl Pts',(-7.21715707056025,52.9577767420853,-11.4039417446916));
#25547=CARTESIAN_POINT('Ctrl Pts',(-7.61147670373317,53.0124780967622,-10.4212172385492));
#25548=CARTESIAN_POINT('Ctrl Pts',(-7.99124082629523,53.1189976509299,-8.38146625795112));
#25549=CARTESIAN_POINT('Ctrl Pts',(-7.98165426017353,53.1684353096838,-7.3457038996455));
#25550=CARTESIAN_POINT('Ctrl Pts',(-7.56733219350833,53.274394399366,-5.32856309764741));
#25551=CARTESIAN_POINT('Ctrl Pts',(-7.16391753611599,53.3282065003057,-4.36685224739507));
#25552=CARTESIAN_POINT('Ctrl Pts',(-6.00411927873589,53.4317278818505,-2.64143505455244));
#25553=CARTESIAN_POINT('Ctrl Pts',(-5.2547732797613,53.4847149013944,-1.89718788925229));
#25554=CARTESIAN_POINT('Ctrl Pts',(-3.52949948587456,53.5917566649436,-0.754624459901292));
#25555=CARTESIAN_POINT('Ctrl Pts',(-2.57506355292129,53.6416707087415,-0.359892258863898));
#25556=CARTESIAN_POINT('Ctrl Pts',(-0.550748628270484,53.746483840006,0.0491226757877679));
#25557=CARTESIAN_POINT('Ctrl Pts',(0.501220410293203,53.8009517331103,0.0523834362455195));
#25558=CARTESIAN_POINT('Ctrl Pts',(2.53689294035174,53.9063529281055,-0.345805101373066));
#25559=CARTESIAN_POINT('Ctrl Pts',(3.50169336609131,53.9566255404585,-0.739738490901493));
#25560=CARTESIAN_POINT('Ctrl Pts',(5.22183529061327,54.0631369800951,-1.87193984619186));
#25561=CARTESIAN_POINT('Ctrl Pts',(5.96193048657355,54.1154425953717,-2.59768254400995));
#25562=CARTESIAN_POINT('Ctrl Pts',(7.13817560015142,54.2186077349236,-4.31052145182514));
#25563=CARTESIAN_POINT('Ctrl Pts',(7.55515623808315,54.2733381452226,-5.28647299768086));
#25564=CARTESIAN_POINT('Ctrl Pts',(7.97941717874886,54.3801873812773,-7.31846109431562));
#25565=CARTESIAN_POINT('Ctrl Pts',(7.99261080995647,54.4295698712085,-8.35282137566351));
#25566=CARTESIAN_POINT('Ctrl Pts',(7.6231181130602,54.5352853019203,-10.379580022952));
#25567=CARTESIAN_POINT('Ctrl Pts',(7.2399605875748,54.5893004394446,-11.3519959759335));
#25568=CARTESIAN_POINT('Ctrl Pts',(6.1183600267905,54.6933403475528,-13.1003543210902));
#25569=CARTESIAN_POINT('Ctrl Pts',(5.38857828921182,54.7454647732774,-13.8580363977351));
#25570=CARTESIAN_POINT('Ctrl Pts',(3.69305506784267,54.8523898023613,-15.0377122934536));
#25571=CARTESIAN_POINT('Ctrl Pts',(2.74762010323095,54.9027362331134,-15.454297360553));
#25572=CARTESIAN_POINT('Ctrl Pts',(1.17380103557826,54.9842240009087,-15.8098607310094));
#25573=CARTESIAN_POINT('Ctrl Pts',(0.587101634914653,55.0146015871955,-15.875));
#25574=CARTESIAN_POINT('Ctrl Pts',(6.80011602582908E-14,55.045,-15.875));
#25575=CARTESIAN_POINT('Origin',(0.,-18.001,-7.93750000000004));
#25576=CARTESIAN_POINT('',(-1.94292120560783E-14,57.9025000069372,-15.875));
#25577=CARTESIAN_POINT('',(8.2569746205115E-15,57.585,-15.875));
#25578=CARTESIAN_POINT('',(-9.72063396823211E-16,-18.001,-15.875));
#25579=CARTESIAN_POINT('Ctrl Pts',(-1.94289029309402E-14,57.9025000069372,
-15.875));
#25580=CARTESIAN_POINT('Ctrl Pts',(1.00230603299107,57.8506035196249,-15.875));
#25581=CARTESIAN_POINT('Ctrl Pts',(1.9959609410133,57.8006823389778,-15.6851412199518));
#25582=CARTESIAN_POINT('Ctrl Pts',(3.89102299059962,57.6984103445198,-14.9329972766124));
#25583=CARTESIAN_POINT('Ctrl Pts',(4.76979217675884,57.6443450358377,-14.3660308679274));
#25584=CARTESIAN_POINT('Ctrl Pts',(6.25173435119394,57.5387003001706,-12.9344540107633));
#25585=CARTESIAN_POINT('Ctrl Pts',(6.84387225904376,57.4893124928267,-12.086611652602));
#25586=CARTESIAN_POINT('Ctrl Pts',(7.68405028232776,57.3823794642433,-10.1880615929251));
#25587=CARTESIAN_POINT('Ctrl Pts',(7.91431425195137,57.3276457713469,-9.15137546263761));
#25588=CARTESIAN_POINT('Ctrl Pts',(7.95686252569159,57.2246127701732,-7.07285951960697));
#25589=CARTESIAN_POINT('Ctrl Pts',(7.77829154751339,57.1720698458426,-6.05128377736823));
#25590=CARTESIAN_POINT('Ctrl Pts',(7.04015426818784,57.0656028579094,-4.12904278181492));
#25591=CARTESIAN_POINT('Ctrl Pts',(6.48613432213068,57.0154533099021,-3.2472746964605));
#25592=CARTESIAN_POINT('Ctrl Pts',(5.06426424004539,56.9099352259738,-1.7371772449326));
#25593=CARTESIAN_POINT('Ctrl Pts',(4.2070022646224,56.8554356091949,-1.12633812031294));
#25594=CARTESIAN_POINT('Ctrl Pts',(2.32294817932973,56.7507227367625,-0.278840170685674));
#25595=CARTESIAN_POINT('Ctrl Pts',(1.31724792115926,56.7007032679948,-0.0434516304225713));
#25596=CARTESIAN_POINT('Ctrl Pts',(-0.749521171617977,56.5936919835465,
0.0333113444225467));
#25597=CARTESIAN_POINT('Ctrl Pts',(-1.7910609478416,56.5409514172919,-0.134456053490981));
#25598=CARTESIAN_POINT('Ctrl Pts',(-3.73884162559752,56.4372861119748,-0.85982070936449));
#25599=CARTESIAN_POINT('Ctrl Pts',(-4.62778972832387,56.3834163166858,-1.40635282421876));
#25600=CARTESIAN_POINT('Ctrl Pts',(-6.14034710128368,56.2775203576562,-2.80404622174758));
#25601=CARTESIAN_POINT('Ctrl Pts',(-6.75167720510281,56.2281093692751,-3.63970193484849));
#25602=CARTESIAN_POINT('Ctrl Pts',(-7.6323961671839,56.1214975064136,-5.51855737820616));
#25603=CARTESIAN_POINT('Ctrl Pts',(-7.88498224369959,56.066785643353,-6.54754730732683));
#25604=CARTESIAN_POINT('Ctrl Pts',(-7.97428981649316,55.9632746391773,-8.6205772700019));
#25605=CARTESIAN_POINT('Ctrl Pts',(-7.81940301583157,55.9115645027195,-9.64426158415518));
#25606=CARTESIAN_POINT('Ctrl Pts',(-7.12570651529608,55.8049377806125,-11.584186062756));
#25607=CARTESIAN_POINT('Ctrl Pts',(-6.59031936774201,55.7542884945185,-12.4808155020628));
#25608=CARTESIAN_POINT('Ctrl Pts',(-5.20189381553948,55.6492125077333,-14.0224188859396));
#25609=CARTESIAN_POINT('Ctrl Pts',(-4.36056678196882,55.5948397826011,-14.6510211460246));
#25610=CARTESIAN_POINT('Ctrl Pts',(-2.49860396205691,55.4897694274817,-15.5406713495898));
#25611=CARTESIAN_POINT('Ctrl Pts',(-1.49856329833446,55.4400912501693,-15.7991481118117));
#25612=CARTESIAN_POINT('Ctrl Pts',(-0.318002086543258,55.378965228842,-15.8702274642353));
#25613=CARTESIAN_POINT('Ctrl Pts',(-0.158918541145936,55.3707283461698,
-15.875));
#25614=CARTESIAN_POINT('Ctrl Pts',(-4.04537514597791E-14,55.3625000069373,
-15.875));
#25615=CARTESIAN_POINT('Ctrl Pts',(6.75848266240564E-14,55.045,-15.875));
#25616=CARTESIAN_POINT('Ctrl Pts',(-0.452205833663068,55.0684139010809,
-15.875));
#25617=CARTESIAN_POINT('Ctrl Pts',(-0.904650297188487,55.0918401577207,
-15.836356781565));
#25618=CARTESIAN_POINT('Ctrl Pts',(-2.36712438493148,55.1675628067331,-15.5834915453526));
#25619=CARTESIAN_POINT('Ctrl Pts',(-3.33808801962979,55.2174301128519,-15.212223217014));
#25620=CARTESIAN_POINT('Ctrl Pts',(-5.08327993400997,55.3237749298375,-14.1199751343461));
#25621=CARTESIAN_POINT('Ctrl Pts',(-5.84100233549749,55.3769891161994,-13.4096943856778));
#25622=CARTESIAN_POINT('Ctrl Pts',(-7.0573993431594,55.4796620485725,-11.7198971070282));
#25623=CARTESIAN_POINT('Ctrl Pts',(-7.49646653809424,55.5343951520355,-10.7510672271912));
#25624=CARTESIAN_POINT('Ctrl Pts',(-7.96421846051841,55.6415392240897,-8.72722283067459));
#25625=CARTESIAN_POINT('Ctrl Pts',(-7.99958288630385,55.6909818503537,-7.69431432987161));
#25626=CARTESIAN_POINT('Ctrl Pts',(-7.67382709560291,55.7964298005714,-5.65877655536126));
#25627=CARTESIAN_POINT('Ctrl Pts',(-7.31062296358912,55.8506184786743,-4.6763531798273));
#25628=CARTESIAN_POINT('Ctrl Pts',(-6.22638360369634,55.9551350507709,-2.90617559972928));
#25629=CARTESIAN_POINT('Ctrl Pts',(-5.51551775745132,56.0065346684165,-2.13567353567475));
#25630=CARTESIAN_POINT('Ctrl Pts',(-3.84884362045724,56.113334246933,-0.920412360942083));
#25631=CARTESIAN_POINT('Ctrl Pts',(-2.91215705111828,56.1642169891423,-0.482811428301656));
#25632=CARTESIAN_POINT('Ctrl Pts',(-0.902774366284792,56.2682569725173,
0.0176270306812168));
#25633=CARTESIAN_POINT('Ctrl Pts',(0.152732482785965,56.3229080431463,0.0672248201678767));
#25634=CARTESIAN_POINT('Ctrl Pts',(2.20363894720756,56.4290980068961,-0.243069237349244));
#25635=CARTESIAN_POINT('Ctrl Pts',(3.18036814836036,56.4786919234767,-0.592738436171752));
#25636=CARTESIAN_POINT('Ctrl Pts',(4.9489277748518,56.5848485409494,-1.64663972616407));
#25637=CARTESIAN_POINT('Ctrl Pts',(5.72336896610363,56.6384499971866,-2.34195994698209));
#25638=CARTESIAN_POINT('Ctrl Pts',(6.97435306189161,56.7414640804755,-4.0049848404559));
#25639=CARTESIAN_POINT('Ctrl Pts',(7.43287526798715,56.7953584552385,-4.96108228034264));
#25640=CARTESIAN_POINT('Ctrl Pts',(7.94457635178483,56.9024966980779,-6.97052835202683));
#25641=CARTESIAN_POINT('Ctrl Pts',(8.0029508044703,56.9521212196272,-8.00184288282747));
#25642=CARTESIAN_POINT('Ctrl Pts',(7.72266974891675,57.0572603672783,-10.0458852922068));
#25643=CARTESIAN_POINT('Ctrl Pts',(7.38039817878971,57.1116038770423,-11.0382543104064));
#25644=CARTESIAN_POINT('Ctrl Pts',(6.33510138818855,57.2165859458937,-12.8305381647968));
#25645=CARTESIAN_POINT('Ctrl Pts',(5.6437278518194,57.2673526819247,-13.6140890221231));
#25646=CARTESIAN_POINT('Ctrl Pts',(4.00687273557042,57.3740105583108,-14.8657364817318));
#25647=CARTESIAN_POINT('Ctrl Pts',(3.07925268208924,57.4255652640134,-15.3248888283259));
#25648=CARTESIAN_POINT('Ctrl Pts',(1.40746958896367,57.5121253237411,-15.7811964611633));
#25649=CARTESIAN_POINT('Ctrl Pts',(0.704519872836865,57.5485220128,-15.875));
#25650=CARTESIAN_POINT('Ctrl Pts',(4.53803661315533E-14,57.585,-15.875));
#25651=CARTESIAN_POINT('Origin',(0.,-18.001,-7.93750000000004));
#25652=CARTESIAN_POINT('',(-2.07476018978207E-14,60.4425000069372,-15.875));
#25653=CARTESIAN_POINT('',(-6.10653576057646E-15,60.125,-15.875));
#25654=CARTESIAN_POINT('',(-9.72063396823211E-16,-18.001,-15.875));
#25655=CARTESIAN_POINT('Ctrl Pts',(-3.1866062751E-14,60.4425000069372,-15.875));
#25656=CARTESIAN_POINT('Ctrl Pts',(0.0810659007883464,60.4383026506875,
-15.875));
#25657=CARTESIAN_POINT('Ctrl Pts',(0.162182741164532,60.4341026569347,-15.8737581149016));
#25658=CARTESIAN_POINT('Ctrl Pts',(1.27711240176256,60.3763748461854,-15.8395640913277));
#25659=CARTESIAN_POINT('Ctrl Pts',(2.29479964502656,60.3257591259032,-15.6061075714052));
#25660=CARTESIAN_POINT('Ctrl Pts',(4.18883445623646,60.2206557380066,-14.7595152794035));
#25661=CARTESIAN_POINT('Ctrl Pts',(5.04594995342874,60.166274628506,-14.1523684799919));
#25662=CARTESIAN_POINT('Ctrl Pts',(6.4654526326233,60.0612247880728,-12.654398213762));
#25663=CARTESIAN_POINT('Ctrl Pts',(7.01909774746457,60.0115297902125,-11.7824239693426));
#25664=CARTESIAN_POINT('Ctrl Pts',(7.77410531512426,59.9044175293509,-9.85256059500888));
#25665=CARTESIAN_POINT('Ctrl Pts',(7.95883998364154,59.8507892297312,-8.8096612890105));
#25666=CARTESIAN_POINT('Ctrl Pts',(7.91262212587057,59.7476296544674,-6.72976726518009));
#25667=CARTESIAN_POINT('Ctrl Pts',(7.68884565251932,59.6939666898923,-5.71271701463284));
#25668=CARTESIAN_POINT('Ctrl Pts',(6.86647297847103,59.5878629275397,-3.82522195452598));
#25669=CARTESIAN_POINT('Ctrl Pts',(6.27718915538661,59.5383232157608,-2.97199908110532));
#25670=CARTESIAN_POINT('Ctrl Pts',(4.7920745275957,59.4320381060541,-1.52374719664043));
#25671=CARTESIAN_POINT('Ctrl Pts',(3.90515282460579,59.3773706251354,-0.948215472250059));
#25672=CARTESIAN_POINT('Ctrl Pts',(1.98005962899069,59.2734415871574,-0.182958397065402));
#25673=CARTESIAN_POINT('Ctrl Pts',(0.96364416930764,59.2223946955456,0.00762683433684866));
#25674=CARTESIAN_POINT('Ctrl Pts',(-1.09834352675043,59.1156309778942,-0.0081930587602151));
#25675=CARTESIAN_POINT('Ctrl Pts',(-2.12422647149672,59.0644081240037,-0.219475798871333));
#25676=CARTESIAN_POINT('Ctrl Pts',(-4.03709441305572,58.9597672746394,-1.0249483296966));
#25677=CARTESIAN_POINT('Ctrl Pts',(-4.90553716562939,58.9055357266085,-1.61159017972865));
#25678=CARTESIAN_POINT('Ctrl Pts',(-6.35728716070558,58.8001652751744,-3.07571052201888));
#25679=CARTESIAN_POINT('Ctrl Pts',(-6.93071050059505,58.7506869565062,-3.93533580739935));
#25680=CARTESIAN_POINT('Ctrl Pts',(-7.730857389611,58.643483347444,-5.8523875790016));
#25681=CARTESIAN_POINT('Ctrl Pts',(-7.93900584987437,58.5888280890297,-6.89564522768173));
#25682=CARTESIAN_POINT('Ctrl Pts',(-7.93601188136394,58.4862177532171,-8.97842987475304));
#25683=CARTESIAN_POINT('Ctrl Pts',(-7.73424899273246,58.432791164476,-9.99783257480142));
#25684=CARTESIAN_POINT('Ctrl Pts',(-6.95289199510558,58.3265026038045,-11.9024072243827));
#25685=CARTESIAN_POINT('Ctrl Pts',(-6.3807665232794,58.2767222658109,-12.7695853151988));
#25686=CARTESIAN_POINT('Ctrl Pts',(-4.9264068263455,58.1707986014925,-14.2482912875934));
#25687=CARTESIAN_POINT('Ctrl Pts',(-4.05382565662097,58.1162006356794,-14.8412769218402));
#25688=CARTESIAN_POINT('Ctrl Pts',(-2.14856615042794,58.0118723832767,-15.6469501937843));
#25689=CARTESIAN_POINT('Ctrl Pts',(-1.13736426870951,57.9613894163571,-15.859519147805));
#25690=CARTESIAN_POINT('Ctrl Pts',(-0.0757975649706369,57.9064245841019,
-15.8747286596535));
#25691=CARTESIAN_POINT('Ctrl Pts',(-0.0378925437277257,57.9044619724947,
-15.875));
#25692=CARTESIAN_POINT('Ctrl Pts',(-1.65020682103393E-14,57.9025000069372,
-15.875));
#25693=CARTESIAN_POINT('Ctrl Pts',(4.16333634234434E-14,57.585,-15.875));
#25694=CARTESIAN_POINT('Ctrl Pts',(-0.339782330037041,57.6025929394809,
-15.875));
#25695=CARTESIAN_POINT('Ctrl Pts',(-0.679929883044116,57.620204789143,-15.8531829030035));
#25696=CARTESIAN_POINT('Ctrl Pts',(-2.03597579501405,57.6904168971709,-15.677760512839));
#25697=CARTESIAN_POINT('Ctrl Pts',(-3.01846250588086,57.7398472625498,-15.3500371537862));
#25698=CARTESIAN_POINT('Ctrl Pts',(-4.81038415668122,57.8457912036368,-14.3352790937223));
#25699=CARTESIAN_POINT('Ctrl Pts',(-5.60146190223546,57.8996175171944,-13.6554687198988));
#25700=CARTESIAN_POINT('Ctrl Pts',(-6.88627321846298,58.003174129505,-12.0211764769394));
#25701=CARTESIAN_POINT('Ctrl Pts',(-7.36378911356066,58.0561003466381,-11.0794791319821));
#25702=CARTESIAN_POINT('Ctrl Pts',(-7.92025569096539,58.1631347809417,-9.08668634075335));
#25703=CARTESIAN_POINT('Ctrl Pts',(-8.00229948056471,58.2130736377048,-8.05710234326254));
#25704=CARTESIAN_POINT('Ctrl Pts',(-7.76885187234643,58.3178625581627,-6.00495505647574));
#25705=CARTESIAN_POINT('Ctrl Pts',(-7.44832322723047,58.3723383680281,-5.00283465188581));
#25706=CARTESIAN_POINT('Ctrl Pts',(-6.44323380849496,58.4777682604099,-3.18839246259855));
#25707=CARTESIAN_POINT('Ctrl Pts',(-5.7717540276406,58.5280100230615,-2.39168096627223));
#25708=CARTESIAN_POINT('Ctrl Pts',(-4.16543162801495,58.6345107045546,-1.10317396789013));
#25709=CARTESIAN_POINT('Ctrl Pts',(-3.24712380499084,58.6868733861705,-0.622126441379978));
#25710=CARTESIAN_POINT('Ctrl Pts',(-1.2552562525196,58.790006487002,-0.0297074686909277));
#25711=CARTESIAN_POINT('Ctrl Pts',(-0.198198163241447,58.8447378763312,
0.0668345080933514));
#25712=CARTESIAN_POINT('Ctrl Pts',(1.86583999797739,58.9516077610969,-0.15464714389086));
#25713=CARTESIAN_POINT('Ctrl Pts',(2.85402266121887,59.000990762468,-0.460286273074888));
#25714=CARTESIAN_POINT('Ctrl Pts',(4.66889230269638,59.1066891337393,-1.43539015288564));
#25715=CARTESIAN_POINT('Ctrl Pts',(5.47637777191838,59.1607166930885,-2.09922980586532));
#25716=CARTESIAN_POINT('Ctrl Pts',(6.79475781869968,59.264789534924,-3.70428102513771));
#25717=CARTESIAN_POINT('Ctrl Pts',(7.29106346199966,59.3168616505675,-4.63153621958218));
#25718=CARTESIAN_POINT('Ctrl Pts',(7.89194961574985,59.4237785969329,-6.60751033148493));
#25719=CARTESIAN_POINT('Ctrl Pts',(7.99752408848844,59.4741575859055,-7.63528348516183));
#25720=CARTESIAN_POINT('Ctrl Pts',(7.81065922498977,59.5785662358421,-9.69484408682032));
#25721=CARTESIAN_POINT('Ctrl Pts',(7.51192916122549,59.633146439635,-10.7061672575415));
#25722=CARTESIAN_POINT('Ctrl Pts',(6.54693177542636,59.7389904444348,-12.5420457180578));
#25723=CARTESIAN_POINT('Ctrl Pts',(5.89506370655858,59.7888356752205,-13.3515877405736));
#25724=CARTESIAN_POINT('Ctrl Pts',(4.31894432922972,59.8951692845151,-14.6761759419956));
#25725=CARTESIAN_POINT('Ctrl Pts',(3.4098803020298,59.9484463287595,-15.1787168423269));
#25726=CARTESIAN_POINT('Ctrl Pts',(1.64368893807556,60.0398945737998,-15.7467998769928));
#25727=CARTESIAN_POINT('Ctrl Pts',(0.823610448553,60.082355849624,-15.875));
#25728=CARTESIAN_POINT('Ctrl Pts',(1.0547118733939E-14,60.125,-15.875));
#25729=CARTESIAN_POINT('Origin',(0.,-18.001,-7.93750000000004));
#25730=CARTESIAN_POINT('',(-1.93598231170393E-14,62.9825000069372,-15.875));
#25731=CARTESIAN_POINT('',(2.011970106995E-15,62.665,-15.875));
#25732=CARTESIAN_POINT('',(-9.72063396823211E-16,-18.001,-15.875));
#25733=CARTESIAN_POINT('Ctrl Pts',(-3.15372727932584E-14,62.9825000069372,
-15.875));
#25734=CARTESIAN_POINT('Ctrl Pts',(0.202097295059188,62.9720359975791,-15.875));
#25735=CARTESIAN_POINT('Ctrl Pts',(0.404416516961662,62.9615604974959,-15.8672817297692));
#25736=CARTESIAN_POINT('Ctrl Pts',(1.63259922643455,62.8979687737096,-15.7731590536421));
#25737=CARTESIAN_POINT('Ctrl Pts',(2.63364172886998,62.8482064285161,-15.4957337446288));
#25738=CARTESIAN_POINT('Ctrl Pts',(4.48821271510264,62.7422597601501,-14.5671154837294));
#25739=CARTESIAN_POINT('Ctrl Pts',(5.32108159298415,62.6876568181105,-13.919307059151));
#25740=CARTESIAN_POINT('Ctrl Pts',(6.67410565714498,62.5833522595343,-12.3543254453134));
#25741=CARTESIAN_POINT('Ctrl Pts',(7.18756598284996,62.532837992169,-11.4575792833147));
#25742=CARTESIAN_POINT('Ctrl Pts',(7.85095345772089,62.4259538799676,-9.50257986084704));
#25743=CARTESIAN_POINT('Ctrl Pts',(7.98829852933518,62.3740857654634,-8.46088434379739));
#25744=CARTESIAN_POINT('Ctrl Pts',(7.85354132625254,62.2698825144621,-6.38856407192546));
#25745=CARTESIAN_POINT('Ctrl Pts',(7.5845388285196,62.2158063716604,-5.37781803848968));
#25746=CARTESIAN_POINT('Ctrl Pts',(6.67850515167161,62.1101775500444,-3.52715093599002));
#25747=CARTESIAN_POINT('Ctrl Pts',(6.05410047661468,62.0607874182207,-2.70285965881397));
#25748=CARTESIAN_POINT('Ctrl Pts',(4.50625049009188,61.9538361533165,-1.31906693082812));
#25749=CARTESIAN_POINT('Ctrl Pts',(3.59062340200669,61.8991019948323,-0.780853875088621));
#25750=CARTESIAN_POINT('Ctrl Pts',(1.62582918411219,61.7960985177442,-0.100652828940019));
#25751=CARTESIAN_POINT('Ctrl Pts',(0.59875659387989,61.7435018795739,0.0438133331380165));
#25752=CARTESIAN_POINT('Ctrl Pts',(-1.45730781215225,61.6370448526294,-0.0670459362428228));
#25753=CARTESIAN_POINT('Ctrl Pts',(-2.46661620655107,61.5869213186422,-0.322801609672158));
#25754=CARTESIAN_POINT('Ctrl Pts',(-4.34099082680039,61.4813776395764,-1.21092100594497));
#25755=CARTESIAN_POINT('Ctrl Pts',(-5.18610754905106,61.4268712647324,-1.83869869527229));
#25756=CARTESIAN_POINT('Ctrl Pts',(-6.57231654782088,61.322180938439,-3.37068079576465));
#25757=CARTESIAN_POINT('Ctrl Pts',(-7.10574521383588,61.2721368134212,-4.2551702600581));
#25758=CARTESIAN_POINT('Ctrl Pts',(-7.81464166704676,61.1651324282433,-6.19782536029372));
#25759=CARTESIAN_POINT('Ctrl Pts',(-7.97550281132237,61.1124453895675,-7.24019516760617));
#25760=CARTESIAN_POINT('Ctrl Pts',(-7.8848546839527,61.00874841751,-9.31656609692131));
#25761=CARTESIAN_POINT('Ctrl Pts',(-7.63840144165978,60.9548660605398,-10.3307035254926));
#25762=CARTESIAN_POINT('Ctrl Pts',(-6.77398691623051,60.8489844409294,-12.200027200501));
#25763=CARTESIAN_POINT('Ctrl Pts',(-6.16707844614086,60.7995781925467,-13.0387922031794));
#25764=CARTESIAN_POINT('Ctrl Pts',(-4.6504368530779,60.6929460987205,-14.4550522143311));
#25765=CARTESIAN_POINT('Ctrl Pts',(-3.7489923611215,60.6382321649877,-15.012121390154));
#25766=CARTESIAN_POINT('Ctrl Pts',(-1.87990224912114,60.5387968203394,-15.7068054476382));
#25767=CARTESIAN_POINT('Ctrl Pts',(-0.943373418127358,60.4913451350848,
-15.875));
#25768=CARTESIAN_POINT('Ctrl Pts',(-3.96904731303493E-14,60.4425000069372,
-15.875));
#25769=CARTESIAN_POINT('Ctrl Pts',(1.7277845820729E-14,60.125,-15.875));
#25770=CARTESIAN_POINT('Ctrl Pts',(-0.226288585779035,60.1367165639378,
-15.875));
#25771=CARTESIAN_POINT('Ctrl Pts',(-0.452843794342004,60.1484469328263,
-15.8653234055953));
#25772=CARTESIAN_POINT('Ctrl Pts',(-1.6992260327771,60.2129809752188,-15.7583040034926));
#25773=CARTESIAN_POINT('Ctrl Pts',(-2.6928575836504,60.2624313282865,-15.4741365811628));
#25774=CARTESIAN_POINT('Ctrl Pts',(-4.52949287564852,60.3678610680446,-14.5378172957273));
#25775=CARTESIAN_POINT('Ctrl Pts',(-5.35259392234133,60.4220600864358,-13.8898368067058));
#25776=CARTESIAN_POINT('Ctrl Pts',(-6.70314601741735,60.5266063575655,-12.3135105812172));
#25777=CARTESIAN_POINT('Ctrl Pts',(-7.21741767317199,60.5779632451856,-11.4002390114388));
#25778=CARTESIAN_POINT('Ctrl Pts',(-7.86089989495349,60.6847543784082,-9.44066014903061));
#25779=CARTESIAN_POINT('Ctrl Pts',(-7.98908164381013,60.735675385345,-8.41471175824484));
#25780=CARTESIAN_POINT('Ctrl Pts',(-7.84696393519802,60.8396891769703,-6.34863050227391));
#25781=CARTESIAN_POINT('Ctrl Pts',(-7.56932150876318,60.8943443121659,-5.32893387479916));
#25782=CARTESIAN_POINT('Ctrl Pts',(-6.64292842814975,61.0005570846869,-3.47302337167262));
#25783=CARTESIAN_POINT('Ctrl Pts',(-6.00974115202779,61.0501373773226,-2.65138266101345));
#25784=CARTESIAN_POINT('Ctrl Pts',(-4.46277146764076,61.15628161346,-1.29289580927297));
#25785=CARTESIAN_POINT('Ctrl Pts',(-3.56275523162316,61.2098978636032,-0.76992870869702));
#25786=CARTESIAN_POINT('Ctrl Pts',(-1.59559148720447,61.312946760467,-0.0914966241905969));
#25787=CARTESIAN_POINT('Ctrl Pts',(-0.545085500598828,61.3667770602637,
0.0505518195889912));
#25788=CARTESIAN_POINT('Ctrl Pts',(1.52401785543784,61.4739092060654,-0.0807414638915074));
#25789=CARTESIAN_POINT('Ctrl Pts',(2.52325426037719,61.5235497053457,-0.342468272518263));
#25790=CARTESIAN_POINT('Ctrl Pts',(4.38205626604549,61.6286677796305,-1.23803692927503));
#25791=CARTESIAN_POINT('Ctrl Pts',(5.22110593153846,61.6830204226522,-1.86911385571455));
#25792=CARTESIAN_POINT('Ctrl Pts',(6.60477821039722,61.7880316012073,-3.41513007765455));
#25793=CARTESIAN_POINT('Ctrl Pts',(7.13751660206741,61.838761541179,-4.31385899089811));
#25794=CARTESIAN_POINT('Ctrl Pts',(7.82490539208493,61.9454098588283,-6.25627151994931));
#25795=CARTESIAN_POINT('Ctrl Pts',(7.97643435265441,61.9970119853646,-7.28024705713402));
#25796=CARTESIAN_POINT('Ctrl Pts',(7.88049079223563,62.1005883383699,-9.35244792683858));
#25797=CARTESIAN_POINT('Ctrl Pts',(7.62474681542995,62.1552949485995,-10.3803051201895));
#25798=CARTESIAN_POINT('Ctrl Pts',(6.7382818869712,62.2618587950999,-12.256318494557));
#25799=CARTESIAN_POINT('Ctrl Pts',(6.12421616988546,62.3112826412378,-13.0902280433275));
#25800=CARTESIAN_POINT('Ctrl Pts',(4.60732456708991,62.4172119016502,-14.4830501085843));
#25801=CARTESIAN_POINT('Ctrl Pts',(3.7169602271815,62.4710517623904,-15.0266493449583));
#25802=CARTESIAN_POINT('Ctrl Pts',(1.86707321036374,62.569311797536,-15.7091456472123));
#25803=CARTESIAN_POINT('Ctrl Pts',(0.936777902232627,62.6164963684569,-15.875));
#25804=CARTESIAN_POINT('Ctrl Pts',(3.33066907387547E-15,62.665,-15.875));
#25805=CARTESIAN_POINT('Origin',(0.,-18.001,-7.93750000000004));
#25806=CARTESIAN_POINT('',(1.25243943714144E-14,65.5225000069373,-15.875));
#25807=CARTESIAN_POINT('',(1.66882607035807E-8,65.2049999982718,-15.875));
#25808=CARTESIAN_POINT('',(-9.72063396823211E-16,-18.001,-15.875));
#25809=CARTESIAN_POINT('Ctrl Pts',(1.33226762955019E-14,65.5225000069373,
-15.875));
#25810=CARTESIAN_POINT('Ctrl Pts',(0.31798534665268,65.5060356517754,-15.875));
#25811=CARTESIAN_POINT('Ctrl Pts',(0.636316449646511,65.4895533943575,-15.8558922241094));
#25812=CARTESIAN_POINT('Ctrl Pts',(1.97149062497534,65.4204219640669,-15.6943732610773));
#25813=CARTESIAN_POINT('Ctrl Pts',(2.95621850317269,65.3710202288267,-15.3750150925043));
#25814=CARTESIAN_POINT('Ctrl Pts',(4.77049532067681,65.2643670008657,-14.367720393661));
#25815=CARTESIAN_POINT('Ctrl Pts',(5.57801341588977,65.2096509963783,-13.6813045822467));
#25816=CARTESIAN_POINT('Ctrl Pts',(6.86449941164187,65.1061974727468,-12.0527046457698));
#25817=CARTESIAN_POINT('Ctrl Pts',(7.3383808086568,65.0543910989868,-11.1319720576279));
#25818=CARTESIAN_POINT('Ctrl Pts',(7.91170114059625,64.9477834231852,-9.15332177337935));
#25819=CARTESIAN_POINT('Ctrl Pts',(8.00264487832203,64.8972024958372,-8.1133662550448));
#25820=CARTESIAN_POINT('Ctrl Pts',(7.77989688373839,64.7920704222477,-6.05077387734165));
#25821=CARTESIAN_POINT('Ctrl Pts',(7.46585471838791,64.7376806043326,-5.0482921676172));
#25822=CARTESIAN_POINT('Ctrl Pts',(6.47715265519464,64.6326524598438,-3.23668389145497));
#25823=CARTESIAN_POINT('Ctrl Pts',(5.81779588770328,64.5829392756886,-2.44164728380225));
#25824=CARTESIAN_POINT('Ctrl Pts',(4.21402507587749,64.4758333815647,-1.12974213176186));
#25825=CARTESIAN_POINT('Ctrl Pts',(3.27881719531308,64.422267612215,-0.633215477804607));
#25826=CARTESIAN_POINT('Ctrl Pts',(1.28577089731952,64.3190734793731,-0.0371655150868924));
#25827=CARTESIAN_POINT('Ctrl Pts',(0.249068143622023,64.2653960300383,0.0628911822732485));
#25828=CARTESIAN_POINT('Ctrl Pts',(-1.79992259375097,64.1593052570558,-0.13882489303033));
#25829=CARTESIAN_POINT('Ctrl Pts',(-2.79296634004953,64.1097773484048,-0.436939094872029));
#25830=CARTESIAN_POINT('Ctrl Pts',(-4.62798300031585,64.0034697089433,-1.40433243496831));
#25831=CARTESIAN_POINT('Ctrl Pts',(-5.44861613942039,63.9487985565476,-2.07122317832839));
#25832=CARTESIAN_POINT('Ctrl Pts',(-6.769193390288,63.8448964529897,-3.66764005408777));
#25833=CARTESIAN_POINT('Ctrl Pts',(-7.26328380690333,63.7938089106022,-4.57617640678974));
#25834=CARTESIAN_POINT('Ctrl Pts',(-7.88256773057987,63.6870539327616,-6.54288354813264));
#25835=CARTESIAN_POINT('Ctrl Pts',(-7.99716772080512,63.6358723480358,-7.58379124967247));
#25836=CARTESIAN_POINT('Ctrl Pts',(-7.81943328777949,63.5312019187572,-9.65163458704426));
#25837=CARTESIAN_POINT('Ctrl Pts',(-7.52843743600606,63.4769603244062,-10.6585944507657));
#25838=CARTESIAN_POINT('Ctrl Pts',(-6.58196697346264,63.3716088285271,-12.490491058003));
#25839=CARTESIAN_POINT('Ctrl Pts',(-5.94050296954954,63.3221206920407,-13.3005597608152));
#25840=CARTESIAN_POINT('Ctrl Pts',(-4.36290956784409,63.2149223220041,-14.6515336183974));
#25841=CARTESIAN_POINT('Ctrl Pts',(-3.43460176955039,63.1603336837683,-15.1704922957151));
#25842=CARTESIAN_POINT('Ctrl Pts',(-1.64512523130868,63.0676798002179,-15.7465518933932));
#25843=CARTESIAN_POINT('Ctrl Pts',(-0.824409094713655,63.0251855088854,
-15.875));
#25844=CARTESIAN_POINT('Ctrl Pts',(-2.73392419813945E-14,62.9825000069372,
-15.875));
#25845=CARTESIAN_POINT('Ctrl Pts',(1.2490009027033E-15,62.665,-15.875));
#25846=CARTESIAN_POINT('Ctrl Pts',(-0.10678118416443,62.6705288187308,-15.875));
#25847=CARTESIAN_POINT('Ctrl Pts',(-0.213647259459413,62.6760620328766,
-15.872845270232));
#25848=CARTESIAN_POINT('Ctrl Pts',(-1.34302158695393,62.7345377464097,-15.8272013626226));
#25849=CARTESIAN_POINT('Ctrl Pts',(-2.34792454259774,62.7845009481365,-15.5885368982462));
#25850=CARTESIAN_POINT('Ctrl Pts',(-4.22888299835772,62.8892664994659,-14.7350472466522));
#25851=CARTESIAN_POINT('Ctrl Pts',(-5.08391034054569,62.943749794255,-14.1216687243596));
#25852=CARTESIAN_POINT('Ctrl Pts',(-6.50106978542234,63.0492070983699,-12.6070847518793));
#25853=CARTESIAN_POINT('Ctrl Pts',(-7.05246541554818,63.0994197763401,-11.7232139155279));
#25854=CARTESIAN_POINT('Ctrl Pts',(-7.7843363065139,63.2059100881859,-9.79846319705741));
#25855=CARTESIAN_POINT('Ctrl Pts',(-7.95956486650432,63.2583279998295,-8.77658404257087));
#25856=CARTESIAN_POINT('Ctrl Pts',(-7.91042328869039,63.3614302547978,-6.69880402378148));
#25857=CARTESIAN_POINT('Ctrl Pts',(-7.67700460042873,63.4161624749171,-5.66317283210756));
#25858=CARTESIAN_POINT('Ctrl Pts',(-6.83110447614055,63.523052036865,-3.7673646936249));
#25859=CARTESIAN_POINT('Ctrl Pts',(-6.23626917479286,63.5724360057793,-2.9212286952175));
#25860=CARTESIAN_POINT('Ctrl Pts',(-4.75000240174356,63.6781179028192,-1.49438308178774));
#25861=CARTESIAN_POINT('Ctrl Pts',(-3.86977713807099,63.7321572644408,-0.93027336542813));
#25862=CARTESIAN_POINT('Ctrl Pts',(-1.93699135180268,63.8362615476154,-0.169845992183665));
#25863=CARTESIAN_POINT('Ctrl Pts',(-0.902252022585847,63.8882840179527,
0.0170235810373091));
#25864=CARTESIAN_POINT('Ctrl Pts',(1.16254452587274,63.995193169801,-0.0191477078170207));
#25865=CARTESIAN_POINT('Ctrl Pts',(2.17298276010862,64.0456038399461,-0.234906896833842));
#25866=CARTESIAN_POINT('Ctrl Pts',(4.07531544991997,64.1499877049775,-1.04643591649846));
#25867=CARTESIAN_POINT('Ctrl Pts',(4.94578121005329,64.2045735311781,-1.6419342765105));
#25868=CARTESIAN_POINT('Ctrl Pts',(6.3956331167362,64.3104423616632,-3.1250429491433));
#25869=CARTESIAN_POINT('Ctrl Pts',(6.96524562977749,64.3602669442802,-3.99425454748881));
#25870=CARTESIAN_POINT('Ctrl Pts',(7.74066191783563,64.4665897807739,-5.90145550622931));
#25871=CARTESIAN_POINT('Ctrl Pts',(7.93913616305028,64.5199274320883,-6.92118389939431));
#25872=CARTESIAN_POINT('Ctrl Pts',(7.93580414760589,64.6225360324781,-9.00382346629569));
#25873=CARTESIAN_POINT('Ctrl Pts',(7.72434917474791,64.6772676622739,-10.0465791137209));
#25874=CARTESIAN_POINT('Ctrl Pts',(6.91824317872534,64.7844469600654,-11.9612009534146));
#25875=CARTESIAN_POINT('Ctrl Pts',(6.342091661726,64.8339051380756,-12.8191145522525));
#25876=CARTESIAN_POINT('Ctrl Pts',(4.88592030297376,64.9393173518797,-14.2785216455929));
#25877=CARTESIAN_POINT('Ctrl Pts',(4.01594808771533,64.9935261647386,-14.8623113341349));
#25878=CARTESIAN_POINT('Ctrl Pts',(2.10051462720201,65.0981007259448,-15.6620746218592));
#25879=CARTESIAN_POINT('Ctrl Pts',(1.07350198982203,65.1494171933907,-15.8702705442612));
#25880=CARTESIAN_POINT('Ctrl Pts',(0.0237043088711802,65.2037726599216,
-15.8749734566493));
#25881=CARTESIAN_POINT('Ctrl Pts',(0.0118515279162405,65.2043863624004,
-15.8749999999751));
#25882=CARTESIAN_POINT('Ctrl Pts',(1.67328657821244E-8,65.2049999991336,
-15.875));
#25883=CARTESIAN_POINT('Origin',(0.,-18.001,-7.93750000000004));
#25884=CARTESIAN_POINT('',(-9.12495460877611E-15,68.0625000069372,-15.875));
#25885=CARTESIAN_POINT('',(-1.87381047919305E-15,67.745,-15.875));
#25886=CARTESIAN_POINT('',(-9.72063396823211E-16,-18.001,-15.875));
#25887=CARTESIAN_POINT('Ctrl Pts',(-1.80411241501588E-14,68.0625000069372,
-15.875));
#25888=CARTESIAN_POINT('Ctrl Pts',(0.433688074095033,68.0400449015164,-15.875));
#25889=CARTESIAN_POINT('Ctrl Pts',(0.867646658930349,68.0175757898376,-15.8394569362102));
#25890=CARTESIAN_POINT('Ctrl Pts',(2.30744279971092,67.9430273388727,-15.6008963918652));
#25891=CARTESIAN_POINT('Ctrl Pts',(3.27552241898614,67.8935284260736,-15.2397501722207));
#25892=CARTESIAN_POINT('Ctrl Pts',(5.04600416610042,67.7863355943929,-14.1544463263054));
#25893=CARTESIAN_POINT('Ctrl Pts',(5.82518660607671,67.7318161969776,-13.4310630253555));
#25894=CARTESIAN_POINT('Ctrl Pts',(7.04237597061802,67.6291349825518,-11.7413550114365));
#25895=CARTESIAN_POINT('Ctrl Pts',(7.47592761909007,67.5756772732154,-10.7966330639291));
#25896=CARTESIAN_POINT('Ctrl Pts',(7.95782719209122,67.4694103717858,-8.79519864354836));
#25897=CARTESIAN_POINT('Ctrl Pts',(8.00189302295181,67.4196664096423,-7.75749681019158));
#25898=CARTESIAN_POINT('Ctrl Pts',(7.68906167925432,67.3136957724166,-5.70714517179668));
#25899=CARTESIAN_POINT('Ctrl Pts',(7.32892036503718,67.2590877202392,-4.71521019537982));
#25900=CARTESIAN_POINT('Ctrl Pts',(6.25607408933573,67.1548080819376,-2.94614230636956));
#25901=CARTESIAN_POINT('Ctrl Pts',(5.56078284775951,67.1042605791076,-2.18164713990146));
#25902=CARTESIAN_POINT('Ctrl Pts',(3.9048740859986,66.9973843651778,-0.949050596015295));
#25903=CARTESIAN_POINT('Ctrl Pts',(2.95619879843677,66.9455633712056,-0.497926058022581));
#25904=CARTESIAN_POINT('Ctrl Pts',(0.943071919052903,66.8413295243412,0.0116014630028445));
#25905=CARTESIAN_POINT('Ctrl Pts',(-0.101548405123127,66.7872421262658,
0.0666974313818716));
#25906=CARTESIAN_POINT('Ctrl Pts',(-2.14129294923519,66.6816300942421,-0.225927537827141));
#25907=CARTESIAN_POINT('Ctrl Pts',(-3.11766848499563,66.6322370806252,-0.566366463438777));
#25908=CARTESIAN_POINT('Ctrl Pts',(-4.91070117103948,66.5252668143996,-1.61331850571048));
#25909=CARTESIAN_POINT('Ctrl Pts',(-5.70465454808869,66.4705322689865,-2.31901377130391));
#25910=CARTESIAN_POINT('Ctrl Pts',(-6.95653847210559,66.3675598567049,-3.97943092341129));
#25911=CARTESIAN_POINT('Ctrl Pts',(-7.41003568161736,66.314906435902,-4.91235547833897));
#25912=CARTESIAN_POINT('Ctrl Pts',(-7.93705275327936,66.2084599009704,-6.90277823869244));
#25913=CARTESIAN_POINT('Ctrl Pts',(-8.00421592914212,66.1583631665413,-7.94164872216537));
#25914=CARTESIAN_POINT('Ctrl Pts',(-7.73591046461968,66.0527927576801,-9.99834006578266));
#25915=CARTESIAN_POINT('Ctrl Pts',(-7.39854633601598,65.9982793995688,-10.9957528004814));
#25916=CARTESIAN_POINT('Ctrl Pts',(-6.36722845879569,65.8936128524359,-12.7861712278592));
#25917=CARTESIAN_POINT('Ctrl Pts',(-5.68972391939372,65.8435423580799,-13.5658425210553));
#25918=CARTESIAN_POINT('Ctrl Pts',(-4.05955075944524,65.7365452666697,-14.8378328977529));
#25919=CARTESIAN_POINT('Ctrl Pts',(-3.11747828465378,65.683913953298,-15.3114860958317));
#25920=CARTESIAN_POINT('Ctrl Pts',(-1.4218679409655,65.5961201879295,-15.7792475927008));
#25921=CARTESIAN_POINT('Ctrl Pts',(-0.711800218347542,65.5593549492248,
-15.875));
#25922=CARTESIAN_POINT('Ctrl Pts',(1.20736753927986E-14,65.5225000069373,
-15.875));
#25923=CARTESIAN_POINT('Ctrl Pts',(1.67328666200728E-8,65.2049999991336,
-15.875));
#25924=CARTESIAN_POINT('Ctrl Pts',(-1.01235319717274,65.2574167002126,-15.8750000021342));
#25925=CARTESIAN_POINT('Ctrl Pts',(-2.01552439406243,65.3077533698532,-15.6813225282047));
#25926=CARTESIAN_POINT('Ctrl Pts',(-3.92677583366418,65.4111468805206,-14.9146103708258));
#25927=CARTESIAN_POINT('Ctrl Pts',(-4.81164344365151,65.4658058045133,-14.3365325951033));
#25928=CARTESIAN_POINT('Ctrl Pts',(-6.29233096466331,65.572040262209,-12.8838516545358));
#25929=CARTESIAN_POINT('Ctrl Pts',(-6.87914313474992,65.6216079664635,-12.0286110836041));
#25930=CARTESIAN_POINT('Ctrl Pts',(-7.69561202403318,65.727740263692,-10.1386182960918));
#25931=CARTESIAN_POINT('Ctrl Pts',(-7.91621294150844,65.7813705506426,-9.12119984513197));
#25932=CARTESIAN_POINT('Ctrl Pts',(-7.95620178249735,65.8844525831829,-7.04085658844557));
#25933=CARTESIAN_POINT('Ctrl Pts',(-7.76810461068915,65.9382221328197,-5.9978958009839));
#25934=CARTESIAN_POINT('Ctrl Pts',(-7.00660948082297,66.0453484056575,-4.06985581544896));
#25935=CARTESIAN_POINT('Ctrl Pts',(-6.45012112291448,66.0950046272612,-3.19965036604002));
#25936=CARTESIAN_POINT('Ctrl Pts',(-5.02596225176608,66.2001024717331,-1.7065114721996));
#25937=CARTESIAN_POINT('Ctrl Pts',(-4.16719289431384,66.2544637285815,-1.10229333846056));
#25938=CARTESIAN_POINT('Ctrl Pts',(-2.27042579493747,66.3595025670694,-0.261582695513758));
#25939=CARTESIAN_POINT('Ctrl Pts',(-1.25155999052137,66.4101978686835,-0.0312918302746155));
#25940=CARTESIAN_POINT('Ctrl Pts',(0.80802194173164,66.5168370228915,0.0250971154595979));
#25941=CARTESIAN_POINT('Ctrl Pts',(1.8290296902527,66.568484833832,-0.145818051007626));
#25942=CARTESIAN_POINT('Ctrl Pts',(3.77137211901572,66.6720334348404,-0.874833121602433));
#25943=CARTESIAN_POINT('Ctrl Pts',(4.67076854080747,66.7267423476151,-1.43455624455437));
#25944=CARTESIAN_POINT('Ctrl Pts',(6.18293899381204,66.8333267158754,-2.85540207612083));
#25945=CARTESIAN_POINT('Ctrl Pts',(6.78734513232732,66.8827447931084,-3.69622717082995));
#25946=CARTESIAN_POINT('Ctrl Pts',(7.64579728348592,66.9886599454099,-5.568169103159));
#25947=CARTESIAN_POINT('Ctrl Pts',(7.88902800709171,67.0425126204529,-6.58275082634948));
#25948=CARTESIAN_POINT('Ctrl Pts',(7.97336727667615,67.1461349622059,-8.65965607432826));
#25949=CARTESIAN_POINT('Ctrl Pts',(7.80912783457669,67.1989485584348,-9.70211051669221));
#25950=CARTESIAN_POINT('Ctrl Pts',(7.09370088741321,67.305969091227,-11.6429716481885));
#25951=CARTESIAN_POINT('Ctrl Pts',(6.5574081612622,67.3559559570471,-12.5256946078923));
#25952=CARTESIAN_POINT('Ctrl Pts',(5.16646318780928,67.4606991356996,-14.052894831553));
#25953=CARTESIAN_POINT('Ctrl Pts',(4.31962152002127,67.5151894545751,-14.6777707668926));
#25954=CARTESIAN_POINT('Ctrl Pts',(2.44243730461787,67.6206727411499,-15.5600386989748));
#25955=CARTESIAN_POINT('Ctrl Pts',(1.43194224651504,67.6708582008068,-15.8126574641793));
#25956=CARTESIAN_POINT('Ctrl Pts',(0.267589531288932,67.7311449933869,-15.8716202456688));
#25957=CARTESIAN_POINT('Ctrl Pts',(0.133733921363328,67.7380756470332,-15.875));
#25958=CARTESIAN_POINT('Ctrl Pts',(-1.58900670399476E-14,67.745,-15.875));
#25959=CARTESIAN_POINT('Origin',(0.,-18.001,-7.93750000000004));
#25960=CARTESIAN_POINT('',(-3.57703071997799E-14,70.6025000069373,-15.875));
#25961=CARTESIAN_POINT('',(-3.747311833248E-15,70.2850000000001,-15.875));
#25962=CARTESIAN_POINT('',(-9.72063396823211E-16,-18.001,-15.875));
#25963=CARTESIAN_POINT('Ctrl Pts',(-7.34134975033385E-14,70.6025000069373,
-15.875));
#25964=CARTESIAN_POINT('Ctrl Pts',(0.55468147166431,70.5737802157667,-15.875));
#25965=CARTESIAN_POINT('Ctrl Pts',(1.10917310827725,70.5450702537025,-15.8168567412127));
#25966=CARTESIAN_POINT('Ctrl Pts',(2.65519167658246,70.4650219147983,-15.4874140063886));
#25967=CARTESIAN_POINT('Ctrl Pts',(3.60546903429097,70.414923428072,-15.0825560851003));
#25968=CARTESIAN_POINT('Ctrl Pts',(5.31698959833044,70.3079339887368,-13.922782238041));
#25969=CARTESIAN_POINT('Ctrl Pts',(6.05728423695684,70.2553602068774,-13.1722964105403));
#25970=CARTESIAN_POINT('Ctrl Pts',(7.19946640267268,70.1515957220018,-11.4362185862728));
#25971=CARTESIAN_POINT('Ctrl Pts',(7.59355757884135,70.0976867479508,-10.4695111044688));
#25972=CARTESIAN_POINT('Ctrl Pts',(7.98719067824395,69.9918362508845,-8.44785329199879));
#25973=CARTESIAN_POINT('Ctrl Pts',(7.98625615382667,69.9424387179082,-7.41272651414423));
#25974=CARTESIAN_POINT('Ctrl Pts',(7.5859664650825,69.8357635883035,-5.37648534904374));
#25975=CARTESIAN_POINT('Ctrl Pts',(7.18118656516031,69.7810455393853,-4.3968205716101));
#25976=CARTESIAN_POINT('Ctrl Pts',(6.02712129486966,69.6776229024158,-2.67154587193301));
#25977=CARTESIAN_POINT('Ctrl Pts',(5.29670537170189,69.6257643506818,-1.93736593228556));
#25978=CARTESIAN_POINT('Ctrl Pts',(3.59037049556738,69.5191669285006,-0.783335574039568));
#25979=CARTESIAN_POINT('Ctrl Pts',(2.62899582321277,69.4686217540813,-0.376995500569623));
#25980=CARTESIAN_POINT('Ctrl Pts',(0.597945629743748,69.3634598902127,0.0455639264374251));
#25981=CARTESIAN_POINT('Ctrl Pts',(-0.452688703198433,69.3090611042784,
0.0551154855814628));
#25982=CARTESIAN_POINT('Ctrl Pts',(-2.4807164905748,69.204055731795,-0.328479105333356));
#25983=CARTESIAN_POINT('Ctrl Pts',(-3.44000422234571,69.1543230279237,-0.711332810312225));
#25984=CARTESIAN_POINT('Ctrl Pts',(-5.18134004871023,69.0472238382526,-1.83367566723749));
#25985=CARTESIAN_POINT('Ctrl Pts',(-5.94127210539138,68.9937228453009,-2.57057409498428));
#25986=CARTESIAN_POINT('Ctrl Pts',(-7.12155151995333,68.8904927597585,-4.28342106841755));
#25987=CARTESIAN_POINT('Ctrl Pts',(-7.53576398510425,68.836800292985,-5.23919402969178));
#25988=CARTESIAN_POINT('Ctrl Pts',(-7.97417133547815,68.7307232145494,-7.25090510299311));
#25989=CARTESIAN_POINT('Ctrl Pts',(-7.99602537296488,68.6812071389458,-8.28738315381936));
#25990=CARTESIAN_POINT('Ctrl Pts',(-7.64013578098366,68.5748760894848,-10.3310633838858));
#25991=CARTESIAN_POINT('Ctrl Pts',(-7.25799660543989,68.520201211879,-11.3172078780045));
#25992=CARTESIAN_POINT('Ctrl Pts',(-6.14510573557978,68.4163273726159,-13.0650237333758));
#25993=CARTESIAN_POINT('Ctrl Pts',(-5.43255623533737,68.365196845588,-13.8146819879853));
#25994=CARTESIAN_POINT('Ctrl Pts',(-3.75180666418746,68.2584510528248,-15.0088026868805));
#25995=CARTESIAN_POINT('Ctrl Pts',(-2.79683739267014,68.2073121017327,-15.4379700976919));
#25996=CARTESIAN_POINT('Ctrl Pts',(-1.1992115311013,68.1245916874823,-15.8069975347168));
#25997=CARTESIAN_POINT('Ctrl Pts',(-0.599864530783218,68.0935592453197,
-15.875));
#25998=CARTESIAN_POINT('Ctrl Pts',(-1.92901250528621E-14,68.0625000069372,
-15.875));
#25999=CARTESIAN_POINT('Ctrl Pts',(-2.05391259555654E-14,67.745,-15.875));
#26000=CARTESIAN_POINT('Ctrl Pts',(-0.891384039551465,67.7911532695368,
-15.875));
#26001=CARTESIAN_POINT('Ctrl Pts',(-1.7773915122855,67.8364542179145,-15.7248304672442));
#26002=CARTESIAN_POINT('Ctrl Pts',(-3.61297397000325,67.9328823135545,-15.0828398530554));
#26003=CARTESIAN_POINT('Ctrl Pts',(-4.52663207304087,67.9876152259936,-14.5419576646853));
#26004=CARTESIAN_POINT('Ctrl Pts',(-6.07012261666185,68.0945233969593,-13.1535806673219));
#26005=CARTESIAN_POINT('Ctrl Pts',(-6.69207962534341,68.1439087193146,-12.3272575904096));
#26006=CARTESIAN_POINT('Ctrl Pts',(-7.59229918481167,68.2495748379419,-10.4739439583062));
#26007=CARTESIAN_POINT('Ctrl Pts',(-7.85814601219587,68.3036253291705,-9.46269350425099));
#26008=CARTESIAN_POINT('Ctrl Pts',(-7.98673368238065,68.4077593993229,-7.38977351839877));
#26009=CARTESIAN_POINT('Ctrl Pts',(-7.84611012968646,68.459735104669,-6.34797524464098));
#26010=CARTESIAN_POINT('Ctrl Pts',(-7.17637265411212,68.5666368012141,-4.39468196874761));
#26011=CARTESIAN_POINT('Ctrl Pts',(-6.6601250121187,68.6170780294673,-3.49964044689932));
#26012=CARTESIAN_POINT('Ctrl Pts',(-5.30245198461667,68.7214382324708,-1.93922920673743));
#26013=CARTESIAN_POINT('Ctrl Pts',(-4.46785065444924,68.7760293035196,-1.2941953574911));
#26014=CARTESIAN_POINT('Ctrl Pts',(-2.61049320716362,68.8819216103495,-0.371198553129155));
#26015=CARTESIAN_POINT('Ctrl Pts',(-1.60829789989605,68.9317270186858,-0.0967770647009433));
#26016=CARTESIAN_POINT('Ctrl Pts',(0.444976416468158,69.0380395829131,0.0540955344220655));
#26017=CARTESIAN_POINT('Ctrl Pts',(1.47642819725269,69.091435194494,-0.0709120054369154));
#26018=CARTESIAN_POINT('Ctrl Pts',(3.45719629546723,69.1940137749849,-0.715165556475455));
#26019=CARTESIAN_POINT('Ctrl Pts',(4.3843592522318,69.2487445829194,-1.23739075811436));
#26020=CARTESIAN_POINT('Ctrl Pts',(5.95793719659881,69.3559400751924,-2.59379686046367));
#26021=CARTESIAN_POINT('Ctrl Pts',(6.59681536733345,69.4054060723789,-3.40602830215141));
#26022=CARTESIAN_POINT('Ctrl Pts',(7.53716663208879,69.5108015548906,-5.24080641497974));
#26023=CARTESIAN_POINT('Ctrl Pts',(7.82482937244818,69.56501957705,-6.24837058041258));
#26024=CARTESIAN_POINT('Ctrl Pts',(7.99605244940215,69.6696208830364,-8.31692586567543));
#26025=CARTESIAN_POINT('Ctrl Pts',(7.87801665925337,69.7208993945324,-9.35796079940542));
#26026=CARTESIAN_POINT('Ctrl Pts',(7.25206501843802,69.8276746720165,-11.3229137027457));
#26027=CARTESIAN_POINT('Ctrl Pts',(6.75504492769195,69.8786681783344,-12.2296730844804));
#26028=CARTESIAN_POINT('Ctrl Pts',(5.42954504333603,69.9826329032435,-13.821372161045));
#26029=CARTESIAN_POINT('Ctrl Pts',(4.60703967623432,70.0372953340462,-14.4853994278399));
#26030=CARTESIAN_POINT('Ctrl Pts',(2.76904453052918,70.1435502549678,-15.4469609983921));
#26031=CARTESIAN_POINT('Ctrl Pts',(1.77479255518857,70.1931064103273,-15.7419667278455));
#26032=CARTESIAN_POINT('Ctrl Pts',(0.501572705197605,70.2590300260852,-15.8631284936286));
#26033=CARTESIAN_POINT('Ctrl Pts',(0.250642322080538,70.2720224705234,-15.875));
#26034=CARTESIAN_POINT('Ctrl Pts',(-5.20417042793042E-15,70.2850000000001,
-15.875));
#26035=CARTESIAN_POINT('Origin',(0.,-18.001,-7.93750000000004));
#26036=CARTESIAN_POINT('',(-9.72063396823211E-16,73.0000000000001,-15.875));
#26037=CARTESIAN_POINT('',(1.12292432555688E-15,72.825,-15.875));
#26038=CARTESIAN_POINT('',(-9.72063396823211E-16,-18.001,-15.875));
#26039=CARTESIAN_POINT('',(2.74837297199504,73.,-15.3839993290006));
#26040=CARTESIAN_POINT('Origin',(0.,73.,-7.93749999999999));
#26041=CARTESIAN_POINT('Ctrl Pts',(2.74837297199475,73.0000000000001,-15.3839993290008));
#26042=CARTESIAN_POINT('Ctrl Pts',(3.59437464131025,72.9550594340577,-15.0717548743275));
#26043=CARTESIAN_POINT('Ctrl Pts',(4.38096265156832,72.9082896699512,-14.6176303844275));
#26044=CARTESIAN_POINT('Ctrl Pts',(5.76270270874511,72.815450657477,-13.4689100881607));
#26045=CARTESIAN_POINT('Ctrl Pts',(6.34930118539488,72.7715825043545,-12.7843132261676));
#26046=CARTESIAN_POINT('Ctrl Pts',(7.3429699107917,72.6739979374842,-11.1254790275496));
#26047=CARTESIAN_POINT('Ctrl Pts',(7.69663294708784,72.6197352866454,-10.1384533621628));
#26048=CARTESIAN_POINT('Ctrl Pts',(8.00161174031953,72.5144245725012,-8.09895165090422));
#26049=CARTESIAN_POINT('Ctrl Pts',(7.95572988529432,72.4649139308815,-7.06676082021326));
#26050=CARTESIAN_POINT('Ctrl Pts',(7.46768900153107,72.357726908696,-5.04863649787649));
#26051=CARTESIAN_POINT('Ctrl Pts',(7.01922926841232,72.3032788768853,-4.08499423286156));
#26052=CARTESIAN_POINT('Ctrl Pts',(5.78611525301393,72.200560231844,-2.4070808512331));
#26053=CARTESIAN_POINT('Ctrl Pts',(5.02049908302566,72.1470861581906,-1.70379959241594));
#26054=CARTESIAN_POINT('Ctrl Pts',(3.26437485118427,72.0408309468112,-0.629542832290954));
#26055=CARTESIAN_POINT('Ctrl Pts',(2.29069621884348,71.9911055858172,-0.268398105084747));
#26056=CARTESIAN_POINT('Ctrl Pts',(0.243547344159033,71.8851101791205,0.064821270957295));
#26057=CARTESIAN_POINT('Ctrl Pts',(-0.81122908592498,71.8304969274595,0.0273254603393398));
#26058=CARTESIAN_POINT('Ctrl Pts',(-2.82473809981346,71.7262432947834,-0.449305473372096));
#26059=CARTESIAN_POINT('Ctrl Pts',(-3.76609380580235,71.6756607697004,-0.875717113837374));
#26060=CARTESIAN_POINT('Ctrl Pts',(-5.44815635567005,71.5687928129177,-2.0720447416791));
#26061=CARTESIAN_POINT('Ctrl Pts',(-6.16910522104993,71.5170203032762,-2.83573318331477));
#26062=CARTESIAN_POINT('Ctrl Pts',(-7.27331242840743,71.4127547779465,-4.59432468902859));
#26063=CARTESIAN_POINT('Ctrl Pts',(-7.64719722588607,71.3586557850724,-5.571456424903));
#26064=CARTESIAN_POINT('Ctrl Pts',(-7.99631495195053,71.2530613299722,-7.60237859159013));
#26065=CARTESIAN_POINT('Ctrl Pts',(-7.97278718391001,71.203664836868,-8.63607257488857));
#26066=CARTESIAN_POINT('Ctrl Pts',(-7.52827571758297,71.0966749348865,-10.6643374475176));
#26067=CARTESIAN_POINT('Ctrl Pts',(-7.10100257500505,71.041940096802,-11.6370346730576));
#26068=CARTESIAN_POINT('Ctrl Pts',(-5.90604744264877,70.9390001163971,-13.3392219121527));
#26069=CARTESIAN_POINT('Ctrl Pts',(-5.15775556231888,70.8862871268732,-14.0577905255233));
#26070=CARTESIAN_POINT('Ctrl Pts',(-3.42595037494629,70.7798515578262,-15.1714458061015));
#26071=CARTESIAN_POINT('Ctrl Pts',(-2.45827221640794,70.7297821829296,-15.554851267113));
#26072=CARTESIAN_POINT('Ctrl Pts',(-0.966818965162028,70.6525590772289,
-15.8308526453184));
#26073=CARTESIAN_POINT('Ctrl Pts',(-0.483337411686185,70.6275258104618,
-15.875));
#26074=CARTESIAN_POINT('Ctrl Pts',(-7.39686090156511E-14,70.6025000069373,
-15.875));
#26075=CARTESIAN_POINT('Ctrl Pts',(-5.13478148889135E-15,70.2850000000001,
-15.875));
#26076=CARTESIAN_POINT('Ctrl Pts',(-0.777177421330428,70.3252399834562,
-15.875));
#26077=CARTESIAN_POINT('Ctrl Pts',(-1.55158524899007,70.365336565418,-15.7608488491832));
#26078=CARTESIAN_POINT('Ctrl Pts',(-3.30231265475548,70.4559841317402,-15.2312860424146));
#26079=CARTESIAN_POINT('Ctrl Pts',(-4.23649762123155,70.5096965065944,-14.7313986180527));
#26080=CARTESIAN_POINT('Ctrl Pts',(-5.83636493185836,70.6168171685367,-13.4136355136902));
#26081=CARTESIAN_POINT('Ctrl Pts',(-6.49304723000878,70.6664887070802,-12.6163446127004));
#26082=CARTESIAN_POINT('Ctrl Pts',(-7.47544971294546,70.7715672857524,-10.8016652876116));
#26083=CARTESIAN_POINT('Ctrl Pts',(-7.78604964647708,70.8259366083522,-9.79848133719328));
#26084=CARTESIAN_POINT('Ctrl Pts',(-8.00207469181669,70.9310015342891,-7.73506814054177));
#26085=CARTESIAN_POINT('Ctrl Pts',(-7.90760817690709,70.9816644604433,-6.69496258235393));
#26086=CARTESIAN_POINT('Ctrl Pts',(-7.32743704232001,71.0882948993028,-4.71807599845438));
#26087=CARTESIAN_POINT('Ctrl Pts',(-6.8505419701571,71.1399863614486,-3.79915534071941));
#26088=CARTESIAN_POINT('Ctrl Pts',(-5.55895784608872,71.2435085992257,-2.1753145531283));
#26089=CARTESIAN_POINT('Ctrl Pts',(-4.74946229624585,71.2982196009796,-1.49178485530757));
#26090=CARTESIAN_POINT('Ctrl Pts',(-2.93207164078339,71.4048232854104,-0.490403897681004));
#26091=CARTESIAN_POINT('Ctrl Pts',(-1.94610588454118,71.4542363050593,-0.174191892264601));
#26092=CARTESIAN_POINT('Ctrl Pts',(0.0992332456347186,71.5601380084559,
0.0663966627234519));
#26093=CARTESIAN_POINT('Ctrl Pts',(1.13955264224962,71.614002717028,-0.0145088029096499));
#26094=CARTESIAN_POINT('Ctrl Pts',(3.14145196896345,71.7176552339138,-0.573609583815303));
#26095=CARTESIAN_POINT('Ctrl Pts',(4.08252146116871,71.7704174893548,-1.05063963155032));
#26096=CARTESIAN_POINT('Ctrl Pts',(5.70881450440919,71.8774315400999,-2.32852778385979));
#26097=CARTESIAN_POINT('Ctrl Pts',(6.38364567440301,71.9274412025371,-3.11047008078335));
#26098=CARTESIAN_POINT('Ctrl Pts',(7.40870062480463,72.0321631297841,-4.90404808705329));
#26099=CARTESIAN_POINT('Ctrl Pts',(7.74263369637828,72.0866599944385,-5.90224069919674));
#26100=CARTESIAN_POINT('Ctrl Pts',(8.00423542243036,72.1921677292453,-7.95983746731116));
#26101=CARTESIAN_POINT('Ctrl Pts',(7.93358266755552,72.242327892559,-8.99887486620816));
#26102=CARTESIAN_POINT('Ctrl Pts',(7.39976478850669,72.3487988845475,-10.9875845715094));
#26103=CARTESIAN_POINT('Ctrl Pts',(6.9432719145105,72.4013202714971,-11.9187244089226));
#26104=CARTESIAN_POINT('Ctrl Pts',(5.68629056082371,72.5043651493195,-13.5745066378289));
#26105=CARTESIAN_POINT('Ctrl Pts',(4.89032358003968,72.5590986277707,-14.2773953572043));
#26106=CARTESIAN_POINT('Ctrl Pts',(3.09414933749014,72.6660242711992,-15.3185571933526));
#26107=CARTESIAN_POINT('Ctrl Pts',(2.11654896885027,72.7154112585455,-15.65591967121));
#26108=CARTESIAN_POINT('Ctrl Pts',(0.736312332434618,72.786875891833,-15.8493886519877));
#26109=CARTESIAN_POINT('Ctrl Pts',(0.368139781712966,72.8059387942585,-15.875));
#26110=CARTESIAN_POINT('Ctrl Pts',(-6.24500451351651E-16,72.825,-15.875));
#26111=CARTESIAN_POINT('Origin',(0.,0.,-3.));
#26112=CARTESIAN_POINT('',(7.42417289639114,16.3976113139839,-3.));
#26113=CARTESIAN_POINT('',(-7.42417289639223,16.3976113139834,-3.));
#26114=CARTESIAN_POINT('Origin',(0.,0.,-3.));
#26115=CARTESIAN_POINT('',(6.18681074697836,13.6646760949931,0.));
#26116=CARTESIAN_POINT('Origin',(6.18681074698069,13.6646760949919,-2.99999999999878));
#26117=CARTESIAN_POINT('',(-6.18681074697897,13.6646760949927,0.));
#26118=CARTESIAN_POINT('Origin',(0.,0.,0.));
#26119=CARTESIAN_POINT('Origin',(-6.18681074697897,13.6646760949927,-3.));
#26120=CARTESIAN_POINT('Origin',(0.,1.11022302462516E-13,-12.875));
#26121=CARTESIAN_POINT('',(6.18681074697913,13.6646760949928,-15.875));
#26122=CARTESIAN_POINT('',(-6.18681074697824,13.6646760949932,-15.875));
#26123=CARTESIAN_POINT('Origin',(0.,1.11022302462516E-13,-15.875));
#26124=CARTESIAN_POINT('',(7.42417289637494,16.3976113139913,-12.8749999999944));
#26125=CARTESIAN_POINT('Origin',(6.18681074697913,13.6646760949928,-12.875));
#26126=CARTESIAN_POINT('',(-7.42417289638977,16.3976113139846,-12.875));
#26127=CARTESIAN_POINT('Origin',(0.,1.11022302462516E-13,-12.875));
#26128=CARTESIAN_POINT('Origin',(-6.18681074697824,13.6646760949932,-12.875));
#26129=CARTESIAN_POINT('Origin',(0.,1.11022302462516E-13,-15.875));
#26130=CARTESIAN_POINT('',(-9.,1.09920120343283E-13,-15.875));
#26131=CARTESIAN_POINT('Origin',(0.,1.11022302462516E-13,-15.875));
#26132=CARTESIAN_POINT('',(-9.,1.09920120343283E-13,0.));
#26133=CARTESIAN_POINT('',(-9.,1.09920120343283E-13,-15.875));
#26134=CARTESIAN_POINT('Origin',(0.,0.,0.));
#26135=CARTESIAN_POINT('Origin',(0.,1.11022302462516E-13,-15.875));
#26136=CARTESIAN_POINT('Ctrl Pts',(7.42417484634227,16.3976156207155,-12.87499999998));
#26137=CARTESIAN_POINT('Ctrl Pts',(7.49425297313204,16.3658856681913,-12.751333844329));
#26138=CARTESIAN_POINT('Ctrl Pts',(7.56155134995267,16.3348713727113,-12.6261535808136));
#26139=CARTESIAN_POINT('Ctrl Pts',(7.62612254669854,16.3046697269754,-12.4994671770732));
#26140=CARTESIAN_POINT('Ctrl Pts',(7.75422681491928,16.2447519939762,-12.2481311346493));
#26141=CARTESIAN_POINT('Ctrl Pts',(7.8715970357136,16.1880292793325,-11.9908686844778));
#26142=CARTESIAN_POINT('Ctrl Pts',(7.97820798185054,16.1353117293752,-11.7274704800121));
#26143=CARTESIAN_POINT('Ctrl Pts',(8.01721016407619,16.1160257220333,-11.6311097859114));
#26144=CARTESIAN_POINT('Ctrl Pts',(8.05478002264463,16.0972716532196,-11.533899256748));
#26145=CARTESIAN_POINT('Ctrl Pts',(8.09090985732795,16.0790913201412,-11.4358370389061));
#26146=CARTESIAN_POINT('Ctrl Pts',(8.16205634437451,16.0432908011739,-11.2427339601735));
#26147=CARTESIAN_POINT('Ctrl Pts',(8.22753637682579,16.0097534434489,-11.0461762836229));
#26148=CARTESIAN_POINT('Ctrl Pts',(8.28688853410253,15.9789727293006,-10.8478320212478));
#26149=CARTESIAN_POINT('Ctrl Pts',(8.32131121783912,15.9611207280098,-10.7327975873204));
#26150=CARTESIAN_POINT('Ctrl Pts',(8.35367325807109,15.9441955973044,-10.6171617077227));
#26151=CARTESIAN_POINT('Ctrl Pts',(8.38388984996585,15.928290085497,-10.5012445343995));
#26152=CARTESIAN_POINT('Ctrl Pts',(8.40113973300348,15.9192100337397,-10.4350703712496));
#26153=CARTESIAN_POINT('Ctrl Pts',(8.41770873842301,15.9104526090396,-10.3687432766716));
#26154=CARTESIAN_POINT('Ctrl Pts',(8.43357670502026,15.9020371015176,-10.3023247062374));
#26155=CARTESIAN_POINT('Ctrl Pts',(8.48142109323413,15.8766630369558,-10.102062382203));
#26156=CARTESIAN_POINT('Ctrl Pts',(8.523181690265,15.8542538078078,-9.90026706475298));
#26157=CARTESIAN_POINT('Ctrl Pts',(8.55878117848867,15.8350118244306,-9.69708852759311));
#26158=CARTESIAN_POINT('Ctrl Pts',(8.58582632375289,15.8203935739563,-9.54273257119468));
#26159=CARTESIAN_POINT('Ctrl Pts',(8.60931643956188,15.807602915796,-9.38757857490814));
#26160=CARTESIAN_POINT('Ctrl Pts',(8.62923459807846,15.7967193688509,-9.23169795700352));
#26161=CARTESIAN_POINT('Ctrl Pts',(8.63350792596552,15.794384365611,-9.19825465495383));
#26162=CARTESIAN_POINT('Ctrl Pts',(8.63761733451759,15.7921368728815,-9.16477496999481));
#26163=CARTESIAN_POINT('Ctrl Pts',(8.64156280552917,15.7899775895407,-9.13125885731573));
#26164=CARTESIAN_POINT('Ctrl Pts',(8.66292988244127,15.7782837833811,-8.94974913254405));
#26165=CARTESIAN_POINT('Ctrl Pts',(8.67947376513277,15.76917652596,-8.7671681095378));
#26166=CARTESIAN_POINT('Ctrl Pts',(8.69110604433138,15.762762383104,-8.58349117024342));
#26167=CARTESIAN_POINT('Ctrl Pts',(8.69218421804267,15.7621678684702,-8.56646650603642));
#26168=CARTESIAN_POINT('Ctrl Pts',(8.69322014673618,15.7615965171088,-8.54943307927023));
#26169=CARTESIAN_POINT('Ctrl Pts',(8.69421378566647,15.7610483994286,-8.53239054158288));
#26170=CARTESIAN_POINT('Ctrl Pts',(8.70328572291703,15.7560440773868,-8.37679193551244));
#26171=CARTESIAN_POINT('Ctrl Pts',(8.70880616372846,15.7529912511763,-8.2201332575878));
#26172=CARTESIAN_POINT('Ctrl Pts',(8.7107488498173,15.7519163037688,-8.06401072201215));
#26173=CARTESIAN_POINT('Ctrl Pts',(8.71131293962653,15.7516041756893,-8.01867806028393));
#26174=CARTESIAN_POINT('Ctrl Pts',(8.7115750876793,15.75145896852,-7.97339056290001));
#26175=CARTESIAN_POINT('Ctrl Pts',(8.71153392734093,15.7514817282356,-7.92818743022105));
#26176=CARTESIAN_POINT('Ctrl Pts',(8.71153351011403,15.7514819589423,-7.92772922304078));
#26177=CARTESIAN_POINT('Ctrl Pts',(8.71153306168016,15.7514822069308,-7.92727102504393));
#26178=CARTESIAN_POINT('Ctrl Pts',(8.71153258203798,15.7514824722023,-7.92681283627777));
#26179=CARTESIAN_POINT('Ctrl Pts',(8.71107948717309,15.7517330613572,-7.49398398029794));
#26180=CARTESIAN_POINT('Ctrl Pts',(8.68356072203589,15.7672456706329,-7.06559071877813));
#26181=CARTESIAN_POINT('Ctrl Pts',(8.62923684404765,15.7968989356927,-6.6415377335116));
#26182=CARTESIAN_POINT('Ctrl Pts',(8.58285778982776,15.8222154344209,-6.27950215865738));
#26183=CARTESIAN_POINT('Ctrl Pts',(8.51694114102254,15.8578381576886,-5.92062950477275));
#26184=CARTESIAN_POINT('Ctrl Pts',(8.43166005791346,15.903053441183,-5.56483757189164));
#26185=CARTESIAN_POINT('Ctrl Pts',(8.41576539569238,15.9114806519099,-5.49852518011659));
#26186=CARTESIAN_POINT('Ctrl Pts',(8.39916523028649,15.920251577545,-5.43228961453733));
#26187=CARTESIAN_POINT('Ctrl Pts',(8.38188287493475,15.9293455250075,-5.36619796746088));
#26188=CARTESIAN_POINT('Ctrl Pts',(8.33068896116534,15.9562836797177,-5.17042082872912));
#26189=CARTESIAN_POINT('Ctrl Pts',(8.27345820241746,15.9860834909743,-4.97580581749668));
#26190=CARTESIAN_POINT('Ctrl Pts',(8.21073783355088,16.0182329075637,-4.7840118256463));
#26191=CARTESIAN_POINT('Ctrl Pts',(8.17202073055818,16.0380786497962,-4.66561794706999));
#26192=CARTESIAN_POINT('Ctrl Pts',(8.13121144680357,16.0588197898457,-4.54829977429853));
#26193=CARTESIAN_POINT('Ctrl Pts',(8.08843644345115,16.0803356899397,-4.43245745460993));
#26194=CARTESIAN_POINT('Ctrl Pts',(8.05247016426092,16.0984267900955,-4.33505437137372));
#26195=CARTESIAN_POINT('Ctrl Pts',(8.01507184801902,16.1170887814765,-4.23846402227408));
#26196=CARTESIAN_POINT('Ctrl Pts',(7.97623595783032,16.1362866611022,-4.14266100529827));
#26197=CARTESIAN_POINT('Ctrl Pts',(7.86998595823516,16.1888095900877,-3.88055627522936));
#26198=CARTESIAN_POINT('Ctrl Pts',(7.75305710254994,16.2453053838483,-3.62448042379799));
#26199=CARTESIAN_POINT('Ctrl Pts',(7.62546188869204,16.3049787177716,-3.3742362248388));
#26200=CARTESIAN_POINT('Ctrl Pts',(7.561098085643,16.3350801815788,-3.2480036817129));
#26201=CARTESIAN_POINT('Ctrl Pts',(7.4940202195112,16.3659910561043,-3.12325541650477));
#26202=CARTESIAN_POINT('Ctrl Pts',(7.42417484827014,16.3976156249738,-3.00000000002115));
#26203=CARTESIAN_POINT('Ctrl Pts',(-7.42417484634355,16.3976156207149,-3.00000000002217));
#26204=CARTESIAN_POINT('Ctrl Pts',(-7.49425297313284,16.3658856681909,-3.12366615567247));
#26205=CARTESIAN_POINT('Ctrl Pts',(-7.56155134995302,16.3348713727112,-3.24884641918707));
#26206=CARTESIAN_POINT('Ctrl Pts',(-7.6261225466986,16.3046697269754,-3.37553282292674));
#26207=CARTESIAN_POINT('Ctrl Pts',(-7.75422681491959,16.2447519939761,-3.62686886535078));
#26208=CARTESIAN_POINT('Ctrl Pts',(-7.87159703571355,16.1880292793326,-3.88413131552216));
#26209=CARTESIAN_POINT('Ctrl Pts',(-7.97820798185047,16.1353117293752,-4.14752951998797));
#26210=CARTESIAN_POINT('Ctrl Pts',(-8.01721016407612,16.1160257220333,-4.24389021408868));
#26211=CARTESIAN_POINT('Ctrl Pts',(-8.05478002264456,16.0972716532196,-4.34110074325211));
#26212=CARTESIAN_POINT('Ctrl Pts',(-8.09090985732791,16.0790913201412,-4.43916296109398));
#26213=CARTESIAN_POINT('Ctrl Pts',(-8.1620563443761,16.0432908011731,-4.63226603983073));
#26214=CARTESIAN_POINT('Ctrl Pts',(-8.22753637682865,16.0097534434475,-4.82882371638596));
#26215=CARTESIAN_POINT('Ctrl Pts',(-8.28688853410642,15.9789727292985,-5.0271679787657));
#26216=CARTESIAN_POINT('Ctrl Pts',(-8.32131121784147,15.9611207280085,-5.14220241268877));
#26217=CARTESIAN_POINT('Ctrl Pts',(-8.35367325807209,15.9441955973039,-5.25783829228192));
#26218=CARTESIAN_POINT('Ctrl Pts',(-8.3838898499657,15.928290085497,-5.37375546560053));
#26219=CARTESIAN_POINT('Ctrl Pts',(-8.40113973300336,15.9192100337397,-5.43992962875046));
#26220=CARTESIAN_POINT('Ctrl Pts',(-8.41770873842293,15.9104526090397,-5.50625672332849));
#26221=CARTESIAN_POINT('Ctrl Pts',(-8.43357670502022,15.9020371015176,-5.57267529376267));
#26222=CARTESIAN_POINT('Ctrl Pts',(-8.48142109322884,15.8766630369586,-5.77293761777444));
#26223=CARTESIAN_POINT('Ctrl Pts',(-8.52318169025573,15.8542538078128,-5.97473293520173));
#26224=CARTESIAN_POINT('Ctrl Pts',(-8.55878117847675,15.835011824437,-6.17791147233861));
#26225=CARTESIAN_POINT('Ctrl Pts',(-8.58582632374597,15.8203935739601,-6.33226742875959));
#26226=CARTESIAN_POINT('Ctrl Pts',(-8.60931643955891,15.8076029157976,-6.48742142506895));
#26227=CARTESIAN_POINT('Ctrl Pts',(-8.62923459807841,15.796719368851,-6.64330204299652));
#26228=CARTESIAN_POINT('Ctrl Pts',(-8.63350792596547,15.794384365611,-6.67674534504622));
#26229=CARTESIAN_POINT('Ctrl Pts',(-8.63761733451752,15.7921368728815,-6.71022503000525));
#26230=CARTESIAN_POINT('Ctrl Pts',(-8.6415628055291,15.7899775895407,-6.74374114268435));
#26231=CARTESIAN_POINT('Ctrl Pts',(-8.66292988244114,15.7782837833812,-6.92525086745615));
#26232=CARTESIAN_POINT('Ctrl Pts',(-8.67947376513277,15.76917652596,-7.10783189046224));
#26233=CARTESIAN_POINT('Ctrl Pts',(-8.69110604433138,15.762762383104,-7.29150882975662));
#26234=CARTESIAN_POINT('Ctrl Pts',(-8.69218421804268,15.7621678684702,-7.30853349396362));
#26235=CARTESIAN_POINT('Ctrl Pts',(-8.69322014673619,15.7615965171088,-7.32556692072984));
#26236=CARTESIAN_POINT('Ctrl Pts',(-8.69421378566647,15.7610483994286,-7.3426094584172));
#26237=CARTESIAN_POINT('Ctrl Pts',(-8.70328572291651,15.7560440773871,-7.49820806447887));
#26238=CARTESIAN_POINT('Ctrl Pts',(-8.70880616372783,15.7529912511766,-7.65486674239446));
#26239=CARTESIAN_POINT('Ctrl Pts',(-8.71074884981696,15.751916303769,-7.81098927796124));
#26240=CARTESIAN_POINT('Ctrl Pts',(-8.71131293962642,15.7516041756893,-7.85632193969836));
#26241=CARTESIAN_POINT('Ctrl Pts',(-8.71157508767931,15.75145896852,-7.90160943709117));
#26242=CARTESIAN_POINT('Ctrl Pts',(-8.71153392734093,15.7514817282356,-7.94681256977899));
#26243=CARTESIAN_POINT('Ctrl Pts',(-8.71153351011403,15.7514819589423,-7.94727077695927));
#26244=CARTESIAN_POINT('Ctrl Pts',(-8.71153306168016,15.7514822069308,-7.94772897495614));
#26245=CARTESIAN_POINT('Ctrl Pts',(-8.71153258203797,15.7514824722023,-7.94818716372231));
#26246=CARTESIAN_POINT('Ctrl Pts',(-8.71107948717285,15.7517330613573,-8.38101601992454));
#26247=CARTESIAN_POINT('Ctrl Pts',(-8.68356072200785,15.7672456706487,-8.80940928166221));
#26248=CARTESIAN_POINT('Ctrl Pts',(-8.62923684396425,15.7968989357382,-9.23346226714217));
#26249=CARTESIAN_POINT('Ctrl Pts',(-8.58285778974884,15.8222154344636,-9.5954978417747));
#26250=CARTESIAN_POINT('Ctrl Pts',(-8.5169411409716,15.8578381577156,-9.95437049544148));
#26251=CARTESIAN_POINT('Ctrl Pts',(-8.43166005791337,15.9030534411831,-10.3101624281084));
#26252=CARTESIAN_POINT('Ctrl Pts',(-8.41576539569222,15.91148065191,-10.3764748198834));
#26253=CARTESIAN_POINT('Ctrl Pts',(-8.39916523028629,15.9202515775451,-10.4427103854627));
#26254=CARTESIAN_POINT('Ctrl Pts',(-8.38188287493453,15.9293455250077,-10.5088020325391));
#26255=CARTESIAN_POINT('Ctrl Pts',(-8.330688961164,15.9562836797184,-10.7045791712749));
#26256=CARTESIAN_POINT('Ctrl Pts',(-8.27345820241499,15.9860834909756,-10.8991941825113));
#26257=CARTESIAN_POINT('Ctrl Pts',(-8.21073783354696,16.0182329075658,-11.0909881743656));
#26258=CARTESIAN_POINT('Ctrl Pts',(-8.17202073055547,16.0380786497975,-11.2093820529379));
#26259=CARTESIAN_POINT('Ctrl Pts',(-8.13121144680218,16.0588197898464,-11.3267002257054));
#26260=CARTESIAN_POINT('Ctrl Pts',(-8.08843644345111,16.0803356899398,-11.4425425453902));
#26261=CARTESIAN_POINT('Ctrl Pts',(-8.05247016426082,16.0984267900955,-11.5399456286264));
#26262=CARTESIAN_POINT('Ctrl Pts',(-8.01507184801894,16.1170887814765,-11.636535977726));
#26263=CARTESIAN_POINT('Ctrl Pts',(-7.97623595783027,16.1362866611023,-11.7323389947018));
#26264=CARTESIAN_POINT('Ctrl Pts',(-7.86998595823514,16.1888095900877,-11.9944437247707));
#26265=CARTESIAN_POINT('Ctrl Pts',(-7.75305710255021,16.2453053838482,-12.2505195762024));
#26266=CARTESIAN_POINT('Ctrl Pts',(-7.62546188869214,16.3049787177716,-12.5007637751614));
#26267=CARTESIAN_POINT('Ctrl Pts',(-7.56109808564288,16.3350801815789,-12.6269963182875));
#26268=CARTESIAN_POINT('Ctrl Pts',(-7.49402021951091,16.3659910561045,-12.7517445834959));
#26269=CARTESIAN_POINT('Ctrl Pts',(-7.42417484826972,16.397615624974,-12.8749999999798));
#26270=CARTESIAN_POINT('Origin',(0.,76.,-7.93749999999999));
#26271=CARTESIAN_POINT('Ctrl Pts',(-5.80913668152293,74.3748153225003,-10.9908197002073));
#26272=CARTESIAN_POINT('Ctrl Pts',(-5.67334876482947,74.3157933474344,-11.3760244264246));
#26273=CARTESIAN_POINT('Ctrl Pts',(-5.48207182842344,74.2522007025348,-11.7998901094902));
#26274=CARTESIAN_POINT('Ctrl Pts',(-4.95384740584261,74.1135707631099,-12.653829766117));
#26275=CARTESIAN_POINT('Ctrl Pts',(-4.66538309328688,74.0478644569286,-13.0286302410656));
#26276=CARTESIAN_POINT('Ctrl Pts',(-3.74940791549978,73.8635536093087,-13.9963130606203));
#26277=CARTESIAN_POINT('Ctrl Pts',(-3.04622404223991,73.7476300383179,-14.5060716837974));
#26278=CARTESIAN_POINT('Ctrl Pts',(-1.74204887561165,73.5661588961296,-15.1231710302632));
#26279=CARTESIAN_POINT('Ctrl Pts',(-0.926330645356949,73.4550883535588,
-15.4378592293412));
#26280=CARTESIAN_POINT('Ctrl Pts',(0.562811661989643,73.2654430613796,-15.6006444679771));
#26281=CARTESIAN_POINT('Ctrl Pts',(0.991359300347177,73.2120251146354,-15.6108736298658));
#26282=CARTESIAN_POINT('Ctrl Pts',(1.86955409604265,73.1046785119871,-15.5571416466731));
#26283=CARTESIAN_POINT('Ctrl Pts',(2.31069667091151,73.0527156300785,-15.4893464683708));
#26284=CARTESIAN_POINT('Ctrl Pts',(2.74837297199499,73.0000000000003,-15.3839993290003));
#26285=CARTESIAN_POINT('',(-3.34416379521191,73.0000000000002,-15.1361439529118));
#26286=CARTESIAN_POINT('Origin',(0.,73.,-7.93749999999999));
#26287=CARTESIAN_POINT('',(-1.41388501872634E-15,73.694202182856,-0.694202182856027));
#26288=CARTESIAN_POINT('Ctrl Pts',(-3.34416379521187,73.,-15.1361439529117));
#26289=CARTESIAN_POINT('Ctrl Pts',(-4.22508208124688,73.0317651468065,-14.6918837683));
#26290=CARTESIAN_POINT('Ctrl Pts',(-5.01478929567479,73.0646106900317,-14.0862063128347));
#26291=CARTESIAN_POINT('Ctrl Pts',(-6.36082539665937,73.1306089592706,-12.580136728871));
#26292=CARTESIAN_POINT('Ctrl Pts',(-6.89299777093761,73.1630625007004,-11.6798119029563));
#26293=CARTESIAN_POINT('Ctrl Pts',(-7.59352950420832,73.2354722402261,-9.64199315526779));
#26294=CARTESIAN_POINT('Ctrl Pts',(-7.67550414883065,73.2681752177959,-8.65873837058869));
#26295=CARTESIAN_POINT('Ctrl Pts',(-7.60286970509253,73.3261655212376,-6.87515120113955));
#26296=CARTESIAN_POINT('Ctrl Pts',(-7.36420970282702,73.3605784477511,-5.89355743635864));
#26297=CARTESIAN_POINT('Ctrl Pts',(-6.56006614657876,73.4260174028793,-4.16903668548547));
#26298=CARTESIAN_POINT('Ctrl Pts',(-5.99694992288785,73.4580449578172,-3.34369296659196));
#26299=CARTESIAN_POINT('Ctrl Pts',(-4.85823706235724,73.5114865221786,-2.30042237137467));
#26300=CARTESIAN_POINT('Ctrl Pts',(-4.47064145492997,73.5284750019196,-2.0095633605085));
#26301=CARTESIAN_POINT('Ctrl Pts',(-3.24491645562334,73.5789367752769,-1.26504415519658));
#26302=CARTESIAN_POINT('Ctrl Pts',(-2.33864132871221,73.6108820263253,-0.928923923375816));
#26303=CARTESIAN_POINT('Ctrl Pts',(-0.933384219456304,73.6607444411162,
-0.70569357476857));
#26304=CARTESIAN_POINT('Ctrl Pts',(-0.465894690246344,73.6774433167434,
-0.677443316743452));
#26305=CARTESIAN_POINT('Ctrl Pts',(-1.38777878078145E-16,73.694202182856,
-0.694202182856026));
#26306=CARTESIAN_POINT('',(-6.04669357079005E-16,76.,-2.99999999999999));
#26307=CARTESIAN_POINT('',(-6.04669357079005E-16,76.,-2.99999999999999));
#26308=CARTESIAN_POINT('Origin',(0.,76.,-7.93749999999999));
#26309=CARTESIAN_POINT('Ctrl Pts',(2.77555756156289E-16,73.694202182856,
-0.694202182856026));
#26310=CARTESIAN_POINT('Ctrl Pts',(0.454376060453808,73.7105467081775,-0.710546708177571));
#26311=CARTESIAN_POINT('Ctrl Pts',(0.907235171861323,73.726948314343,-0.769702150673434));
#26312=CARTESIAN_POINT('Ctrl Pts',(2.26893059456179,73.7766019097737,-1.08089595715675));
#26313=CARTESIAN_POINT('Ctrl Pts',(3.13748436394977,73.8088335460852,-1.46722967249179));
#26314=CARTESIAN_POINT('Ctrl Pts',(4.7286962188268,73.8805074247047,-2.60266444957381));
#26315=CARTESIAN_POINT('Ctrl Pts',(5.35369283675739,73.9143938763295,-3.31453476733563));
#26316=CARTESIAN_POINT('Ctrl Pts',(6.25899628022628,73.975690028823,-4.7679037847388));
#26317=CARTESIAN_POINT('Ctrl Pts',(6.57538939670816,74.0084067304685,-5.58569923670778));
#26318=CARTESIAN_POINT('Ctrl Pts',(6.88151449957619,74.0722484654855,-7.25660344054492));
#26319=CARTESIAN_POINT('Ctrl Pts',(6.89995184173098,74.1046959288186,-8.18342538444765));
#26320=CARTESIAN_POINT('Ctrl Pts',(6.49722993178434,74.1755027990535,-10.0042182724129));
#26321=CARTESIAN_POINT('Ctrl Pts',(6.14535741819483,74.2094533637712,-10.8118598844939));
#26322=CARTESIAN_POINT('Ctrl Pts',(5.31863856072002,74.264263195562,-12.0097425581265));
#26323=CARTESIAN_POINT('Ctrl Pts',(4.9281190222573,74.2858035323405,-12.4428896711152));
#26324=CARTESIAN_POINT('Ctrl Pts',(4.05499771184754,74.3304865900484,-13.1839033554255));
#26325=CARTESIAN_POINT('Ctrl Pts',(3.58197878378907,74.3527482881805,-13.4911923382182));
#26326=CARTESIAN_POINT('Ctrl Pts',(3.07575458898223,74.3748153225001,-13.734789356643));
#26327=CARTESIAN_POINT('Origin',(0.,-18.001,-7.93750000000004));
#26328=CARTESIAN_POINT('Ctrl Pts',(-8.32667268468867E-16,72.825,-15.875));
#26329=CARTESIAN_POINT('Ctrl Pts',(-0.395827506290079,72.8454947954835,
-15.875));
#26330=CARTESIAN_POINT('Ctrl Pts',(-0.791617129110936,72.8659876294712,
-15.8453912454244));
#26331=CARTESIAN_POINT('Ctrl Pts',(-1.93136566829669,72.9250004894723,-15.6734516698727));
#26332=CARTESIAN_POINT('Ctrl Pts',(-2.65872844411335,72.9615973108245,-15.4545661585517));
#26333=CARTESIAN_POINT('Ctrl Pts',(-3.34416379521214,73.0000000000001,-15.1361439529117));
#26334=CARTESIAN_POINT('Origin',(0.,1.11022302462516E-13,-15.875));
#26335=CARTESIAN_POINT('',(-2.57755123502973,16.6150404676652,-15.875));
#26336=CARTESIAN_POINT('Ctrl Pts',(-6.18681074697824,13.6646760949932,-15.875));
#26337=CARTESIAN_POINT('Ctrl Pts',(-6.04942753338936,13.7268776392074,-15.875));
#26338=CARTESIAN_POINT('Ctrl Pts',(-5.91423497782962,13.7936520594916,-15.875));
#26339=CARTESIAN_POINT('Ctrl Pts',(-5.78131071258862,13.8644897336605,-15.875));
#26340=CARTESIAN_POINT('Ctrl Pts',(-5.64040818509895,13.9395791638243,-15.875));
#26341=CARTESIAN_POINT('Ctrl Pts',(-5.50205371352212,14.019234808701,-15.875));
#26342=CARTESIAN_POINT('Ctrl Pts',(-5.36636167242817,14.1029047612554,-15.875));
#26343=CARTESIAN_POINT('Ctrl Pts',(-5.29440248962166,14.1472759812823,-15.875));
#26344=CARTESIAN_POINT('Ctrl Pts',(-5.22319249151731,14.1927770029562,-15.875));
#26345=CARTESIAN_POINT('Ctrl Pts',(-5.15275208328258,14.2393303034111,-15.875));
#26346=CARTESIAN_POINT('Ctrl Pts',(-4.82417650905228,14.4564823303883,-15.875));
#26347=CARTESIAN_POINT('Ctrl Pts',(-4.51455185467379,14.6945381516704,-15.875));
#26348=CARTESIAN_POINT('Ctrl Pts',(-4.21891718821225,14.9480256152924,-15.875));
#26349=CARTESIAN_POINT('Ctrl Pts',(-3.62764785528917,15.4550005425365,-15.875));
#26350=CARTESIAN_POINT('Ctrl Pts',(-3.09286826794447,16.0242864292497,-15.875));
#26351=CARTESIAN_POINT('Ctrl Pts',(-2.57755123502973,16.6150404676652,-15.875));
#26352=CARTESIAN_POINT('Ctrl Pts',(-2.57755123503017,16.6150404676659,-15.875));
#26353=CARTESIAN_POINT('Ctrl Pts',(-2.53648329737381,16.6621203203971,-15.875));
#26354=CARTESIAN_POINT('Ctrl Pts',(-2.49248343900961,16.7057360650919,-15.875));
#26355=CARTESIAN_POINT('Ctrl Pts',(-2.44700266076792,16.7475590170876,-15.875));
#26356=CARTESIAN_POINT('Ctrl Pts',(-2.4020906969716,16.788858901973,-15.875));
#26357=CARTESIAN_POINT('Ctrl Pts',(-2.35562102859357,16.8282993969611,-15.875));
#26358=CARTESIAN_POINT('Ctrl Pts',(-2.3080370454668,16.8664261008931,-15.8749999999998));
#26359=CARTESIAN_POINT('Ctrl Pts',(-2.30742826936455,16.8669138832241,-15.8749999999998));
#26360=CARTESIAN_POINT('Ctrl Pts',(-2.30681931537933,16.8674014466309,-15.8749999999998));
#26361=CARTESIAN_POINT('Ctrl Pts',(-2.30621018438793,16.8678887923135,-15.8749999999998));
#26362=CARTESIAN_POINT('Ctrl Pts',(-2.23061417258728,16.9283706763259,-15.8749999999995));
#26363=CARTESIAN_POINT('Ctrl Pts',(-2.15212082757854,16.9856522751252,-15.875));
#26364=CARTESIAN_POINT('Ctrl Pts',(-2.0718228292108,17.0403639484817,-15.8749999999997));
#26365=CARTESIAN_POINT('Ctrl Pts',(-2.05098109666076,17.054564627037,-15.8749999999996));
#26366=CARTESIAN_POINT('Ctrl Pts',(-2.03001761816751,17.0685919387124,-15.8749999999995));
#26367=CARTESIAN_POINT('Ctrl Pts',(-2.00895126657008,17.0824564612662,-15.8749999999992));
#26368=CARTESIAN_POINT('Ctrl Pts',(-2.00765800896842,17.0833076005394,-15.8749999999992));
#26369=CARTESIAN_POINT('Ctrl Pts',(-2.00636435367826,17.0841581316114,-15.8749999999992));
#26370=CARTESIAN_POINT('Ctrl Pts',(-2.00507030581251,17.0850080563855,-15.8749999999992));
#26371=CARTESIAN_POINT('Ctrl Pts',(-1.90188935724152,17.1527768358274,-15.8749999999978));
#26372=CARTESIAN_POINT('Ctrl Pts',(-1.796434748319,17.2164714546352,-15.8749999999985));
#26373=CARTESIAN_POINT('Ctrl Pts',(-1.68924216461426,17.2770977324932,-15.8749999999992));
#26374=CARTESIAN_POINT('Ctrl Pts',(-1.58388083753985,17.3366882831633,-15.8749999999998));
#26375=CARTESIAN_POINT('Ctrl Pts',(-1.47682790841131,17.3932876269073,-15.8749999999999));
#26376=CARTESIAN_POINT('Ctrl Pts',(-1.36838950083533,17.4474158111803,-15.8749999999999));
#26377=CARTESIAN_POINT('Ctrl Pts',(-1.36701527573572,17.4481017702523,-15.8749999999999));
#26378=CARTESIAN_POINT('Ctrl Pts',(-1.36564083943549,17.4487873299025,-15.8749999999999));
#26379=CARTESIAN_POINT('Ctrl Pts',(-1.36426619268609,17.4494724911175,-15.8749999999999));
#26380=CARTESIAN_POINT('Ctrl Pts',(-1.24440837618391,17.5092128769371,-15.8749999999996));
#26381=CARTESIAN_POINT('Ctrl Pts',(-1.12295905583498,17.5659434337456,-15.8749999999586));
#26382=CARTESIAN_POINT('Ctrl Pts',(-1.00026331620377,17.6199805908429,-15.8749999998258));
#26383=CARTESIAN_POINT('Ctrl Pts',(-0.898709167959604,17.6647066545109,
-15.874999999716));
#26384=CARTESIAN_POINT('Ctrl Pts',(-0.796301966219198,17.7075888044325,
-15.874999999598));
#26385=CARTESIAN_POINT('Ctrl Pts',(-0.693249644331463,17.7488301778621,
-15.8749999996073));
#26386=CARTESIAN_POINT('Ctrl Pts',(-0.550308584896857,17.8060349598853,
-15.8749999996201));
#26387=CARTESIAN_POINT('Ctrl Pts',(-0.406059151969994,17.8600031401019,
-15.8749999998645));
#26388=CARTESIAN_POINT('Ctrl Pts',(-0.261072807205695,17.911130219345,-15.8749999999505));
#26389=CARTESIAN_POINT('Ctrl Pts',(-0.174270671136077,17.9417395825683,
-15.8750000000021));
#26390=CARTESIAN_POINT('Ctrl Pts',(-0.0872048169539691,17.9713317586215,
-15.875));
#26391=CARTESIAN_POINT('Ctrl Pts',(5.82643290799559E-14,18.0000000000001,
-15.875));
#26392=CARTESIAN_POINT('',(2.57755123502973,16.6150404676651,-15.875));
#26393=CARTESIAN_POINT('Ctrl Pts',(6.56141807553468E-14,18.0000000000001,
-15.875));
#26394=CARTESIAN_POINT('Ctrl Pts',(0.163234899420945,17.9463369294279,-15.875));
#26395=CARTESIAN_POINT('Ctrl Pts',(0.325479452729011,17.8896359397147,-15.8749999997925));
#26396=CARTESIAN_POINT('Ctrl Pts',(0.486261202262205,17.829207831248,-15.8749999978486));
#26397=CARTESIAN_POINT('Ctrl Pts',(0.556197005496128,17.8029232043187,-15.8749999970031));
#26398=CARTESIAN_POINT('Ctrl Pts',(0.625856192700561,17.7759340687492,-15.8749999959428));
#26399=CARTESIAN_POINT('Ctrl Pts',(0.695200618726449,17.7481866429567,-15.8749999948273));
#26400=CARTESIAN_POINT('Ctrl Pts',(0.695202869078957,17.7481857425023,-15.8749999948272));
#26401=CARTESIAN_POINT('Ctrl Pts',(0.695205119431131,17.7481848420472,-15.8749999948272));
#26402=CARTESIAN_POINT('Ctrl Pts',(0.695207369782971,17.7481839415913,-15.8749999948272));
#26403=CARTESIAN_POINT('Ctrl Pts',(0.792820281938614,17.7091251069099,-15.8749999932568));
#26404=CARTESIAN_POINT('Ctrl Pts',(0.889818282082731,17.6685776890752,-15.8749999939569));
#26405=CARTESIAN_POINT('Ctrl Pts',(0.986075309087794,17.6263508819597,-15.874999995884));
#26406=CARTESIAN_POINT('Ctrl Pts',(1.0779093479489,17.5860643868717,-15.8749999977226));
#26407=CARTESIAN_POINT('Ctrl Pts',(1.16906840852933,17.544249418016,-15.8749999995905));
#26408=CARTESIAN_POINT('Ctrl Pts',(1.25946486042866,17.5007819756592,-15.8749999998948));
#26409=CARTESIAN_POINT('Ctrl Pts',(1.29635651290361,17.4830424986808,-15.875000000019));
#26410=CARTESIAN_POINT('Ctrl Pts',(1.33312145695237,17.4650282848733,-15.875));
#26411=CARTESIAN_POINT('Ctrl Pts',(1.36975523467035,17.4467329717171,-15.875));
#26412=CARTESIAN_POINT('Ctrl Pts',(1.36977642588146,17.4467223885923,-15.875));
#26413=CARTESIAN_POINT('Ctrl Pts',(1.36979761704848,17.4467118053719,-15.875));
#26414=CARTESIAN_POINT('Ctrl Pts',(1.36981880817139,17.4467012220559,-15.875));
#26415=CARTESIAN_POINT('Ctrl Pts',(1.48005617514885,17.3916462402392,-15.875));
#26416=CARTESIAN_POINT('Ctrl Pts',(1.58909781966939,17.3339013736985,-15.875));
#26417=CARTESIAN_POINT('Ctrl Pts',(1.69590260920769,17.2733228121837,-15.875));
#26418=CARTESIAN_POINT('Ctrl Pts',(1.80272792862359,17.2127326063367,-15.875));
#26419=CARTESIAN_POINT('Ctrl Pts',(1.90750675821464,17.1492444885504,-15.875));
#26420=CARTESIAN_POINT('Ctrl Pts',(2.00963535661709,17.0820035460311,-15.875));
#26421=CARTESIAN_POINT('Ctrl Pts',(2.00964517091121,17.0819970843505,-15.875));
#26422=CARTESIAN_POINT('Ctrl Pts',(2.00965498518143,17.0819906226361,-15.875));
#26423=CARTESIAN_POINT('Ctrl Pts',(2.00966479942777,17.0819841608878,-15.875));
#26424=CARTESIAN_POINT('Ctrl Pts',(2.11178308708155,17.014748975667,-15.875));
#26425=CARTESIAN_POINT('Ctrl Pts',(2.21131503888981,16.9438514389378,-15.875));
#26426=CARTESIAN_POINT('Ctrl Pts',(2.30688671952936,16.8673460056645,-15.875));
#26427=CARTESIAN_POINT('Ctrl Pts',(2.30689131206627,16.8673423293241,-15.875));
#26428=CARTESIAN_POINT('Ctrl Pts',(2.30689590459396,16.8673386529707,-15.875));
#26429=CARTESIAN_POINT('Ctrl Pts',(2.30690049711243,16.8673349766043,-15.875));
#26430=CARTESIAN_POINT('Ctrl Pts',(2.35469121108945,16.8290779335589,-15.875));
#26431=CARTESIAN_POINT('Ctrl Pts',(2.40147429518024,16.789416499467,-15.875));
#26432=CARTESIAN_POINT('Ctrl Pts',(2.4468278441479,16.7477195558332,-15.875));
#26433=CARTESIAN_POINT('Ctrl Pts',(2.49217613728494,16.7060274442816,-15.875));
#26434=CARTESIAN_POINT('Ctrl Pts',(2.53621611943434,16.6624266103822,-15.875));
#26435=CARTESIAN_POINT('Ctrl Pts',(2.57755123502764,16.6150404676675,-15.875));
#26436=CARTESIAN_POINT('Ctrl Pts',(2.57755123502976,16.6150404676651,-15.875));
#26437=CARTESIAN_POINT('Ctrl Pts',(3.09339220814419,16.0236857897033,-15.875));
#26438=CARTESIAN_POINT('Ctrl Pts',(3.62953325790838,15.452428023713,-15.875));
#26439=CARTESIAN_POINT('Ctrl Pts',(4.22657730609841,14.9414637355988,-15.875));
#26440=CARTESIAN_POINT('Ctrl Pts',(4.46002708929085,14.7416719402682,-15.875));
#26441=CARTESIAN_POINT('Ctrl Pts',(4.70080932940665,14.5526624071818,-15.875));
#26442=CARTESIAN_POINT('Ctrl Pts',(4.95042406413429,14.3770855263889,-15.875));
#26443=CARTESIAN_POINT('Ctrl Pts',(5.1714780269072,14.2215980496062,-15.875));
#26444=CARTESIAN_POINT('Ctrl Pts',(5.39945880318352,14.076644774025,-15.875));
#26445=CARTESIAN_POINT('Ctrl Pts',(5.63543015960283,13.9441001459419,-15.875));
#26446=CARTESIAN_POINT('Ctrl Pts',(5.81446516266139,13.8435365510449,-15.875));
#26447=CARTESIAN_POINT('Ctrl Pts',(5.99810030405848,13.7501165276488,-15.875));
#26448=CARTESIAN_POINT('Ctrl Pts',(6.18681074697913,13.6646760949928,-15.875));
#26449=CARTESIAN_POINT('Origin',(0.,0.,0.));
#26450=CARTESIAN_POINT('',(2.57755123502967,16.615040467665,0.));
#26451=CARTESIAN_POINT('Ctrl Pts',(6.18681074697836,13.6646760949931,-3.90312782094782E-15));
#26452=CARTESIAN_POINT('Ctrl Pts',(6.04942753363656,13.7268776390737,-3.90312782094782E-15));
#26453=CARTESIAN_POINT('Ctrl Pts',(5.91423497832213,13.7936520592212,-3.9031272724464E-15));
#26454=CARTESIAN_POINT('Ctrl Pts',(5.7813107133205,13.864489733245,-3.90312839779568E-15));
#26455=CARTESIAN_POINT('Ctrl Pts',(5.64040818592427,13.9395791633405,-3.90312959068968E-15));
#26456=CARTESIAN_POINT('Ctrl Pts',(5.50205371444,14.0192348081498,-3.90312762761502E-15));
#26457=CARTESIAN_POINT('Ctrl Pts',(5.36636167343317,14.1029047606296,-3.90316800608413E-15));
#26458=CARTESIAN_POINT('Ctrl Pts',(5.29440249028531,14.1472759808558,-3.90318941929032E-15));
#26459=CARTESIAN_POINT('Ctrl Pts',(5.22319249184617,14.1927770027392,-3.90322389755505E-15));
#26460=CARTESIAN_POINT('Ctrl Pts',(5.15275208328281,14.2393303034112,-3.90329226654004E-15));
#26461=CARTESIAN_POINT('Ctrl Pts',(4.82417650905236,14.4564823303883,-3.90361117977412E-15));
#26462=CARTESIAN_POINT('Ctrl Pts',(4.51455185467436,14.694538151671,-3.90293915145114E-15));
#26463=CARTESIAN_POINT('Ctrl Pts',(4.21891718821264,14.9480256152927,-3.90333349758813E-15));
#26464=CARTESIAN_POINT('Ctrl Pts',(3.62764785528921,15.4550005425363,-3.9041221898621E-15));
#26465=CARTESIAN_POINT('Ctrl Pts',(3.09286826794445,16.0242864292495,-3.9031278220838E-15));
#26466=CARTESIAN_POINT('Ctrl Pts',(2.57755123502973,16.6150404676649,-3.90312782094782E-15));
#26467=CARTESIAN_POINT('Ctrl Pts',(2.57755123502967,16.615040467665,-3.90312782094782E-15));
#26468=CARTESIAN_POINT('Ctrl Pts',(2.53664321583118,16.6619369915551,-3.90312783753E-15));
#26469=CARTESIAN_POINT('Ctrl Pts',(2.49260173716415,16.7056313191094,-4.86323593045554E-15));
#26470=CARTESIAN_POINT('Ctrl Pts',(2.44692282074809,16.7476322243581,-4.45426722229462E-15));
#26471=CARTESIAN_POINT('Ctrl Pts',(2.40124621644852,16.7896310036591,-4.04531921478443E-15));
#26472=CARTESIAN_POINT('Ctrl Pts',(2.35376064355281,16.8298668109454,-3.90316469176341E-15));
#26473=CARTESIAN_POINT('Ctrl Pts',(2.30550348248287,16.8684526549718,-3.90360339707742E-15));
#26474=CARTESIAN_POINT('Ctrl Pts',(2.30549795427634,16.868457075259,-3.90360344733428E-15));
#26475=CARTESIAN_POINT('Ctrl Pts',(2.30549242605973,16.8684614955246,-3.90360349758508E-15));
#26476=CARTESIAN_POINT('Ctrl Pts',(2.30548689783303,16.8684659157685,-3.90360354782982E-15));
#26477=CARTESIAN_POINT('Ctrl Pts',(2.20897530897574,16.9456343795253,-3.90448071870476E-15));
#26478=CARTESIAN_POINT('Ctrl Pts',(2.1088973161954,17.0167607154954,-3.80478103571114E-15));
#26479=CARTESIAN_POINT('Ctrl Pts',(2.00654625140481,17.0840357067547,-4.01874756173234E-15));
#26480=CARTESIAN_POINT('Ctrl Pts',(2.00653452597976,17.0840434138349,-4.01877207391958E-15));
#26481=CARTESIAN_POINT('Ctrl Pts',(2.00652280052487,17.0840511208646,-4.01879658554702E-15));
#26482=CARTESIAN_POINT('Ctrl Pts',(2.00651107504016,17.0840588278437,-4.0188210966111E-15));
#26483=CARTESIAN_POINT('Ctrl Pts',(1.90414776448742,17.1513406433296,-4.23280232840214E-15));
#26484=CARTESIAN_POINT('Ctrl Pts',(1.7994492991963,17.2146660834217,-4.13342344656728E-15));
#26485=CARTESIAN_POINT('Ctrl Pts',(1.6929747873709,17.274982420926,-4.03076142423713E-15));
#26486=CARTESIAN_POINT('Ctrl Pts',(1.58652466725004,17.3352849408672,-3.9281229202277E-15));
#26487=CARTESIAN_POINT('Ctrl Pts',(1.47828499287738,17.3925554738715,-3.90603445548038E-15));
#26488=CARTESIAN_POINT('Ctrl Pts',(1.36856924611844,17.4473251477231,-3.91849178334325E-15));
#26489=CARTESIAN_POINT('Ctrl Pts',(1.36854410497944,17.4473376980819,-3.91849463791446E-15));
#26490=CARTESIAN_POINT('Ctrl Pts',(1.36851896376299,17.4473502483093,-3.91849749145131E-15));
#26491=CARTESIAN_POINT('Ctrl Pts',(1.36849382246909,17.4473627984054,-3.91850034395322E-15));
#26492=CARTESIAN_POINT('Ctrl Pts',(1.14904840747076,17.5569061278786,-3.94339836500619E-15));
#26493=CARTESIAN_POINT('Ctrl Pts',(0.923340187830619,17.6566523551606,-3.89436736404263E-15));
#26494=CARTESIAN_POINT('Ctrl Pts',(0.694759689676839,17.7481734415667,-3.93289872637456E-15));
#26495=CARTESIAN_POINT('Ctrl Pts',(0.694723521974647,17.7481879227119,-3.93290482309256E-15));
#26496=CARTESIAN_POINT('Ctrl Pts',(0.694687354237592,17.7482024036388,-3.93292082649647E-15));
#26497=CARTESIAN_POINT('Ctrl Pts',(0.69465118646567,17.7482168843473,-3.93294675089361E-15));
#26498=CARTESIAN_POINT('Ctrl Pts',(0.500498710332174,17.8259508797229,-4.07211169335415E-15));
#26499=CARTESIAN_POINT('Ctrl Pts',(0.305013033138498,17.8973939584755,-2.1129514982979E-11));
#26500=CARTESIAN_POINT('Ctrl Pts',(0.106113584617659,17.9646283560373,-2.93212936336714E-12));
#26501=CARTESIAN_POINT('Ctrl Pts',(0.0708535797065735,17.9765473694174,
2.9382179480916E-13));
#26502=CARTESIAN_POINT('Ctrl Pts',(0.0354862560896116,17.9883340325599,
-3.35120567100207E-15));
#26503=CARTESIAN_POINT('Ctrl Pts',(1.34330150810747E-13,18.,-3.25260651745651E-15));
#26504=CARTESIAN_POINT('',(-2.57755123502756,16.6150404676675,0.));
#26505=CARTESIAN_POINT('Ctrl Pts',(1.00919272938427E-13,18.,-3.25260651745651E-15));
#26506=CARTESIAN_POINT('Ctrl Pts',(-0.163234977781181,17.9463369036664,
-3.70647810751983E-15));
#26507=CARTESIAN_POINT('Ctrl Pts',(-0.325479608497338,17.8896358852711,
-2.075071171567E-10));
#26508=CARTESIAN_POINT('Ctrl Pts',(-0.486261433812618,17.829207744229,-2.15138301120851E-9));
#26509=CARTESIAN_POINT('Ctrl Pts',(-0.556197159254499,17.8029231447565,
-2.9969162084646E-9));
#26510=CARTESIAN_POINT('Ctrl Pts',(-0.625856269235421,17.7759340381391,
-4.05715075919456E-9));
#26511=CARTESIAN_POINT('Ctrl Pts',(-0.69520061873086,17.748186642968,-5.17270802021755E-9));
#26512=CARTESIAN_POINT('Ctrl Pts',(-0.695202869082881,17.7481857425139,
-5.17274422210789E-9));
#26513=CARTESIAN_POINT('Ctrl Pts',(-0.695205119434567,17.748184842059,-5.17278042406062E-9));
#26514=CARTESIAN_POINT('Ctrl Pts',(-0.69520736978592,17.7481839416033,-5.17281662607575E-9));
#26515=CARTESIAN_POINT('Ctrl Pts',(-0.792820282116332,17.70912510685,-6.7431421330446E-9));
#26516=CARTESIAN_POINT('Ctrl Pts',(-0.889818282432727,17.6685776889372,
-6.04304683973043E-9));
#26517=CARTESIAN_POINT('Ctrl Pts',(-0.986075309607311,17.6263508817377,
-4.1159309985783E-9));
#26518=CARTESIAN_POINT('Ctrl Pts',(-1.07790934859941,17.586064386583,-2.27736568554749E-9));
#26519=CARTESIAN_POINT('Ctrl Pts',(-1.16906840930876,17.5442494176561,-4.09449895856158E-10));
#26520=CARTESIAN_POINT('Ctrl Pts',(-1.25946486133493,17.5007819752242,-1.0514569748843E-10));
#26521=CARTESIAN_POINT('Ctrl Pts',(-1.29635651350569,17.4830424983862,1.90437412412553E-11));
#26522=CARTESIAN_POINT('Ctrl Pts',(-1.33312145725236,17.4650282847238,-3.91465477576115E-15));
#26523=CARTESIAN_POINT('Ctrl Pts',(-1.36975523467049,17.4467329717176,-3.90420294014398E-15));
#26524=CARTESIAN_POINT('Ctrl Pts',(-1.36977642588111,17.446722388593,-3.90419689416495E-15));
#26525=CARTESIAN_POINT('Ctrl Pts',(-1.36979761704765,17.4467118053728,-3.90419380688497E-15));
#26526=CARTESIAN_POINT('Ctrl Pts',(-1.36981880817008,17.4467012220571,-3.90419364112946E-15));
#26527=CARTESIAN_POINT('Ctrl Pts',(-1.48005617514827,17.3916462402406,-3.90333137200445E-15));
#26528=CARTESIAN_POINT('Ctrl Pts',(-1.58909781966898,17.3339013736989,-3.90950951142143E-15));
#26529=CARTESIAN_POINT('Ctrl Pts',(-1.69590260920755,17.2733228121837,-3.97030686335835E-15));
#26530=CARTESIAN_POINT('Ctrl Pts',(-1.80272792862322,17.2127326063365,-4.03111590168284E-15));
#26531=CARTESIAN_POINT('Ctrl Pts',(-1.90750675821447,17.1492444885502,-4.090111775224E-15));
#26532=CARTESIAN_POINT('Ctrl Pts',(-2.00963535661692,17.082003546031,-3.9687347184938E-15));
#26533=CARTESIAN_POINT('Ctrl Pts',(-2.00964517091037,17.0819970843508,-3.96872305447342E-15));
#26534=CARTESIAN_POINT('Ctrl Pts',(-2.00965498517993,17.0819906226368,-3.96871139022941E-15));
#26535=CARTESIAN_POINT('Ctrl Pts',(-2.0096647994256,17.0819841608889,-3.96869972576296E-15));
#26536=CARTESIAN_POINT('Ctrl Pts',(-2.11178308708009,17.0147489756678,-3.84732969085294E-15));
#26537=CARTESIAN_POINT('Ctrl Pts',(-2.21131503888902,16.9438514389382,-3.91028333280058E-15));
#26538=CARTESIAN_POINT('Ctrl Pts',(-2.30688671952919,16.8673460056643,-3.90564247479998E-15));
#26539=CARTESIAN_POINT('Ctrl Pts',(-2.30689131206538,16.8673423293246,-3.90564225179136E-15));
#26540=CARTESIAN_POINT('Ctrl Pts',(-2.30689590459235,16.8673386529717,-3.90564202876022E-15));
#26541=CARTESIAN_POINT('Ctrl Pts',(-2.30690049711011,16.8673349766059,-3.90564180570655E-15));
#26542=CARTESIAN_POINT('Ctrl Pts',(-2.35469121108777,16.8290779335601,-3.90332066193792E-15));
#26543=CARTESIAN_POINT('Ctrl Pts',(-2.40147429518223,16.7894164994713,-4.08152894233206E-15));
#26544=CARTESIAN_POINT('Ctrl Pts',(-2.44682784415303,16.7477195558388,-4.56166899524867E-15));
#26545=CARTESIAN_POINT('Ctrl Pts',(-2.49217613729193,16.7060274442897,-5.04175340675553E-15));
#26546=CARTESIAN_POINT('Ctrl Pts',(-2.53621611943382,16.6624266103826,-3.90312784896662E-15));
#26547=CARTESIAN_POINT('Ctrl Pts',(-2.57755123502756,16.6150404676675,-3.90312782094782E-15));
#26548=CARTESIAN_POINT('Ctrl Pts',(-2.57755123502756,16.6150404676675,-3.90312782094782E-15));
#26549=CARTESIAN_POINT('Ctrl Pts',(-3.09339220814233,16.0236857897052,-3.90312781973625E-15));
#26550=CARTESIAN_POINT('Ctrl Pts',(-3.62953325790676,15.4524280237144,-3.90460918672713E-15));
#26551=CARTESIAN_POINT('Ctrl Pts',(-4.22657730609724,14.9414637356001,-3.90365083757559E-15));
#26552=CARTESIAN_POINT('Ctrl Pts',(-4.46002708931194,14.7416719402505,-3.90327611413184E-15));
#26553=CARTESIAN_POINT('Ctrl Pts',(-4.70080932945974,14.5526624071656,-3.96947826803498E-15));
#26554=CARTESIAN_POINT('Ctrl Pts',(-4.95042406421973,14.3770855263738,-4.05016361199005E-15));
#26555=CARTESIAN_POINT('Ctrl Pts',(-5.17147802720282,14.2215980494645,-4.12161698613911E-15));
#26556=CARTESIAN_POINT('Ctrl Pts',(-5.39945880370098,14.0766447737736,-4.20445864407361E-15));
#26557=CARTESIAN_POINT('Ctrl Pts',(-5.63543016034986,13.9441001455877,-4.26266359505368E-15));
#26558=CARTESIAN_POINT('Ctrl Pts',(-5.81446516317737,13.8435365508404,-4.30682456319525E-15));
#26559=CARTESIAN_POINT('Ctrl Pts',(-5.99810030432704,13.7501165275657,-4.33680868994202E-15));
#26560=CARTESIAN_POINT('Ctrl Pts',(-6.18681074697897,13.6646760949927,-4.33680868994202E-15));
#26561=CARTESIAN_POINT('Origin',(0.,76.,-7.93749999999999));
#26562=CARTESIAN_POINT('Origin',(4.32565866516615,20.8014139268345,-1.69615259943912));
#26563=CARTESIAN_POINT('',(3.73830603269933,20.2061012558294,-2.5436239488228));
#26564=CARTESIAN_POINT('',(4.52144288428828,20.9998514259673,-1.41366213459292));
#26565=CARTESIAN_POINT('',(3.7383057650626,19.5711013646158,-2.543623843377));
#26566=CARTESIAN_POINT('',(3.73830577451205,19.5711012915154,-2.54362383229417));
#26567=CARTESIAN_POINT('',(3.73830600779846,20.2061009926513,-2.54362399397926));
#26568=CARTESIAN_POINT('Ctrl Pts',(-6.56268467749999,75.2062500034686,-7.93749999999999));
#26569=CARTESIAN_POINT('Ctrl Pts',(-6.56268467749997,75.0792500034686,-10.0698455118856));
#26570=CARTESIAN_POINT('Ctrl Pts',(-5.30932343282159,74.9522500034687,-11.7949492688802));
#26571=CARTESIAN_POINT('Ctrl Pts',(-4.05596218814312,74.8252500034686,-13.5200530258749));
#26572=CARTESIAN_POINT('Ctrl Pts',(-2.0279810940716,74.6982500034687,-14.1789840269267));
#26573=CARTESIAN_POINT('Ctrl Pts',(0.,74.5712500034686,-14.8379150279786));
#26574=CARTESIAN_POINT('Ctrl Pts',(2.0279810940716,74.4442500034688,-14.1789840269267));
#26575=CARTESIAN_POINT('Ctrl Pts',(4.05596218814312,74.3172500034686,-13.5200530258749));
#26576=CARTESIAN_POINT('Ctrl Pts',(5.30932343282159,74.1902500034686,-11.7949492688802));
#26577=CARTESIAN_POINT('Ctrl Pts',(6.56268467750008,74.0632500034686,-10.0698455118856));
#26578=CARTESIAN_POINT('Ctrl Pts',(6.5626846775001,73.9362500034686,-7.93749999999999));
#26579=CARTESIAN_POINT('Ctrl Pts',(6.56268467749991,73.8092500034686,-5.80515448811441));
#26580=CARTESIAN_POINT('Ctrl Pts',(5.30932343282159,73.6822500034686,-4.08005073111967));
#26581=CARTESIAN_POINT('Ctrl Pts',(4.05596218814324,73.5552500034685,-2.35494697412514));
#26582=CARTESIAN_POINT('Ctrl Pts',(2.02798109407165,73.4282500034686,-1.69601597307328));
#26583=CARTESIAN_POINT('Ctrl Pts',(0.,73.3012500034685,-1.0370849720215));
#26584=CARTESIAN_POINT('Ctrl Pts',(-2.02798109407154,73.1742500034685,-1.69601597307328));
#26585=CARTESIAN_POINT('Ctrl Pts',(-4.05596218814312,73.0472500034686,-2.35494697412514));
#26586=CARTESIAN_POINT('Ctrl Pts',(-5.30932343282159,72.9202500034686,-4.08005073111967));
#26587=CARTESIAN_POINT('Ctrl Pts',(-6.56268467750003,72.7932500034685,-5.80515448811441));
#26588=CARTESIAN_POINT('Ctrl Pts',(-6.56268467749993,72.6662500034687,-7.93749999999999));
#26589=CARTESIAN_POINT('Ctrl Pts',(-6.56268467749997,72.5392500034685,-10.0698455118856));
#26590=CARTESIAN_POINT('Ctrl Pts',(-5.30932343282159,72.4122500034687,-11.7949492688802));
#26591=CARTESIAN_POINT('Ctrl Pts',(-4.05596218814312,72.2852500034686,-13.5200530258749));
#26592=CARTESIAN_POINT('Ctrl Pts',(-2.0279810940716,72.1582500034688,-14.1789840269267));
#26593=CARTESIAN_POINT('Ctrl Pts',(0.,72.0312500034686,-14.8379150279786));
#26594=CARTESIAN_POINT('Ctrl Pts',(2.02798109407154,71.9042500034687,-14.1789840269267));
#26595=CARTESIAN_POINT('Ctrl Pts',(4.05596218814318,71.7772500034686,-13.5200530258749));
#26596=CARTESIAN_POINT('Ctrl Pts',(5.30932343282159,71.6502500034686,-11.7949492688802));
#26597=CARTESIAN_POINT('Ctrl Pts',(6.56268467750003,71.5232500034685,-10.0698455118856));
#26598=CARTESIAN_POINT('Ctrl Pts',(6.5626846775001,71.3962500034686,-7.93749999999999));
#26599=CARTESIAN_POINT('Ctrl Pts',(6.56268467750008,71.2692500034686,-5.80515448811441));
#26600=CARTESIAN_POINT('Ctrl Pts',(5.30932343282153,71.1422500034686,-4.08005073111967));
#26601=CARTESIAN_POINT('Ctrl Pts',(4.05596218814312,71.0152500034686,-2.35494697412514));
#26602=CARTESIAN_POINT('Ctrl Pts',(2.0279810940716,70.8882500034687,-1.69601597307328));
#26603=CARTESIAN_POINT('Ctrl Pts',(0.,70.7612500034686,-1.0370849720215));
#26604=CARTESIAN_POINT('Ctrl Pts',(-2.02798109407148,70.6342500034686,-1.69601597307328));
#26605=CARTESIAN_POINT('Ctrl Pts',(-4.05596218814318,70.5072500034686,-2.35494697412514));
#26606=CARTESIAN_POINT('Ctrl Pts',(-5.30932343282159,70.3802500034686,-4.08005073111967));
#26607=CARTESIAN_POINT('Ctrl Pts',(-6.56268467750003,70.2532500034686,-5.80515448811441));
#26608=CARTESIAN_POINT('Ctrl Pts',(-6.56268467749999,70.1262500034686,-7.93749999999999));
#26609=CARTESIAN_POINT('Ctrl Pts',(-6.56268467750003,69.9992500034686,-10.0698455118856));
#26610=CARTESIAN_POINT('Ctrl Pts',(-5.30932343282153,69.8722500034687,-11.7949492688802));
#26611=CARTESIAN_POINT('Ctrl Pts',(-4.05596218814324,69.7452500034685,-13.5200530258749));
#26612=CARTESIAN_POINT('Ctrl Pts',(-2.02798109407154,69.6182500034687,-14.1789840269267));
#26613=CARTESIAN_POINT('Ctrl Pts',(-5.83678785436452E-14,69.4912500034686,
-14.8379150279786));
#26614=CARTESIAN_POINT('Ctrl Pts',(2.02798109407154,69.3642500034687,-14.1789840269267));
#26615=CARTESIAN_POINT('Ctrl Pts',(4.05596218814318,69.2372500034687,-13.5200530258749));
#26616=CARTESIAN_POINT('Ctrl Pts',(5.30932343282164,69.1102500034686,-11.7949492688802));
#26617=CARTESIAN_POINT('Ctrl Pts',(6.56268467750003,68.9832500034685,-10.0698455118856));
#26618=CARTESIAN_POINT('Ctrl Pts',(6.56268467749999,68.8562500034686,-7.93749999999999));
#26619=CARTESIAN_POINT('Ctrl Pts',(6.56268467750003,68.7292500034685,-5.80515448811441));
#26620=CARTESIAN_POINT('Ctrl Pts',(5.30932343282159,68.6022500034686,-4.08005073111967));
#26621=CARTESIAN_POINT('Ctrl Pts',(4.05596218814318,68.4752500034685,-2.35494697412514));
#26622=CARTESIAN_POINT('Ctrl Pts',(2.0279810940716,68.3482500034686,-1.69601597307328));
#26623=CARTESIAN_POINT('Ctrl Pts',(-1.1673575708729E-13,68.2212500034685,
-1.0370849720215));
#26624=CARTESIAN_POINT('Ctrl Pts',(-2.02798109407154,68.0942500034687,-1.69601597307328));
#26625=CARTESIAN_POINT('Ctrl Pts',(-4.05596218814306,67.9672500034686,-2.35494697412514));
#26626=CARTESIAN_POINT('Ctrl Pts',(-5.30932343282159,67.8402500034686,-4.08005073111967));
#26627=CARTESIAN_POINT('Ctrl Pts',(-6.56268467749997,67.7132500034685,-5.80515448811441));
#26628=CARTESIAN_POINT('Ctrl Pts',(-6.56268467749999,67.5862500034686,-7.93749999999999));
#26629=CARTESIAN_POINT('Ctrl Pts',(-6.56268467749991,67.4592500034685,-10.0698455118856));
#26630=CARTESIAN_POINT('Ctrl Pts',(-5.30932343282153,67.3322500034686,-11.7949492688802));
#26631=CARTESIAN_POINT('Ctrl Pts',(-4.05596218814312,67.2052500034686,-13.5200530258749));
#26632=CARTESIAN_POINT('Ctrl Pts',(-2.02798109407154,67.0782500034687,-14.1789840269267));
#26633=CARTESIAN_POINT('Ctrl Pts',(0.,66.9512500034685,-14.8379150279786));
#26634=CARTESIAN_POINT('Ctrl Pts',(2.02798109407154,66.8242500034687,-14.1789840269267));
#26635=CARTESIAN_POINT('Ctrl Pts',(4.05596218814318,66.6972500034686,-13.5200530258749));
#26636=CARTESIAN_POINT('Ctrl Pts',(5.30932343282153,66.5702500034686,-11.7949492688802));
#26637=CARTESIAN_POINT('Ctrl Pts',(6.56268467750003,66.4432500034685,-10.0698455118856));
#26638=CARTESIAN_POINT('Ctrl Pts',(6.56268467749999,66.3162500034687,-7.93749999999999));
#26639=CARTESIAN_POINT('Ctrl Pts',(6.56268467749997,66.1892500034686,-5.80515448811441));
#26640=CARTESIAN_POINT('Ctrl Pts',(5.30932343282159,66.0622500034686,-4.08005073111967));
#26641=CARTESIAN_POINT('Ctrl Pts',(4.05596218814318,65.9352500034686,-2.35494697412514));
#26642=CARTESIAN_POINT('Ctrl Pts',(2.02798109407148,65.8082500034686,-1.69601597307328));
#26643=CARTESIAN_POINT('Ctrl Pts',(5.83678785436452E-14,65.6812500034686,
-1.0370849720215));
#26644=CARTESIAN_POINT('Ctrl Pts',(-2.0279810940716,65.5542500034686,-1.69601597307328));
#26645=CARTESIAN_POINT('Ctrl Pts',(-4.05596218814318,65.4272500034686,-2.35494697412514));
#26646=CARTESIAN_POINT('Ctrl Pts',(-5.30932343282153,65.3002500034686,-4.08005073111967));
#26647=CARTESIAN_POINT('Ctrl Pts',(-6.56268467749997,65.1732500034685,-5.80515448811441));
#26648=CARTESIAN_POINT('Ctrl Pts',(-6.56268467749999,65.0462500034685,-7.93749999999999));
#26649=CARTESIAN_POINT('Ctrl Pts',(-6.56268467750003,64.9192500034685,-10.0698455118856));
#26650=CARTESIAN_POINT('Ctrl Pts',(-5.30932343282159,64.7922500034686,-11.7949492688802));
#26651=CARTESIAN_POINT('Ctrl Pts',(-4.05596218814306,64.6652500034686,-13.5200530258749));
#26652=CARTESIAN_POINT('Ctrl Pts',(-2.02798109407154,64.5382500034687,-14.1789840269267));
#26653=CARTESIAN_POINT('Ctrl Pts',(1.1673575708729E-13,64.4112500034686,
-14.8379150279786));
#26654=CARTESIAN_POINT('Ctrl Pts',(2.0279810940716,64.2842500034687,-14.1789840269267));
#26655=CARTESIAN_POINT('Ctrl Pts',(4.05596218814324,64.1572500034685,-13.5200530258749));
#26656=CARTESIAN_POINT('Ctrl Pts',(5.30932343282159,64.0302500034686,-11.7949492688802));
#26657=CARTESIAN_POINT('Ctrl Pts',(6.56268467750003,63.9032500034685,-10.0698455118856));
#26658=CARTESIAN_POINT('Ctrl Pts',(6.56268467749999,63.7762500034686,-7.93749999999999));
#26659=CARTESIAN_POINT('Ctrl Pts',(6.56268467750008,63.6492500034686,-5.80515448811441));
#26660=CARTESIAN_POINT('Ctrl Pts',(5.30932343282159,63.5222500034686,-4.08005073111967));
#26661=CARTESIAN_POINT('Ctrl Pts',(4.05596218814318,63.3952500034686,-2.35494697412514));
#26662=CARTESIAN_POINT('Ctrl Pts',(2.02798109407154,63.2682500034685,-1.69601597307328));
#26663=CARTESIAN_POINT('Ctrl Pts',(0.,63.1412500034685,-1.0370849720215));
#26664=CARTESIAN_POINT('Ctrl Pts',(-2.02798109407154,63.0142500034686,-1.69601597307328));
#26665=CARTESIAN_POINT('Ctrl Pts',(-4.05596218814318,62.8872500034686,-2.35494697412514));
#26666=CARTESIAN_POINT('Ctrl Pts',(-5.30932343282164,62.7602500034687,-4.08005073111967));
#26667=CARTESIAN_POINT('Ctrl Pts',(-6.56268467749997,62.6332500034685,-5.80515448811441));
#26668=CARTESIAN_POINT('Ctrl Pts',(-6.56268467749999,62.5062500034685,-7.93749999999999));
#26669=CARTESIAN_POINT('Ctrl Pts',(-6.56268467750003,62.3792500034687,-10.0698455118856));
#26670=CARTESIAN_POINT('Ctrl Pts',(-5.30932343282159,62.2522500034686,-11.7949492688802));
#26671=CARTESIAN_POINT('Ctrl Pts',(-4.05596218814318,62.1252500034685,-13.5200530258749));
#26672=CARTESIAN_POINT('Ctrl Pts',(-2.02798109407148,61.9982500034687,-14.1789840269267));
#26673=CARTESIAN_POINT('Ctrl Pts',(0.,61.8712500034686,-14.8379150279786));
#26674=CARTESIAN_POINT('Ctrl Pts',(2.0279810940716,61.7442500034687,-14.1789840269267));
#26675=CARTESIAN_POINT('Ctrl Pts',(4.05596218814312,61.6172500034686,-13.5200530258749));
#26676=CARTESIAN_POINT('Ctrl Pts',(5.30932343282159,61.4902500034686,-11.7949492688802));
#26677=CARTESIAN_POINT('Ctrl Pts',(6.56268467749991,61.3632500034686,-10.0698455118856));
#26678=CARTESIAN_POINT('Ctrl Pts',(6.56268467749993,61.2362500034686,-7.93749999999999));
#26679=CARTESIAN_POINT('Ctrl Pts',(6.56268467750003,61.1092500034686,-5.80515448811441));
#26680=CARTESIAN_POINT('Ctrl Pts',(5.30932343282159,60.9822500034687,-4.08005073111967));
#26681=CARTESIAN_POINT('Ctrl Pts',(4.05596218814306,60.8552500034686,-2.35494697412514));
#26682=CARTESIAN_POINT('Ctrl Pts',(2.02798109407154,60.7282500034685,-1.69601597307328));
#26683=CARTESIAN_POINT('Ctrl Pts',(0.,60.6012500034686,-1.0370849720215));
#26684=CARTESIAN_POINT('Ctrl Pts',(-2.02798109407154,60.4742500034686,-1.69601597307317));
#26685=CARTESIAN_POINT('Ctrl Pts',(-4.05596218814312,60.3472500034685,-2.35494697412514));
#26686=CARTESIAN_POINT('Ctrl Pts',(-5.30932343282159,60.2202500034686,-4.08005073111967));
#26687=CARTESIAN_POINT('Ctrl Pts',(-6.56268467749997,60.0932500034686,-5.80515448811441));
#26688=CARTESIAN_POINT('Ctrl Pts',(-6.56268467749999,59.9662500034687,-7.93749999999999));
#26689=CARTESIAN_POINT('Ctrl Pts',(-6.56268467750003,59.8392500034686,-10.0698455118856));
#26690=CARTESIAN_POINT('Ctrl Pts',(-5.30932343282159,59.7122500034685,-11.7949492688802));
#26691=CARTESIAN_POINT('Ctrl Pts',(-4.05596218814306,59.5852500034686,-13.5200530258749));
#26692=CARTESIAN_POINT('Ctrl Pts',(-2.02798109407148,59.4582500034687,-14.1789840269267));
#26693=CARTESIAN_POINT('Ctrl Pts',(1.1673575708729E-13,59.3312500034686,
-14.8379150279786));
#26694=CARTESIAN_POINT('Ctrl Pts',(2.02798109407148,59.2042500034687,-14.1789840269267));
#26695=CARTESIAN_POINT('Ctrl Pts',(4.05596218814324,59.0772500034685,-13.5200530258749));
#26696=CARTESIAN_POINT('Ctrl Pts',(5.30932343282159,58.9502500034686,-11.7949492688802));
#26697=CARTESIAN_POINT('Ctrl Pts',(6.56268467750008,58.8232500034686,-10.0698455118856));
#26698=CARTESIAN_POINT('Ctrl Pts',(6.56268467749999,58.6962500034686,-7.93749999999999));
#26699=CARTESIAN_POINT('Ctrl Pts',(6.56268467750003,58.5692500034686,-5.80515448811441));
#26700=CARTESIAN_POINT('Ctrl Pts',(5.30932343282159,58.4422500034686,-4.08005073111967));
#26701=CARTESIAN_POINT('Ctrl Pts',(4.05596218814312,58.3152500034686,-2.35494697412514));
#26702=CARTESIAN_POINT('Ctrl Pts',(2.02798109407154,58.1882500034687,-1.69601597307328));
#26703=CARTESIAN_POINT('Ctrl Pts',(5.83678785436452E-14,58.0612500034686,
-1.0370849720215));
#26704=CARTESIAN_POINT('Ctrl Pts',(-2.02798109407154,57.9342500034686,-1.69601597307317));
#26705=CARTESIAN_POINT('Ctrl Pts',(-4.05596218814312,57.8072500034686,-2.35494697412514));
#26706=CARTESIAN_POINT('Ctrl Pts',(-5.30932343282159,57.6802500034686,-4.08005073111967));
#26707=CARTESIAN_POINT('Ctrl Pts',(-6.56268467750003,57.5532500034687,-5.80515448811441));
#26708=CARTESIAN_POINT('Ctrl Pts',(-6.56268467749993,57.4262500034687,-7.93749999999999));
#26709=CARTESIAN_POINT('Ctrl Pts',(-6.56268467749997,57.2992500034685,-10.0698455118856));
#26710=CARTESIAN_POINT('Ctrl Pts',(-5.30932343282159,57.1722500034686,-11.7949492688802));
#26711=CARTESIAN_POINT('Ctrl Pts',(-4.05596218814312,57.0452500034685,-13.5200530258749));
#26712=CARTESIAN_POINT('Ctrl Pts',(-2.0279810940716,56.9182500034687,-14.1789840269267));
#26713=CARTESIAN_POINT('Ctrl Pts',(0.,56.7912500034686,-14.8379150279786));
#26714=CARTESIAN_POINT('Ctrl Pts',(2.02798109407154,56.6642500034688,-14.1789840269267));
#26715=CARTESIAN_POINT('Ctrl Pts',(4.05596218814312,56.5372500034686,-13.5200530258749));
#26716=CARTESIAN_POINT('Ctrl Pts',(5.30932343282159,56.4102500034686,-11.7949492688802));
#26717=CARTESIAN_POINT('Ctrl Pts',(6.56268467750008,56.2832500034686,-10.0698455118856));
#26718=CARTESIAN_POINT('Ctrl Pts',(6.56268467749999,56.1562500034686,-7.93749999999999));
#26719=CARTESIAN_POINT('Ctrl Pts',(6.56268467750003,56.0292500034686,-5.80515448811441));
#26720=CARTESIAN_POINT('Ctrl Pts',(5.30932343282164,55.9022500034686,-4.08005073111967));
#26721=CARTESIAN_POINT('Ctrl Pts',(4.05596218814324,55.7752500034686,-2.35494697412514));
#26722=CARTESIAN_POINT('Ctrl Pts',(2.0279810940716,55.6482500034686,-1.69601597307317));
#26723=CARTESIAN_POINT('Ctrl Pts',(0.,55.5212500034686,-1.0370849720215));
#26724=CARTESIAN_POINT('Ctrl Pts',(-2.02798109407148,55.3942500034686,-1.69601597307317));
#26725=CARTESIAN_POINT('Ctrl Pts',(-4.05596218814312,55.2672500034686,-2.35494697412514));
#26726=CARTESIAN_POINT('Ctrl Pts',(-5.30932343282159,55.1402500034686,-4.08005073111967));
#26727=CARTESIAN_POINT('Ctrl Pts',(-6.56268467749991,55.0132500034686,-5.80515448811441));
#26728=CARTESIAN_POINT('Ctrl Pts',(-6.56268467749987,54.8862500034686,-7.93750000000004));
#26729=CARTESIAN_POINT('Ctrl Pts',(-6.56268467749997,54.7592500034686,-10.0698455118856));
#26730=CARTESIAN_POINT('Ctrl Pts',(-5.30932343282153,54.6322500034687,-11.7949492688803));
#26731=CARTESIAN_POINT('Ctrl Pts',(-4.05596218814312,54.5052500034686,-13.5200530258749));
#26732=CARTESIAN_POINT('Ctrl Pts',(-2.02798109407154,54.3782500034687,-14.1789840269267));
#26733=CARTESIAN_POINT('Ctrl Pts',(0.,54.2512500034685,-14.8379150279786));
#26734=CARTESIAN_POINT('Ctrl Pts',(2.02798109407154,54.1242500034687,-14.1789840269267));
#26735=CARTESIAN_POINT('Ctrl Pts',(4.05596218814312,53.9972500034686,-13.5200530258749));
#26736=CARTESIAN_POINT('Ctrl Pts',(5.30932343282164,53.8702500034687,-11.7949492688803));
#26737=CARTESIAN_POINT('Ctrl Pts',(6.56268467749997,53.7432500034685,-10.0698455118856));
#26738=CARTESIAN_POINT('Ctrl Pts',(6.56268467749999,53.6162500034686,-7.93750000000004));
#26739=CARTESIAN_POINT('Ctrl Pts',(6.56268467750003,53.4892500034685,-5.80515448811441));
#26740=CARTESIAN_POINT('Ctrl Pts',(5.30932343282159,53.3622500034686,-4.08005073111972));
#26741=CARTESIAN_POINT('Ctrl Pts',(4.05596218814312,53.2352500034685,-2.35494697412514));
#26742=CARTESIAN_POINT('Ctrl Pts',(2.0279810940716,53.1082500034686,-1.69601597307323));
#26743=CARTESIAN_POINT('Ctrl Pts',(0.,52.9812500034685,-1.0370849720215));
#26744=CARTESIAN_POINT('Ctrl Pts',(-2.02798109407148,52.8542500034686,-1.69601597307323));
#26745=CARTESIAN_POINT('Ctrl Pts',(-4.05596218814312,52.7272500034686,-2.35494697412514));
#26746=CARTESIAN_POINT('Ctrl Pts',(-5.30932343282159,52.6002500034685,-4.08005073111972));
#26747=CARTESIAN_POINT('Ctrl Pts',(-6.56268467750003,52.4732500034686,-5.80515448811441));
#26748=CARTESIAN_POINT('Ctrl Pts',(-6.56268467749999,52.3462500034686,-7.93750000000004));
#26749=CARTESIAN_POINT('Ctrl Pts',(-6.56268467749997,52.2192500034685,-10.0698455118856));
#26750=CARTESIAN_POINT('Ctrl Pts',(-5.30932343282153,52.0922500034686,-11.7949492688803));
#26751=CARTESIAN_POINT('Ctrl Pts',(-4.05596218814312,51.9652500034685,-13.5200530258749));
#26752=CARTESIAN_POINT('Ctrl Pts',(-2.02798109407154,51.8382500034687,-14.1789840269267));
#26753=CARTESIAN_POINT('Ctrl Pts',(0.,51.7112500034685,-14.8379150279786));
#26754=CARTESIAN_POINT('Ctrl Pts',(2.02798109407154,51.5842500034687,-14.1789840269267));
#26755=CARTESIAN_POINT('Ctrl Pts',(4.05596218814312,51.4572500034686,-13.5200530258749));
#26756=CARTESIAN_POINT('Ctrl Pts',(5.30932343282164,51.3302500034686,-11.7949492688803));
#26757=CARTESIAN_POINT('Ctrl Pts',(6.56268467750008,51.2032500034686,-10.0698455118856));
#26758=CARTESIAN_POINT('Ctrl Pts',(6.56268467749999,51.0762500034687,-7.93750000000004));
#26759=CARTESIAN_POINT('Ctrl Pts',(6.56268467749997,50.9492500034685,-5.80515448811441));
#26760=CARTESIAN_POINT('Ctrl Pts',(5.30932343282159,50.8222500034686,-4.08005073111972));
#26761=CARTESIAN_POINT('Ctrl Pts',(4.05596218814312,50.6952500034686,-2.35494697412514));
#26762=CARTESIAN_POINT('Ctrl Pts',(2.0279810940716,50.5682500034686,-1.69601597307323));
#26763=CARTESIAN_POINT('Ctrl Pts',(0.,50.4412500034686,-1.0370849720215));
#26764=CARTESIAN_POINT('Ctrl Pts',(-2.0279810940716,50.3142500034687,-1.69601597307323));
#26765=CARTESIAN_POINT('Ctrl Pts',(-4.05596218814312,50.1872500034686,-2.35494697412514));
#26766=CARTESIAN_POINT('Ctrl Pts',(-5.30932343282153,50.0602500034686,-4.08005073111972));
#26767=CARTESIAN_POINT('Ctrl Pts',(-6.56268467750003,49.9332500034686,-5.80515448811441));
#26768=CARTESIAN_POINT('Ctrl Pts',(-6.56268467749999,49.8062500034686,-7.93750000000004));
#26769=CARTESIAN_POINT('Ctrl Pts',(-6.56268467749997,49.6792500034685,-10.0698455118856));
#26770=CARTESIAN_POINT('Ctrl Pts',(-5.30932343282159,49.5522500034686,-11.7949492688803));
#26771=CARTESIAN_POINT('Ctrl Pts',(-4.05596218814312,49.4252500034686,-13.5200530258749));
#26772=CARTESIAN_POINT('Ctrl Pts',(-2.02798109407154,49.2982500034686,-14.1789840269267));
#26773=CARTESIAN_POINT('Ctrl Pts',(0.,49.1712500034685,-14.8379150279786));
#26774=CARTESIAN_POINT('Ctrl Pts',(2.0279810940716,49.0442500034687,-14.1789840269267));
#26775=CARTESIAN_POINT('Ctrl Pts',(4.05596218814318,48.9172500034685,-13.5200530258749));
#26776=CARTESIAN_POINT('Ctrl Pts',(5.30932343282159,48.7902500034686,-11.7949492688803));
#26777=CARTESIAN_POINT('Ctrl Pts',(6.56268467750003,48.6632500034685,-10.0698455118856));
#26778=CARTESIAN_POINT('Ctrl Pts',(6.56268467750004,48.5362500034686,-7.93750000000004));
#26779=CARTESIAN_POINT('Ctrl Pts',(6.56268467750008,48.4092500034685,-5.80515448811441));
#26780=CARTESIAN_POINT('Ctrl Pts',(5.30932343282159,48.2822500034686,-4.08005073111972));
#26781=CARTESIAN_POINT('Ctrl Pts',(4.05596218814312,48.1552500034686,-2.35494697412514));
#26782=CARTESIAN_POINT('Ctrl Pts',(2.02798109407154,48.0282500034685,-1.69601597307323));
#26783=CARTESIAN_POINT('Ctrl Pts',(0.,47.9012500034685,-1.0370849720215));
#26784=CARTESIAN_POINT('Ctrl Pts',(-2.02798109407154,47.7742500034686,-1.69601597307323));
#26785=CARTESIAN_POINT('Ctrl Pts',(-4.05596218814318,47.6472500034685,-2.35494697412514));
#26786=CARTESIAN_POINT('Ctrl Pts',(-5.30932343282153,47.5202500034686,-4.08005073111972));
#26787=CARTESIAN_POINT('Ctrl Pts',(-6.56268467750003,47.3932500034686,-5.80515448811441));
#26788=CARTESIAN_POINT('Ctrl Pts',(-6.56268467749999,47.2662500034685,-7.93750000000004));
#26789=CARTESIAN_POINT('Ctrl Pts',(-6.56268467750003,47.1392500034685,-10.0698455118856));
#26790=CARTESIAN_POINT('Ctrl Pts',(-5.30932343282159,47.0122500034686,-11.7949492688803));
#26791=CARTESIAN_POINT('Ctrl Pts',(-4.05596218814324,46.8852500034686,-13.5200530258749));
#26792=CARTESIAN_POINT('Ctrl Pts',(-2.02798109407148,46.7582500034687,-14.1789840269267));
#26793=CARTESIAN_POINT('Ctrl Pts',(-1.1673575708729E-13,46.6312500034685,
-14.8379150279786));
#26794=CARTESIAN_POINT('Ctrl Pts',(2.0279810940716,46.5042500034687,-14.1789840269267));
#26795=CARTESIAN_POINT('Ctrl Pts',(4.05596218814318,46.3772500034685,-13.5200530258749));
#26796=CARTESIAN_POINT('Ctrl Pts',(5.30932343282159,46.2502500034686,-11.7949492688803));
#26797=CARTESIAN_POINT('Ctrl Pts',(6.56268467750003,46.1232500034686,-10.0698455118856));
#26798=CARTESIAN_POINT('Ctrl Pts',(6.56268467749993,45.9962500034686,-7.93750000000004));
#26799=CARTESIAN_POINT('Ctrl Pts',(6.56268467750008,45.8692500034686,-5.80515448811441));
#26800=CARTESIAN_POINT('Ctrl Pts',(5.30932343282159,45.7422500034685,-4.08005073111972));
#26801=CARTESIAN_POINT('Ctrl Pts',(4.05596218814318,45.6152500034686,-2.35494697412514));
#26802=CARTESIAN_POINT('Ctrl Pts',(2.02798109407154,45.4882500034685,-1.69601597307323));
#26803=CARTESIAN_POINT('Ctrl Pts',(-1.1673575708729E-13,45.3612500034685,
-1.0370849720215));
#26804=CARTESIAN_POINT('Ctrl Pts',(-2.02798109407154,45.2342500034686,-1.69601597307323));
#26805=CARTESIAN_POINT('Ctrl Pts',(-4.05596218814306,45.1072500034685,-2.35494697412514));
#26806=CARTESIAN_POINT('Ctrl Pts',(-5.30932343282159,44.9802500034686,-4.08005073111972));
#26807=CARTESIAN_POINT('Ctrl Pts',(-6.56268467749997,44.8532500034685,-5.80515448811441));
#26808=CARTESIAN_POINT('Ctrl Pts',(-6.56268467749993,44.7262500034686,-7.93750000000004));
#26809=CARTESIAN_POINT('Ctrl Pts',(-6.56268467749991,44.5992500034686,-10.0698455118856));
#26810=CARTESIAN_POINT('Ctrl Pts',(-5.30932343282159,44.4722500034685,-11.7949492688803));
#26811=CARTESIAN_POINT('Ctrl Pts',(-4.05596218814306,44.3452500034686,-13.5200530258749));
#26812=CARTESIAN_POINT('Ctrl Pts',(-2.02798109407148,44.2182500034687,-14.1789840269267));
#26813=CARTESIAN_POINT('Ctrl Pts',(0.,44.0912500034687,-14.8379150279786));
#26814=CARTESIAN_POINT('Ctrl Pts',(2.0279810940716,43.9642500034687,-14.1789840269267));
#26815=CARTESIAN_POINT('Ctrl Pts',(4.05596218814318,43.8372500034685,-13.5200530258749));
#26816=CARTESIAN_POINT('Ctrl Pts',(5.30932343282159,43.7102500034686,-11.7949492688803));
#26817=CARTESIAN_POINT('Ctrl Pts',(6.56268467750003,43.5832500034686,-10.0698455118856));
#26818=CARTESIAN_POINT('Ctrl Pts',(6.56268467749999,43.4562500034686,-7.93750000000004));
#26819=CARTESIAN_POINT('Ctrl Pts',(6.56268467749997,43.3292500034686,-5.80515448811441));
#26820=CARTESIAN_POINT('Ctrl Pts',(5.30932343282164,43.2022500034686,-4.08005073111972));
#26821=CARTESIAN_POINT('Ctrl Pts',(4.05596218814306,43.0752500034686,-2.35494697412514));
#26822=CARTESIAN_POINT('Ctrl Pts',(2.02798109407154,42.9482500034687,-1.69601597307323));
#26823=CARTESIAN_POINT('Ctrl Pts',(1.1673575708729E-13,42.8212500034686,
-1.0370849720215));
#26824=CARTESIAN_POINT('Ctrl Pts',(-2.02798109407154,42.6942500034686,-1.69601597307323));
#26825=CARTESIAN_POINT('Ctrl Pts',(-4.05596218814318,42.5672500034685,-2.35494697412514));
#26826=CARTESIAN_POINT('Ctrl Pts',(-5.30932343282159,42.4402500034686,-4.08005073111972));
#26827=CARTESIAN_POINT('Ctrl Pts',(-6.56268467749997,42.3132500034686,-5.80515448811441));
#26828=CARTESIAN_POINT('Ctrl Pts',(-6.56268467749993,42.1862500034687,-7.93750000000004));
#26829=CARTESIAN_POINT('Ctrl Pts',(-6.56268467750003,42.0592500034685,-10.0698455118856));
#26830=CARTESIAN_POINT('Ctrl Pts',(-5.30932343282159,41.9322500034685,-11.7949492688803));
#26831=CARTESIAN_POINT('Ctrl Pts',(-4.05596218814306,41.8052500034685,-13.5200530258749));
#26832=CARTESIAN_POINT('Ctrl Pts',(-2.02798109407148,41.6782500034687,-14.1789840269267));
#26833=CARTESIAN_POINT('Ctrl Pts',(1.1673575708729E-13,41.5512500034686,
-14.8379150279786));
#26834=CARTESIAN_POINT('Ctrl Pts',(2.02798109407154,41.4242500034688,-14.1789840269267));
#26835=CARTESIAN_POINT('Ctrl Pts',(4.05596218814324,41.2972500034684,-13.5200530258749));
#26836=CARTESIAN_POINT('Ctrl Pts',(5.30932343282159,41.1702500034686,-11.7949492688803));
#26837=CARTESIAN_POINT('Ctrl Pts',(6.56268467750003,41.0432500034686,-10.0698455118856));
#26838=CARTESIAN_POINT('Ctrl Pts',(6.56268467749999,40.9162500034685,-7.93750000000004));
#26839=CARTESIAN_POINT('Ctrl Pts',(6.56268467750014,40.7892500034686,-5.80515448811441));
#26840=CARTESIAN_POINT('Ctrl Pts',(5.30932343282164,40.6622500034686,-4.08005073111972));
#26841=CARTESIAN_POINT('Ctrl Pts',(4.05596218814318,40.5352500034686,-2.35494697412514));
#26842=CARTESIAN_POINT('Ctrl Pts',(2.0279810940716,40.4082500034686,-1.69601597307323));
#26843=CARTESIAN_POINT('Ctrl Pts',(0.,40.2812500034686,-1.0370849720215));
#26844=CARTESIAN_POINT('Ctrl Pts',(-2.02798109407148,40.1542500034686,-1.69601597307323));
#26845=CARTESIAN_POINT('Ctrl Pts',(-4.05596218814312,40.0272500034685,-2.35494697412514));
#26846=CARTESIAN_POINT('Ctrl Pts',(-5.30932343282159,39.9002500034686,-4.08005073111972));
#26847=CARTESIAN_POINT('Ctrl Pts',(-6.56268467749997,39.7732500034686,-5.80515448811441));
#26848=CARTESIAN_POINT('Ctrl Pts',(-6.56268467749987,39.6462500034686,-7.93750000000004));
#26849=CARTESIAN_POINT('Ctrl Pts',(-6.56268467750003,39.5192500034686,-10.0698455118856));
#26850=CARTESIAN_POINT('Ctrl Pts',(-5.30932343282153,39.3922500034687,-11.7949492688803));
#26851=CARTESIAN_POINT('Ctrl Pts',(-4.05596218814318,39.2652500034686,-13.5200530258749));
#26852=CARTESIAN_POINT('Ctrl Pts',(-2.02798109407154,39.1382500034687,-14.1789840269267));
#26853=CARTESIAN_POINT('Ctrl Pts',(0.,39.0112500034685,-14.8379150279786));
#26854=CARTESIAN_POINT('Ctrl Pts',(2.02798109407154,38.8842500034687,-14.1789840269267));
#26855=CARTESIAN_POINT('Ctrl Pts',(4.05596218814312,38.7572500034686,-13.5200530258749));
#26856=CARTESIAN_POINT('Ctrl Pts',(5.30932343282164,38.6302500034687,-11.7949492688803));
#26857=CARTESIAN_POINT('Ctrl Pts',(6.56268467749991,38.5032500034686,-10.0698455118856));
#26858=CARTESIAN_POINT('Ctrl Pts',(6.56268467749999,38.3762500034686,-7.93750000000004));
#26859=CARTESIAN_POINT('Ctrl Pts',(6.56268467750003,38.2492500034685,-5.80515448811441));
#26860=CARTESIAN_POINT('Ctrl Pts',(5.3093234328217,38.1222500034686,-4.08005073111972));
#26861=CARTESIAN_POINT('Ctrl Pts',(4.05596218814312,37.9952500034685,-2.35494697412514));
#26862=CARTESIAN_POINT('Ctrl Pts',(2.0279810940716,37.8682500034686,-1.69601597307323));
#26863=CARTESIAN_POINT('Ctrl Pts',(0.,37.7412500034685,-1.0370849720215));
#26864=CARTESIAN_POINT('Ctrl Pts',(-2.02798109407148,37.6142500034686,-1.69601597307323));
#26865=CARTESIAN_POINT('Ctrl Pts',(-4.05596218814312,37.4872500034686,-2.35494697412514));
#26866=CARTESIAN_POINT('Ctrl Pts',(-5.30932343282153,37.3602500034685,-4.08005073111972));
#26867=CARTESIAN_POINT('Ctrl Pts',(-6.56268467749997,37.2332500034686,-5.80515448811441));
#26868=CARTESIAN_POINT('Ctrl Pts',(-6.56268467749999,37.1062500034686,-7.93750000000004));
#26869=CARTESIAN_POINT('Ctrl Pts',(-6.56268467749997,36.9792500034686,-10.0698455118856));
#26870=CARTESIAN_POINT('Ctrl Pts',(-5.30932343282153,36.8522500034686,-11.7949492688803));
#26871=CARTESIAN_POINT('Ctrl Pts',(-4.05596218814306,36.7252500034685,-13.5200530258749));
#26872=CARTESIAN_POINT('Ctrl Pts',(-2.02798109407154,36.5982500034687,-14.1789840269267));
#26873=CARTESIAN_POINT('Ctrl Pts',(1.1673575708729E-13,36.4712500034686,
-14.8379150279786));
#26874=CARTESIAN_POINT('Ctrl Pts',(2.02798109407154,36.3442500034687,-14.1789840269267));
#26875=CARTESIAN_POINT('Ctrl Pts',(4.05596218814324,36.2172500034686,-13.5200530258749));
#26876=CARTESIAN_POINT('Ctrl Pts',(5.30932343282164,36.0902500034686,-11.7949492688803));
#26877=CARTESIAN_POINT('Ctrl Pts',(6.56268467750008,35.9632500034686,-10.0698455118856));
#26878=CARTESIAN_POINT('Ctrl Pts',(6.56268467749999,35.8362500034687,-7.93750000000004));
#26879=CARTESIAN_POINT('Ctrl Pts',(6.56268467750003,35.7092500034686,-5.80515448811441));
#26880=CARTESIAN_POINT('Ctrl Pts',(5.30932343282159,35.5822500034686,-4.08005073111972));
#26881=CARTESIAN_POINT('Ctrl Pts',(4.05596218814312,35.4552500034686,-2.35494697412514));
#26882=CARTESIAN_POINT('Ctrl Pts',(2.0279810940716,35.3282500034686,-1.69601597307323));
#26883=CARTESIAN_POINT('Ctrl Pts',(5.83678785436452E-14,35.2012500034686,
-1.0370849720215));
#26884=CARTESIAN_POINT('Ctrl Pts',(-2.02798109407148,35.0742500034686,-1.69601597307323));
#26885=CARTESIAN_POINT('Ctrl Pts',(-4.05596218814312,34.9472500034686,-2.35494697412514));
#26886=CARTESIAN_POINT('Ctrl Pts',(-5.30932343282153,34.8202500034686,-4.08005073111972));
#26887=CARTESIAN_POINT('Ctrl Pts',(-6.56268467750003,34.6932500034686,-5.80515448811441));
#26888=CARTESIAN_POINT('Ctrl Pts',(-6.56268467749999,34.5662500034686,-7.93750000000004));
#26889=CARTESIAN_POINT('Ctrl Pts',(-6.56268467749997,34.4392500034686,-10.0698455118856));
#26890=CARTESIAN_POINT('Ctrl Pts',(-5.30932343282148,34.3122500034686,-11.7949492688803));
#26891=CARTESIAN_POINT('Ctrl Pts',(-4.05596218814312,34.1852500034684,-13.5200530258749));
#26892=CARTESIAN_POINT('Ctrl Pts',(-2.02798109407154,34.0582500034686,-14.1789840269267));
#26893=CARTESIAN_POINT('Ctrl Pts',(0.,33.9312500034685,-14.8379150279786));
#26894=CARTESIAN_POINT('Ctrl Pts',(2.0279810940716,33.8042500034687,-14.1789840269267));
#26895=CARTESIAN_POINT('Ctrl Pts',(4.05596218814312,33.6772500034686,-13.5200530258749));
#26896=CARTESIAN_POINT('Ctrl Pts',(5.30932343282164,33.5502500034686,-11.7949492688803));
#26897=CARTESIAN_POINT('Ctrl Pts',(6.56268467750008,33.4232500034685,-10.0698455118856));
#26898=CARTESIAN_POINT('Ctrl Pts',(6.56268467750004,33.2962500034686,-7.93750000000004));
#26899=CARTESIAN_POINT('Ctrl Pts',(6.56268467749991,33.1692500034685,-5.80515448811441));
#26900=CARTESIAN_POINT('Ctrl Pts',(5.30932343282159,33.0422500034686,-4.08005073111972));
#26901=CARTESIAN_POINT('Ctrl Pts',(4.05596218814324,32.9152500034685,-2.35494697412514));
#26902=CARTESIAN_POINT('Ctrl Pts',(2.02798109407165,32.7882500034686,-1.69601597307323));
#26903=CARTESIAN_POINT('Ctrl Pts',(0.,32.6612500034685,-1.0370849720215));
#26904=CARTESIAN_POINT('Ctrl Pts',(-2.02798109407154,32.5342500034686,-1.69601597307323));
#26905=CARTESIAN_POINT('Ctrl Pts',(-4.05596218814312,32.4072500034686,-2.35494697412514));
#26906=CARTESIAN_POINT('Ctrl Pts',(-5.30932343282148,32.2802500034686,-4.08005073111972));
#26907=CARTESIAN_POINT('Ctrl Pts',(-6.56268467749991,32.1532500034685,-5.80515448811441));
#26908=CARTESIAN_POINT('Ctrl Pts',(-6.56268467749999,32.0262500034685,-7.93750000000004));
#26909=CARTESIAN_POINT('Ctrl Pts',(-6.56268467749997,31.8992500034685,-10.0698455118856));
#26910=CARTESIAN_POINT('Ctrl Pts',(-5.30932343282159,31.7722500034686,-11.7949492688803));
#26911=CARTESIAN_POINT('Ctrl Pts',(-4.05596218814312,31.6452500034686,-13.5200530258749));
#26912=CARTESIAN_POINT('Ctrl Pts',(-2.02798109407148,31.5182500034687,-14.1789840269267));
#26913=CARTESIAN_POINT('Ctrl Pts',(0.,31.3912500034685,-14.8379150279786));
#26914=CARTESIAN_POINT('Ctrl Pts',(2.0279810940716,31.2642500034687,-14.1789840269267));
#26915=CARTESIAN_POINT('Ctrl Pts',(4.05596218814312,31.1372500034686,-13.5200530258749));
#26916=CARTESIAN_POINT('Ctrl Pts',(5.30932343282159,31.0102500034686,-11.7949492688803));
#26917=CARTESIAN_POINT('Ctrl Pts',(6.56268467749997,30.8832500034686,-10.0698455118856));
#26918=CARTESIAN_POINT('Ctrl Pts',(6.56268467750004,30.7562500034686,-7.93750000000004));
#26919=CARTESIAN_POINT('Ctrl Pts',(6.56268467750003,30.6292500034685,-5.80515448811441));
#26920=CARTESIAN_POINT('Ctrl Pts',(5.30932343282159,30.5022500034686,-4.08005073111972));
#26921=CARTESIAN_POINT('Ctrl Pts',(4.05596218814312,30.3752500034686,-2.35494697412514));
#26922=CARTESIAN_POINT('Ctrl Pts',(2.02798109407154,30.2482500034685,-1.69601597307323));
#26923=CARTESIAN_POINT('Ctrl Pts',(0.,30.1212500034685,-1.0370849720215));
#26924=CARTESIAN_POINT('Ctrl Pts',(-2.02798109407154,29.9942500034686,-1.69601597307323));
#26925=CARTESIAN_POINT('Ctrl Pts',(-4.05596218814312,29.8672500034686,-2.35494697412503));
#26926=CARTESIAN_POINT('Ctrl Pts',(-5.30932343282148,29.7402500034687,-4.08005073111972));
#26927=CARTESIAN_POINT('Ctrl Pts',(-6.56268467750003,29.6132500034685,-5.80515448811441));
#26928=CARTESIAN_POINT('Ctrl Pts',(-6.56268467749993,29.4862500034685,-7.93750000000004));
#26929=CARTESIAN_POINT('Ctrl Pts',(-6.56268467749997,29.3592500034685,-10.0698455118856));
#26930=CARTESIAN_POINT('Ctrl Pts',(-5.30932343282159,29.2322500034685,-11.7949492688803));
#26931=CARTESIAN_POINT('Ctrl Pts',(-4.05596218814312,29.1052500034686,-13.5200530258749));
#26932=CARTESIAN_POINT('Ctrl Pts',(-2.02798109407148,28.9782500034687,-14.1789840269267));
#26933=CARTESIAN_POINT('Ctrl Pts',(0.,28.8512500034685,-14.8379150279786));
#26934=CARTESIAN_POINT('Ctrl Pts',(2.0279810940716,28.7242500034687,-14.1789840269267));
#26935=CARTESIAN_POINT('Ctrl Pts',(4.05596218814318,28.5972500034685,-13.5200530258749));
#26936=CARTESIAN_POINT('Ctrl Pts',(5.30932343282159,28.4702500034686,-11.7949492688803));
#26937=CARTESIAN_POINT('Ctrl Pts',(6.56268467750008,28.3432500034685,-10.0698455118856));
#26938=CARTESIAN_POINT('Ctrl Pts',(6.56268467749999,28.2162500034686,-7.93750000000004));
#26939=CARTESIAN_POINT('Ctrl Pts',(6.56268467749997,28.0892500034686,-5.80515448811441));
#26940=CARTESIAN_POINT('Ctrl Pts',(5.30932343282164,27.9622500034686,-4.08005073111972));
#26941=CARTESIAN_POINT('Ctrl Pts',(4.05596218814312,27.8352500034686,-2.35494697412514));
#26942=CARTESIAN_POINT('Ctrl Pts',(2.02798109407154,27.7082500034687,-1.69601597307323));
#26943=CARTESIAN_POINT('Ctrl Pts',(0.,27.5812500034685,-1.0370849720215));
#26944=CARTESIAN_POINT('Ctrl Pts',(-2.02798109407148,27.4542500034686,-1.69601597307323));
#26945=CARTESIAN_POINT('Ctrl Pts',(-4.05596218814312,27.3272500034686,-2.35494697412503));
#26946=CARTESIAN_POINT('Ctrl Pts',(-5.30932343282159,27.2002500034686,-4.08005073111972));
#26947=CARTESIAN_POINT('Ctrl Pts',(-6.56268467750003,27.0732500034685,-5.80515448811441));
#26948=CARTESIAN_POINT('Ctrl Pts',(-6.56268467749993,26.9462500034687,-7.93750000000004));
#26949=CARTESIAN_POINT('Ctrl Pts',(-6.56268467749991,26.8192500034686,-10.0698455118856));
#26950=CARTESIAN_POINT('Ctrl Pts',(-5.30932343282159,26.6922500034685,-11.7949492688803));
#26951=CARTESIAN_POINT('Ctrl Pts',(-4.05596218814312,26.5652500034685,-13.5200530258749));
#26952=CARTESIAN_POINT('Ctrl Pts',(-2.02798109407148,26.4382500034687,-14.1789840269267));
#26953=CARTESIAN_POINT('Ctrl Pts',(0.,26.3112500034686,-14.8379150279786));
#26954=CARTESIAN_POINT('Ctrl Pts',(2.02798109407165,26.1842500034687,-14.1789840269267));
#26955=CARTESIAN_POINT('Ctrl Pts',(4.05596218814318,26.0572500034686,-13.5200530258749));
#26956=CARTESIAN_POINT('Ctrl Pts',(5.30932343282159,25.9302500034686,-11.7949492688803));
#26957=CARTESIAN_POINT('Ctrl Pts',(6.56268467750003,25.8032500034686,-10.0698455118856));
#26958=CARTESIAN_POINT('Ctrl Pts',(6.56268467749999,25.6762500034685,-7.93750000000004));
#26959=CARTESIAN_POINT('Ctrl Pts',(6.56268467749997,25.5492500034686,-5.80515448811441));
#26960=CARTESIAN_POINT('Ctrl Pts',(5.30932343282164,25.4222500034686,-4.08005073111972));
#26961=CARTESIAN_POINT('Ctrl Pts',(4.05596218814312,25.2952500034686,-2.35494697412514));
#26962=CARTESIAN_POINT('Ctrl Pts',(2.0279810940716,25.1682500034687,-1.69601597307323));
#26963=CARTESIAN_POINT('Ctrl Pts',(0.,25.0412500034686,-1.0370849720215));
#26964=CARTESIAN_POINT('Ctrl Pts',(-2.02798109407148,24.9142500034685,-1.69601597307323));
#26965=CARTESIAN_POINT('Ctrl Pts',(-4.05596218814318,24.7872500034685,-2.35494697412503));
#26966=CARTESIAN_POINT('Ctrl Pts',(-5.30932343282159,24.6602500034686,-4.08005073111972));
#26967=CARTESIAN_POINT('Ctrl Pts',(-6.56268467750003,24.5332500034686,-5.80515448811441));
#26968=CARTESIAN_POINT('Ctrl Pts',(-6.56268467749987,24.4062500034686,-7.93750000000004));
#26969=CARTESIAN_POINT('Ctrl Pts',(-6.56268467750003,24.2792500034686,-10.0698455118856));
#26970=CARTESIAN_POINT('Ctrl Pts',(-5.30932343282153,24.1522500034687,-11.7949492688803));
#26971=CARTESIAN_POINT('Ctrl Pts',(-4.05596218814324,24.0252500034686,-13.5200530258749));
#26972=CARTESIAN_POINT('Ctrl Pts',(-2.02798109407154,23.8982500034687,-14.1789840269267));
#26973=CARTESIAN_POINT('Ctrl Pts',(0.,23.7712500034685,-14.8379150279786));
#26974=CARTESIAN_POINT('Ctrl Pts',(2.02798109407154,23.6442500034687,-14.1789840269267));
#26975=CARTESIAN_POINT('Ctrl Pts',(4.05596218814318,23.5172500034685,-13.5200530258749));
#26976=CARTESIAN_POINT('Ctrl Pts',(5.30932343282164,23.3902500034686,-11.7949492688803));
#26977=CARTESIAN_POINT('Ctrl Pts',(6.56268467750003,23.2632500034686,-10.0698455118856));
#26978=CARTESIAN_POINT('Ctrl Pts',(6.56268467749999,23.1362500034686,-7.93750000000004));
#26979=CARTESIAN_POINT('Ctrl Pts',(6.56268467750008,23.0092500034686,-5.80515448811441));
#26980=CARTESIAN_POINT('Ctrl Pts',(5.3093234328217,22.8822500034686,-4.08005073111972));
#26981=CARTESIAN_POINT('Ctrl Pts',(4.05596218814318,22.7552500034685,-2.35494697412503));
#26982=CARTESIAN_POINT('Ctrl Pts',(2.0279810940716,22.6282500034686,-1.69601597307323));
#26983=CARTESIAN_POINT('Ctrl Pts',(-1.1673575708729E-13,22.5012500034685,
-1.0370849720215));
#26984=CARTESIAN_POINT('Ctrl Pts',(-2.02798109407148,22.3742500034686,-1.69601597307323));
#26985=CARTESIAN_POINT('Ctrl Pts',(-4.05596218814306,22.2472500034686,-2.35494697412503));
#26986=CARTESIAN_POINT('Ctrl Pts',(-5.30932343282153,22.1202500034686,-4.08005073111972));
#26987=CARTESIAN_POINT('Ctrl Pts',(-6.56268467749997,21.9932500034685,-5.80515448811441));
#26988=CARTESIAN_POINT('Ctrl Pts',(-6.56268467749987,21.8662500034686,-7.93750000000004));
#26989=CARTESIAN_POINT('Ctrl Pts',(-6.56268467750003,21.7392500034685,-10.0698455118856));
#26990=CARTESIAN_POINT('Ctrl Pts',(-5.30932343282153,21.6122500034686,-11.7949492688803));
#26991=CARTESIAN_POINT('Ctrl Pts',(-4.05596218814318,21.4852500034685,-13.5200530258749));
#26992=CARTESIAN_POINT('Ctrl Pts',(-2.02798109407154,21.3582500034687,-14.1789840269267));
#26993=CARTESIAN_POINT('Ctrl Pts',(0.,21.2312500034686,-14.8379150279786));
#26994=CARTESIAN_POINT('Ctrl Pts',(2.02798109407154,21.1042500034687,-14.1789840269267));
#26995=CARTESIAN_POINT('Ctrl Pts',(4.05596218814312,20.9772500034686,-13.5200530258749));
#26996=CARTESIAN_POINT('Ctrl Pts',(5.30932343282164,20.8502500034686,-11.7949492688803));
#26997=CARTESIAN_POINT('Ctrl Pts',(6.56268467749991,20.7232500034686,-10.0698455118856));
#26998=CARTESIAN_POINT('Ctrl Pts',(6.56268467749999,20.5962500034686,-7.93750000000004));
#26999=CARTESIAN_POINT('Ctrl Pts',(6.56268467749997,20.4692500034686,-5.80515448811441));
#27000=CARTESIAN_POINT('Ctrl Pts',(5.3093234328217,20.3422500034686,-4.08005073111972));
#27001=CARTESIAN_POINT('Ctrl Pts',(4.65426917438044,20.2758749729855,-3.17844589287373));
#27002=CARTESIAN_POINT('Ctrl Pts',(3.73830600779964,20.2061014294359,-2.54362399397772));
#27003=CARTESIAN_POINT('Ctrl Pts',(0.0390188495637537,19.9243080309083,
0.0202220033661115));
#27004=CARTESIAN_POINT('Ctrl Pts',(-3.66026830867225,19.6425146323806,2.58406800071006));
#27005=CARTESIAN_POINT('Ctrl Pts',(-7.93751285522927,76.0000074219705,-7.93749999999999));
#27006=CARTESIAN_POINT('Ctrl Pts',(-7.93751285522931,75.8730074219702,-10.5165542657659));
#27007=CARTESIAN_POINT('Ctrl Pts',(-6.42158279295009,75.7460074219701,-12.6030529961856));
#27008=CARTESIAN_POINT('Ctrl Pts',(-4.905652730671,75.6190074219701,-14.6895517266055));
#27009=CARTESIAN_POINT('Ctrl Pts',(-2.45282636533548,75.4920074219701,-15.4865233241424));
#27010=CARTESIAN_POINT('Ctrl Pts',(5.83684243132838E-14,75.36500742197,
-16.2834949216793));
#27011=CARTESIAN_POINT('Ctrl Pts',(2.45282636533542,75.2380074219704,-15.4865233241424));
#27012=CARTESIAN_POINT('Ctrl Pts',(4.905652730671,75.11100742197,-14.6895517266055));
#27013=CARTESIAN_POINT('Ctrl Pts',(6.42158279295009,74.9840074219701,-12.6030529961856));
#27014=CARTESIAN_POINT('Ctrl Pts',(7.93751285522931,74.8570074219701,-10.5165542657659));
#27015=CARTESIAN_POINT('Ctrl Pts',(7.93751285522933,74.7300074219701,-7.93749999999999));
#27016=CARTESIAN_POINT('Ctrl Pts',(7.93751285522926,74.6030074219699,-5.35844573423412));
#27017=CARTESIAN_POINT('Ctrl Pts',(6.42158279295014,74.4760074219701,-3.27194700381432));
#27018=CARTESIAN_POINT('Ctrl Pts',(4.90565273067095,74.3490074219701,-1.18544827339454));
#27019=CARTESIAN_POINT('Ctrl Pts',(2.45282636533548,74.2220074219701,-0.388476675857597));
#27020=CARTESIAN_POINT('Ctrl Pts',(1.16736848626568E-13,74.09500742197,
0.408494921679244));
#27021=CARTESIAN_POINT('Ctrl Pts',(-2.45282636533548,73.9680074219701,-0.388476675857597));
#27022=CARTESIAN_POINT('Ctrl Pts',(-4.90565273067095,73.8410074219701,-1.18544827339454));
#27023=CARTESIAN_POINT('Ctrl Pts',(-6.42158279295014,73.7140074219701,-3.27194700381421));
#27024=CARTESIAN_POINT('Ctrl Pts',(-7.93751285522926,73.58700742197,-5.35844573423412));
#27025=CARTESIAN_POINT('Ctrl Pts',(-7.93751285522933,73.4600074219702,-7.93749999999999));
#27026=CARTESIAN_POINT('Ctrl Pts',(-7.93751285522931,73.33300742197,-10.5165542657659));
#27027=CARTESIAN_POINT('Ctrl Pts',(-6.42158279295009,73.2060074219702,-12.6030529961856));
#27028=CARTESIAN_POINT('Ctrl Pts',(-4.90565273067083,73.07900742197,-14.6895517266055));
#27029=CARTESIAN_POINT('Ctrl Pts',(-2.45282636533553,72.9520074219703,-15.4865233241424));
#27030=CARTESIAN_POINT('Ctrl Pts',(5.83684243132838E-14,72.82500742197,
-16.2834949216793));
#27031=CARTESIAN_POINT('Ctrl Pts',(2.45282636533548,72.6980074219702,-15.4865233241424));
#27032=CARTESIAN_POINT('Ctrl Pts',(4.90565273067089,72.5710074219701,-14.6895517266055));
#27033=CARTESIAN_POINT('Ctrl Pts',(6.42158279295014,72.4440074219703,-12.6030529961856));
#27034=CARTESIAN_POINT('Ctrl Pts',(7.93751285522931,72.3170074219701,-10.5165542657659));
#27035=CARTESIAN_POINT('Ctrl Pts',(7.93751285522939,72.1900074219701,-7.93749999999999));
#27036=CARTESIAN_POINT('Ctrl Pts',(7.93751285522931,72.0630074219699,-5.35844573423412));
#27037=CARTESIAN_POINT('Ctrl Pts',(6.4215827929502,71.93600742197,-3.27194700381432));
#27038=CARTESIAN_POINT('Ctrl Pts',(4.905652730671,71.80900742197,-1.18544827339454));
#27039=CARTESIAN_POINT('Ctrl Pts',(2.45282636533537,71.6820074219701,-0.388476675857597));
#27040=CARTESIAN_POINT('Ctrl Pts',(0.,71.55500742197,0.408494921679244));
#27041=CARTESIAN_POINT('Ctrl Pts',(-2.45282636533548,71.4280074219701,-0.388476675857597));
#27042=CARTESIAN_POINT('Ctrl Pts',(-4.90565273067095,71.3010074219701,-1.18544827339454));
#27043=CARTESIAN_POINT('Ctrl Pts',(-6.42158279295009,71.1740074219701,-3.27194700381421));
#27044=CARTESIAN_POINT('Ctrl Pts',(-7.93751285522926,71.0470074219702,-5.35844573423412));
#27045=CARTESIAN_POINT('Ctrl Pts',(-7.93751285522927,70.9200074219701,-7.93749999999999));
#27046=CARTESIAN_POINT('Ctrl Pts',(-7.9375128552292,70.7930074219701,-10.5165542657659));
#27047=CARTESIAN_POINT('Ctrl Pts',(-6.42158279295009,70.6660074219703,-12.6030529961856));
#27048=CARTESIAN_POINT('Ctrl Pts',(-4.90565273067095,70.5390074219701,-14.6895517266055));
#27049=CARTESIAN_POINT('Ctrl Pts',(-2.45282636533553,70.4120074219703,-15.4865233241424));
#27050=CARTESIAN_POINT('Ctrl Pts',(5.4576963861738E-19,70.2850074219701,
-16.2834949216793));
#27051=CARTESIAN_POINT('Ctrl Pts',(2.45282636533548,70.1580074219703,-15.4865233241424));
#27052=CARTESIAN_POINT('Ctrl Pts',(4.90565273067089,70.0310074219701,-14.6895517266055));
#27053=CARTESIAN_POINT('Ctrl Pts',(6.42158279295014,69.9040074219702,-12.6030529961856));
#27054=CARTESIAN_POINT('Ctrl Pts',(7.93751285522937,69.77700742197,-10.5165542657659));
#27055=CARTESIAN_POINT('Ctrl Pts',(7.93751285522939,69.6500074219702,-7.93749999999999));
#27056=CARTESIAN_POINT('Ctrl Pts',(7.93751285522931,69.5230074219701,-5.35844573423412));
#27057=CARTESIAN_POINT('Ctrl Pts',(6.4215827929502,69.39600742197,-3.27194700381432));
#27058=CARTESIAN_POINT('Ctrl Pts',(4.90565273067089,69.26900742197,-1.18544827339454));
#27059=CARTESIAN_POINT('Ctrl Pts',(2.45282636533542,69.14200742197,-0.388476675857597));
#27060=CARTESIAN_POINT('Ctrl Pts',(1.09153927723476E-18,69.0150074219701,
0.408494921679244));
#27061=CARTESIAN_POINT('Ctrl Pts',(-2.45282636533542,68.88800742197,-0.388476675857597));
#27062=CARTESIAN_POINT('Ctrl Pts',(-4.90565273067095,68.76100742197,-1.18544827339454));
#27063=CARTESIAN_POINT('Ctrl Pts',(-6.42158279295009,68.6340074219701,-3.27194700381421));
#27064=CARTESIAN_POINT('Ctrl Pts',(-7.93751285522937,68.5070074219701,-5.35844573423412));
#27065=CARTESIAN_POINT('Ctrl Pts',(-7.93751285522927,68.3800074219701,-7.93749999999999));
#27066=CARTESIAN_POINT('Ctrl Pts',(-7.93751285522926,68.25300742197,-10.5165542657659));
#27067=CARTESIAN_POINT('Ctrl Pts',(-6.42158279295009,68.1260074219703,-12.6030529961856));
#27068=CARTESIAN_POINT('Ctrl Pts',(-4.90565273067095,67.9990074219701,-14.6895517266055));
#27069=CARTESIAN_POINT('Ctrl Pts',(-2.45282636533548,67.8720074219703,-15.4865233241424));
#27070=CARTESIAN_POINT('Ctrl Pts',(1.16736848626568E-13,67.74500742197,
-16.2834949216793));
#27071=CARTESIAN_POINT('Ctrl Pts',(2.45282636533548,67.6180074219702,-15.4865233241424));
#27072=CARTESIAN_POINT('Ctrl Pts',(4.90565273067089,67.4910074219701,-14.6895517266055));
#27073=CARTESIAN_POINT('Ctrl Pts',(6.4215827929502,67.3640074219702,-12.6030529961856));
#27074=CARTESIAN_POINT('Ctrl Pts',(7.93751285522926,67.2370074219701,-10.5165542657659));
#27075=CARTESIAN_POINT('Ctrl Pts',(7.93751285522939,67.1100074219701,-7.93749999999999));
#27076=CARTESIAN_POINT('Ctrl Pts',(7.93751285522931,66.9830074219701,-5.35844573423412));
#27077=CARTESIAN_POINT('Ctrl Pts',(6.4215827929502,66.85600742197,-3.27194700381432));
#27078=CARTESIAN_POINT('Ctrl Pts',(4.905652730671,66.72900742197,-1.18544827339454));
#27079=CARTESIAN_POINT('Ctrl Pts',(2.45282636533542,66.6020074219701,-0.388476675857597));
#27080=CARTESIAN_POINT('Ctrl Pts',(-5.4576963861738E-19,66.4750074219701,
0.408494921679244));
#27081=CARTESIAN_POINT('Ctrl Pts',(-2.45282636533553,66.3480074219701,-0.388476675857597));
#27082=CARTESIAN_POINT('Ctrl Pts',(-4.90565273067089,66.2210074219701,-1.18544827339454));
#27083=CARTESIAN_POINT('Ctrl Pts',(-6.42158279295009,66.09400742197,-3.27194700381421));
#27084=CARTESIAN_POINT('Ctrl Pts',(-7.9375128552292,65.96700742197,-5.35844573423412));
#27085=CARTESIAN_POINT('Ctrl Pts',(-7.93751285522927,65.8400074219701,-7.93749999999999));
#27086=CARTESIAN_POINT('Ctrl Pts',(-7.93751285522926,65.7130074219699,-10.5165542657659));
#27087=CARTESIAN_POINT('Ctrl Pts',(-6.42158279295003,65.5860074219702,-12.6030529961856));
#27088=CARTESIAN_POINT('Ctrl Pts',(-4.90565273067095,65.45900742197,-14.6895517266055));
#27089=CARTESIAN_POINT('Ctrl Pts',(-2.45282636533548,65.3320074219702,-15.4865233241424));
#27090=CARTESIAN_POINT('Ctrl Pts',(-1.09153927723476E-18,65.20500742197,
-16.2834949216793));
#27091=CARTESIAN_POINT('Ctrl Pts',(2.45282636533537,65.0780074219702,-15.4865233241424));
#27092=CARTESIAN_POINT('Ctrl Pts',(4.90565273067095,64.9510074219701,-14.6895517266055));
#27093=CARTESIAN_POINT('Ctrl Pts',(6.4215827929502,64.8240074219702,-12.6030529961856));
#27094=CARTESIAN_POINT('Ctrl Pts',(7.93751285522937,64.6970074219701,-10.5165542657659));
#27095=CARTESIAN_POINT('Ctrl Pts',(7.93751285522927,64.5700074219701,-7.93749999999999));
#27096=CARTESIAN_POINT('Ctrl Pts',(7.93751285522931,64.4430074219701,-5.35844573423412));
#27097=CARTESIAN_POINT('Ctrl Pts',(6.42158279295009,64.3160074219702,-3.27194700381421));
#27098=CARTESIAN_POINT('Ctrl Pts',(4.90565273067089,64.1890074219699,-1.18544827339454));
#27099=CARTESIAN_POINT('Ctrl Pts',(2.45282636533548,64.0620074219701,-0.388476675857597));
#27100=CARTESIAN_POINT('Ctrl Pts',(0.,63.9350074219701,0.408494921679244));
#27101=CARTESIAN_POINT('Ctrl Pts',(-2.45282636533548,63.8080074219701,-0.388476675857597));
#27102=CARTESIAN_POINT('Ctrl Pts',(-4.90565273067089,63.68100742197,-1.18544827339454));
#27103=CARTESIAN_POINT('Ctrl Pts',(-6.42158279295009,63.5540074219701,-3.27194700381421));
#27104=CARTESIAN_POINT('Ctrl Pts',(-7.93751285522931,63.4270074219701,-5.35844573423412));
#27105=CARTESIAN_POINT('Ctrl Pts',(-7.93751285522927,63.3000074219701,-7.93749999999999));
#27106=CARTESIAN_POINT('Ctrl Pts',(-7.93751285522926,63.1730074219701,-10.5165542657659));
#27107=CARTESIAN_POINT('Ctrl Pts',(-6.42158279295003,63.0460074219702,-12.6030529961856));
#27108=CARTESIAN_POINT('Ctrl Pts',(-4.90565273067095,62.9190074219701,-14.6895517266055));
#27109=CARTESIAN_POINT('Ctrl Pts',(-2.45282636533548,62.7920074219702,-15.4865233241424));
#27110=CARTESIAN_POINT('Ctrl Pts',(0.,62.66500742197,-16.2834949216793));
#27111=CARTESIAN_POINT('Ctrl Pts',(2.45282636533542,62.5380074219702,-15.4865233241424));
#27112=CARTESIAN_POINT('Ctrl Pts',(4.90565273067095,62.41100742197,-14.6895517266055));
#27113=CARTESIAN_POINT('Ctrl Pts',(6.42158279295009,62.2840074219701,-12.6030529961856));
#27114=CARTESIAN_POINT('Ctrl Pts',(7.93751285522926,62.1570074219701,-10.5165542657659));
#27115=CARTESIAN_POINT('Ctrl Pts',(7.93751285522933,62.0300074219701,-7.93749999999999));
#27116=CARTESIAN_POINT('Ctrl Pts',(7.93751285522937,61.9030074219701,-5.35844573423412));
#27117=CARTESIAN_POINT('Ctrl Pts',(6.42158279295009,61.7760074219701,-3.27194700381421));
#27118=CARTESIAN_POINT('Ctrl Pts',(4.90565273067095,61.6490074219701,-1.18544827339454));
#27119=CARTESIAN_POINT('Ctrl Pts',(2.45282636533548,61.5220074219701,-0.388476675857597));
#27120=CARTESIAN_POINT('Ctrl Pts',(0.,61.3950074219701,0.408494921679244));
#27121=CARTESIAN_POINT('Ctrl Pts',(-2.45282636533548,61.2680074219701,-0.388476675857598));
#27122=CARTESIAN_POINT('Ctrl Pts',(-4.905652730671,61.1410074219701,-1.18544827339454));
#27123=CARTESIAN_POINT('Ctrl Pts',(-6.42158279295003,61.0140074219702,-3.27194700381421));
#27124=CARTESIAN_POINT('Ctrl Pts',(-7.93751285522931,60.88700742197,-5.35844573423412));
#27125=CARTESIAN_POINT('Ctrl Pts',(-7.93751285522922,60.76000742197,-7.93749999999999));
#27126=CARTESIAN_POINT('Ctrl Pts',(-7.93751285522926,60.63300742197,-10.5165542657659));
#27127=CARTESIAN_POINT('Ctrl Pts',(-6.42158279295009,60.5060074219702,-12.6030529961856));
#27128=CARTESIAN_POINT('Ctrl Pts',(-4.90565273067089,60.3790074219701,-14.6895517266055));
#27129=CARTESIAN_POINT('Ctrl Pts',(-2.45282636533548,60.2520074219701,-15.4865233241424));
#27130=CARTESIAN_POINT('Ctrl Pts',(-1.09153927723476E-18,60.12500742197,
-16.2834949216793));
#27131=CARTESIAN_POINT('Ctrl Pts',(2.45282636533542,59.9980074219701,-15.4865233241424));
#27132=CARTESIAN_POINT('Ctrl Pts',(4.90565273067095,59.8710074219699,-14.6895517266055));
#27133=CARTESIAN_POINT('Ctrl Pts',(6.42158279295009,59.7440074219701,-12.6030529961856));
#27134=CARTESIAN_POINT('Ctrl Pts',(7.93751285522931,59.6170074219701,-10.5165542657659));
#27135=CARTESIAN_POINT('Ctrl Pts',(7.93751285522933,59.4900074219701,-7.93749999999999));
#27136=CARTESIAN_POINT('Ctrl Pts',(7.93751285522937,59.36300742197,-5.35844573423412));
#27137=CARTESIAN_POINT('Ctrl Pts',(6.42158279295014,59.2360074219701,-3.27194700381421));
#27138=CARTESIAN_POINT('Ctrl Pts',(4.90565273067095,59.1090074219701,-1.18544827339454));
#27139=CARTESIAN_POINT('Ctrl Pts',(2.45282636533548,58.9820074219701,-0.388476675857597));
#27140=CARTESIAN_POINT('Ctrl Pts',(-5.4576963861738E-19,58.85500742197,
0.408494921679244));
#27141=CARTESIAN_POINT('Ctrl Pts',(-2.45282636533548,58.7280074219701,-0.388476675857598));
#27142=CARTESIAN_POINT('Ctrl Pts',(-4.90565273067089,58.6010074219702,-1.18544827339454));
#27143=CARTESIAN_POINT('Ctrl Pts',(-6.42158279295009,58.4740074219701,-3.27194700381421));
#27144=CARTESIAN_POINT('Ctrl Pts',(-7.9375128552292,58.3470074219701,-5.35844573423412));
#27145=CARTESIAN_POINT('Ctrl Pts',(-7.93751285522922,58.2200074219702,-7.93749999999999));
#27146=CARTESIAN_POINT('Ctrl Pts',(-7.93751285522931,58.0930074219701,-10.5165542657659));
#27147=CARTESIAN_POINT('Ctrl Pts',(-6.42158279295009,57.9660074219701,-12.6030529961856));
#27148=CARTESIAN_POINT('Ctrl Pts',(-4.90565273067089,57.83900742197,-14.6895517266055));
#27149=CARTESIAN_POINT('Ctrl Pts',(-2.45282636533542,57.7120074219702,-15.4865233241424));
#27150=CARTESIAN_POINT('Ctrl Pts',(0.,57.5850074219701,-16.2834949216793));
#27151=CARTESIAN_POINT('Ctrl Pts',(2.45282636533548,57.4580074219702,-15.4865233241424));
#27152=CARTESIAN_POINT('Ctrl Pts',(4.90565273067095,57.33100742197,-14.6895517266055));
#27153=CARTESIAN_POINT('Ctrl Pts',(6.42158279295014,57.2040074219703,-12.6030529961856));
#27154=CARTESIAN_POINT('Ctrl Pts',(7.93751285522931,57.07700742197,-10.5165542657659));
#27155=CARTESIAN_POINT('Ctrl Pts',(7.93751285522939,56.95000742197,-7.93749999999999));
#27156=CARTESIAN_POINT('Ctrl Pts',(7.93751285522926,56.8230074219701,-5.35844573423412));
#27157=CARTESIAN_POINT('Ctrl Pts',(6.42158279295014,56.6960074219701,-3.27194700381421));
#27158=CARTESIAN_POINT('Ctrl Pts',(4.90565273067095,56.5690074219701,-1.18544827339454));
#27159=CARTESIAN_POINT('Ctrl Pts',(2.45282636533548,56.4420074219701,-0.388476675857598));
#27160=CARTESIAN_POINT('Ctrl Pts',(0.,56.3150074219701,0.408494921679244));
#27161=CARTESIAN_POINT('Ctrl Pts',(-2.45282636533548,56.1880074219701,-0.388476675857598));
#27162=CARTESIAN_POINT('Ctrl Pts',(-4.90565273067095,56.06100742197,-1.18544827339454));
#27163=CARTESIAN_POINT('Ctrl Pts',(-6.42158279295009,55.9340074219701,-3.27194700381421));
#27164=CARTESIAN_POINT('Ctrl Pts',(-7.93751285522931,55.80700742197,-5.35844573423412));
#27165=CARTESIAN_POINT('Ctrl Pts',(-7.93751285522927,55.6800074219702,-7.93749999999999));
#27166=CARTESIAN_POINT('Ctrl Pts',(-7.9375128552292,55.5530074219702,-10.5165542657659));
#27167=CARTESIAN_POINT('Ctrl Pts',(-6.42158279295009,55.4260074219702,-12.6030529961856));
#27168=CARTESIAN_POINT('Ctrl Pts',(-4.90565273067089,55.2990074219701,-14.6895517266055));
#27169=CARTESIAN_POINT('Ctrl Pts',(-2.45282636533548,55.1720074219703,-15.4865233241424));
#27170=CARTESIAN_POINT('Ctrl Pts',(-1.16736848626568E-13,55.04500742197,
-16.2834949216793));
#27171=CARTESIAN_POINT('Ctrl Pts',(2.45282636533548,54.9180074219703,-15.4865233241424));
#27172=CARTESIAN_POINT('Ctrl Pts',(4.90565273067083,54.7910074219699,-14.6895517266055));
#27173=CARTESIAN_POINT('Ctrl Pts',(6.42158279295014,54.6640074219702,-12.6030529961857));
#27174=CARTESIAN_POINT('Ctrl Pts',(7.93751285522931,54.53700742197,-10.5165542657659));
#27175=CARTESIAN_POINT('Ctrl Pts',(7.93751285522939,54.4100074219701,-7.93750000000004));
#27176=CARTESIAN_POINT('Ctrl Pts',(7.93751285522937,54.2830074219701,-5.35844573423412));
#27177=CARTESIAN_POINT('Ctrl Pts',(6.4215827929502,54.1560074219701,-3.27194700381427));
#27178=CARTESIAN_POINT('Ctrl Pts',(4.90565273067083,54.0290074219701,-1.18544827339454));
#27179=CARTESIAN_POINT('Ctrl Pts',(2.45282636533542,53.90200742197,-0.388476675857653));
#27180=CARTESIAN_POINT('Ctrl Pts',(-5.83684243132838E-14,53.77500742197,
0.408494921679244));
#27181=CARTESIAN_POINT('Ctrl Pts',(-2.45282636533542,53.6480074219701,-0.388476675857653));
#27182=CARTESIAN_POINT('Ctrl Pts',(-4.90565273067095,53.5210074219699,-1.18544827339454));
#27183=CARTESIAN_POINT('Ctrl Pts',(-6.42158279295009,53.39400742197,-3.27194700381427));
#27184=CARTESIAN_POINT('Ctrl Pts',(-7.93751285522926,53.26700742197,-5.35844573423412));
#27185=CARTESIAN_POINT('Ctrl Pts',(-7.93751285522927,53.1400074219701,-7.93750000000004));
#27186=CARTESIAN_POINT('Ctrl Pts',(-7.93751285522931,53.0130074219701,-10.5165542657659));
#27187=CARTESIAN_POINT('Ctrl Pts',(-6.42158279295009,52.8860074219702,-12.6030529961857));
#27188=CARTESIAN_POINT('Ctrl Pts',(-4.905652730671,52.7590074219701,-14.6895517266055));
#27189=CARTESIAN_POINT('Ctrl Pts',(-2.45282636533548,52.6320074219702,-15.4865233241424));
#27190=CARTESIAN_POINT('Ctrl Pts',(1.16736848626568E-13,52.5050074219701,
-16.2834949216793));
#27191=CARTESIAN_POINT('Ctrl Pts',(2.45282636533548,52.3780074219702,-15.4865233241424));
#27192=CARTESIAN_POINT('Ctrl Pts',(4.905652730671,52.2510074219701,-14.6895517266055));
#27193=CARTESIAN_POINT('Ctrl Pts',(6.4215827929502,52.1240074219702,-12.6030529961857));
#27194=CARTESIAN_POINT('Ctrl Pts',(7.93751285522931,51.9970074219699,-10.5165542657659));
#27195=CARTESIAN_POINT('Ctrl Pts',(7.93751285522939,51.8700074219702,-7.93750000000004));
#27196=CARTESIAN_POINT('Ctrl Pts',(7.93751285522931,51.7430074219701,-5.35844573423412));
#27197=CARTESIAN_POINT('Ctrl Pts',(6.4215827929502,51.61600742197,-3.27194700381427));
#27198=CARTESIAN_POINT('Ctrl Pts',(4.90565273067095,51.4890074219701,-1.18544827339454));
#27199=CARTESIAN_POINT('Ctrl Pts',(2.45282636533542,51.3620074219701,-0.388476675857653));
#27200=CARTESIAN_POINT('Ctrl Pts',(1.16736848626568E-13,51.2350074219701,
0.408494921679244));
#27201=CARTESIAN_POINT('Ctrl Pts',(-2.45282636533542,51.1080074219701,-0.388476675857653));
#27202=CARTESIAN_POINT('Ctrl Pts',(-4.90565273067095,50.9810074219701,-1.18544827339454));
#27203=CARTESIAN_POINT('Ctrl Pts',(-6.42158279295009,50.85400742197,-3.27194700381427));
#27204=CARTESIAN_POINT('Ctrl Pts',(-7.93751285522926,50.7270074219701,-5.35844573423412));
#27205=CARTESIAN_POINT('Ctrl Pts',(-7.93751285522927,50.6000074219701,-7.93750000000004));
#27206=CARTESIAN_POINT('Ctrl Pts',(-7.93751285522931,50.47300742197,-10.5165542657659));
#27207=CARTESIAN_POINT('Ctrl Pts',(-6.42158279295003,50.3460074219702,-12.6030529961857));
#27208=CARTESIAN_POINT('Ctrl Pts',(-4.90565273067083,50.2190074219701,-14.6895517266055));
#27209=CARTESIAN_POINT('Ctrl Pts',(-2.45282636533548,50.0920074219702,-15.4865233241424));
#27210=CARTESIAN_POINT('Ctrl Pts',(1.16736848626568E-13,49.9650074219701,
-16.2834949216793));
#27211=CARTESIAN_POINT('Ctrl Pts',(2.45282636533548,49.8380074219702,-15.4865233241424));
#27212=CARTESIAN_POINT('Ctrl Pts',(4.90565273067089,49.7110074219701,-14.6895517266055));
#27213=CARTESIAN_POINT('Ctrl Pts',(6.4215827929502,49.5840074219702,-12.6030529961857));
#27214=CARTESIAN_POINT('Ctrl Pts',(7.93751285522931,49.4570074219702,-10.5165542657659));
#27215=CARTESIAN_POINT('Ctrl Pts',(7.93751285522939,49.3300074219701,-7.93750000000004));
#27216=CARTESIAN_POINT('Ctrl Pts',(7.93751285522931,49.2030074219701,-5.35844573423412));
#27217=CARTESIAN_POINT('Ctrl Pts',(6.4215827929502,49.0760074219702,-3.27194700381427));
#27218=CARTESIAN_POINT('Ctrl Pts',(4.905652730671,48.94900742197,-1.18544827339454));
#27219=CARTESIAN_POINT('Ctrl Pts',(2.45282636533548,48.8220074219701,-0.388476675857653));
#27220=CARTESIAN_POINT('Ctrl Pts',(0.,48.6950074219701,0.408494921679244));
#27221=CARTESIAN_POINT('Ctrl Pts',(-2.45282636533548,48.5680074219701,-0.388476675857653));
#27222=CARTESIAN_POINT('Ctrl Pts',(-4.90565273067095,48.44100742197,-1.18544827339454));
#27223=CARTESIAN_POINT('Ctrl Pts',(-6.42158279295009,48.3140074219701,-3.27194700381427));
#27224=CARTESIAN_POINT('Ctrl Pts',(-7.93751285522926,48.1870074219701,-5.35844573423412));
#27225=CARTESIAN_POINT('Ctrl Pts',(-7.93751285522927,48.06000742197,-7.93750000000004));
#27226=CARTESIAN_POINT('Ctrl Pts',(-7.9375128552292,47.9330074219701,-10.5165542657659));
#27227=CARTESIAN_POINT('Ctrl Pts',(-6.42158279295003,47.8060074219702,-12.6030529961857));
#27228=CARTESIAN_POINT('Ctrl Pts',(-4.90565273067095,47.6790074219701,-14.6895517266055));
#27229=CARTESIAN_POINT('Ctrl Pts',(-2.45282636533548,47.5520074219702,-15.4865233241424));
#27230=CARTESIAN_POINT('Ctrl Pts',(1.09153927723476E-18,47.4250074219701,
-16.2834949216793));
#27231=CARTESIAN_POINT('Ctrl Pts',(2.45282636533542,47.2980074219702,-15.4865233241424));
#27232=CARTESIAN_POINT('Ctrl Pts',(4.90565273067089,47.17100742197,-14.6895517266055));
#27233=CARTESIAN_POINT('Ctrl Pts',(6.4215827929502,47.0440074219702,-12.6030529961857));
#27234=CARTESIAN_POINT('Ctrl Pts',(7.93751285522937,46.9170074219701,-10.5165542657659));
#27235=CARTESIAN_POINT('Ctrl Pts',(7.93751285522933,46.7900074219701,-7.93750000000004));
#27236=CARTESIAN_POINT('Ctrl Pts',(7.93751285522931,46.66300742197,-5.35844573423412));
#27237=CARTESIAN_POINT('Ctrl Pts',(6.42158279295009,46.5360074219702,-3.27194700381427));
#27238=CARTESIAN_POINT('Ctrl Pts',(4.90565273067089,46.4090074219701,-1.18544827339454));
#27239=CARTESIAN_POINT('Ctrl Pts',(2.45282636533548,46.2820074219701,-0.388476675857653));
#27240=CARTESIAN_POINT('Ctrl Pts',(1.09153927723476E-18,46.15500742197,
0.408494921679244));
#27241=CARTESIAN_POINT('Ctrl Pts',(-2.45282636533548,46.0280074219701,-0.388476675857653));
#27242=CARTESIAN_POINT('Ctrl Pts',(-4.90565273067095,45.9010074219699,-1.18544827339454));
#27243=CARTESIAN_POINT('Ctrl Pts',(-6.42158279295003,45.7740074219702,-3.27194700381427));
#27244=CARTESIAN_POINT('Ctrl Pts',(-7.93751285522931,45.64700742197,-5.35844573423412));
#27245=CARTESIAN_POINT('Ctrl Pts',(-7.93751285522922,45.52000742197,-7.93750000000004));
#27246=CARTESIAN_POINT('Ctrl Pts',(-7.93751285522926,45.39300742197,-10.5165542657659));
#27247=CARTESIAN_POINT('Ctrl Pts',(-6.42158279294998,45.2660074219702,-12.6030529961857));
#27248=CARTESIAN_POINT('Ctrl Pts',(-4.90565273067095,45.13900742197,-14.6895517266055));
#27249=CARTESIAN_POINT('Ctrl Pts',(-2.45282636533548,45.0120074219701,-15.4865233241424));
#27250=CARTESIAN_POINT('Ctrl Pts',(1.16736848626568E-13,44.88500742197,
-16.2834949216792));
#27251=CARTESIAN_POINT('Ctrl Pts',(2.45282636533542,44.7580074219701,-15.4865233241424));
#27252=CARTESIAN_POINT('Ctrl Pts',(4.90565273067095,44.6310074219701,-14.6895517266055));
#27253=CARTESIAN_POINT('Ctrl Pts',(6.42158279295009,44.5040074219701,-12.6030529961857));
#27254=CARTESIAN_POINT('Ctrl Pts',(7.93751285522926,44.37700742197,-10.5165542657659));
#27255=CARTESIAN_POINT('Ctrl Pts',(7.93751285522933,44.2500074219701,-7.93750000000004));
#27256=CARTESIAN_POINT('Ctrl Pts',(7.93751285522931,44.12300742197,-5.35844573423412));
#27257=CARTESIAN_POINT('Ctrl Pts',(6.42158279295014,43.9960074219701,-3.27194700381427));
#27258=CARTESIAN_POINT('Ctrl Pts',(4.905652730671,43.86900742197,-1.18544827339454));
#27259=CARTESIAN_POINT('Ctrl Pts',(2.45282636533548,43.7420074219702,-0.388476675857653));
#27260=CARTESIAN_POINT('Ctrl Pts',(-1.09153927723476E-18,43.6150074219699,
0.408494921679244));
#27261=CARTESIAN_POINT('Ctrl Pts',(-2.45282636533548,43.4880074219701,-0.388476675857653));
#27262=CARTESIAN_POINT('Ctrl Pts',(-4.90565273067089,43.36100742197,-1.18544827339454));
#27263=CARTESIAN_POINT('Ctrl Pts',(-6.42158279294998,43.2340074219701,-3.27194700381427));
#27264=CARTESIAN_POINT('Ctrl Pts',(-7.9375128552292,43.1070074219701,-5.35844573423412));
#27265=CARTESIAN_POINT('Ctrl Pts',(-7.93751285522922,42.9800074219701,-7.93750000000004));
#27266=CARTESIAN_POINT('Ctrl Pts',(-7.93751285522926,42.85300742197,-10.5165542657659));
#27267=CARTESIAN_POINT('Ctrl Pts',(-6.42158279295009,42.7260074219701,-12.6030529961857));
#27268=CARTESIAN_POINT('Ctrl Pts',(-4.90565273067095,42.5990074219699,-14.6895517266055));
#27269=CARTESIAN_POINT('Ctrl Pts',(-2.45282636533542,42.4720074219702,-15.4865233241424));
#27270=CARTESIAN_POINT('Ctrl Pts',(-1.09153927723476E-18,42.3450074219701,
-16.2834949216792));
#27271=CARTESIAN_POINT('Ctrl Pts',(2.45282636533548,42.2180074219702,-15.4865233241424));
#27272=CARTESIAN_POINT('Ctrl Pts',(4.90565273067095,42.0910074219701,-14.6895517266055));
#27273=CARTESIAN_POINT('Ctrl Pts',(6.42158279295014,41.9640074219702,-12.6030529961857));
#27274=CARTESIAN_POINT('Ctrl Pts',(7.93751285522937,41.8370074219701,-10.5165542657659));
#27275=CARTESIAN_POINT('Ctrl Pts',(7.93751285522939,41.71000742197,-7.93750000000004));
#27276=CARTESIAN_POINT('Ctrl Pts',(7.93751285522931,41.5830074219701,-5.35844573423412));
#27277=CARTESIAN_POINT('Ctrl Pts',(6.4215827929502,41.4560074219701,-3.27194700381427));
#27278=CARTESIAN_POINT('Ctrl Pts',(4.90565273067089,41.3290074219701,-1.18544827339454));
#27279=CARTESIAN_POINT('Ctrl Pts',(2.45282636533548,41.2020074219701,-0.388476675857653));
#27280=CARTESIAN_POINT('Ctrl Pts',(0.,41.07500742197,0.408494921679244));
#27281=CARTESIAN_POINT('Ctrl Pts',(-2.45282636533548,40.9480074219701,-0.388476675857653));
#27282=CARTESIAN_POINT('Ctrl Pts',(-4.90565273067089,40.8210074219701,-1.18544827339454));
#27283=CARTESIAN_POINT('Ctrl Pts',(-6.42158279295009,40.6940074219701,-3.27194700381427));
#27284=CARTESIAN_POINT('Ctrl Pts',(-7.93751285522931,40.56700742197,-5.35844573423412));
#27285=CARTESIAN_POINT('Ctrl Pts',(-7.93751285522922,40.4400074219702,-7.93750000000004));
#27286=CARTESIAN_POINT('Ctrl Pts',(-7.93751285522926,40.3130074219699,-10.5165542657659));
#27287=CARTESIAN_POINT('Ctrl Pts',(-6.42158279295009,40.1860074219702,-12.6030529961857));
#27288=CARTESIAN_POINT('Ctrl Pts',(-4.90565273067095,40.05900742197,-14.6895517266055));
#27289=CARTESIAN_POINT('Ctrl Pts',(-2.45282636533542,39.9320074219703,-15.4865233241424));
#27290=CARTESIAN_POINT('Ctrl Pts',(0.,39.80500742197,-16.2834949216792));
#27291=CARTESIAN_POINT('Ctrl Pts',(2.45282636533548,39.6780074219702,-15.4865233241424));
#27292=CARTESIAN_POINT('Ctrl Pts',(4.90565273067095,39.55100742197,-14.6895517266055));
#27293=CARTESIAN_POINT('Ctrl Pts',(6.42158279295014,39.4240074219703,-12.6030529961857));
#27294=CARTESIAN_POINT('Ctrl Pts',(7.93751285522926,39.29700742197,-10.5165542657659));
#27295=CARTESIAN_POINT('Ctrl Pts',(7.93751285522939,39.1700074219701,-7.93750000000004));
#27296=CARTESIAN_POINT('Ctrl Pts',(7.93751285522926,39.04300742197,-5.35844573423412));
#27297=CARTESIAN_POINT('Ctrl Pts',(6.4215827929502,38.91600742197,-3.27194700381427));
#27298=CARTESIAN_POINT('Ctrl Pts',(4.90565273067095,38.78900742197,-1.18544827339454));
#27299=CARTESIAN_POINT('Ctrl Pts',(2.45282636533542,38.6620074219701,-0.388476675857653));
#27300=CARTESIAN_POINT('Ctrl Pts',(0.,38.53500742197,0.408494921679244));
#27301=CARTESIAN_POINT('Ctrl Pts',(-2.45282636533542,38.40800742197,-0.388476675857653));
#27302=CARTESIAN_POINT('Ctrl Pts',(-4.905652730671,38.2810074219701,-1.18544827339454));
#27303=CARTESIAN_POINT('Ctrl Pts',(-6.42158279295009,38.1540074219701,-3.27194700381427));
#27304=CARTESIAN_POINT('Ctrl Pts',(-7.93751285522931,38.02700742197,-5.35844573423412));
#27305=CARTESIAN_POINT('Ctrl Pts',(-7.93751285522927,37.9000074219701,-7.93750000000004));
#27306=CARTESIAN_POINT('Ctrl Pts',(-7.93751285522926,37.7730074219701,-10.5165542657659));
#27307=CARTESIAN_POINT('Ctrl Pts',(-6.42158279295009,37.6460074219702,-12.6030529961857));
#27308=CARTESIAN_POINT('Ctrl Pts',(-4.90565273067089,37.51900742197,-14.6895517266055));
#27309=CARTESIAN_POINT('Ctrl Pts',(-2.45282636533548,37.3920074219702,-15.4865233241423));
#27310=CARTESIAN_POINT('Ctrl Pts',(-1.09153927723476E-18,37.26500742197,
-16.2834949216792));
#27311=CARTESIAN_POINT('Ctrl Pts',(2.45282636533548,37.1380074219702,-15.4865233241423));
#27312=CARTESIAN_POINT('Ctrl Pts',(4.90565273067095,37.0110074219701,-14.6895517266055));
#27313=CARTESIAN_POINT('Ctrl Pts',(6.4215827929502,36.8840074219702,-12.6030529961857));
#27314=CARTESIAN_POINT('Ctrl Pts',(7.93751285522931,36.7570074219701,-10.5165542657659));
#27315=CARTESIAN_POINT('Ctrl Pts',(7.93751285522939,36.6300074219701,-7.93750000000004));
#27316=CARTESIAN_POINT('Ctrl Pts',(7.93751285522937,36.5030074219699,-5.35844573423412));
#27317=CARTESIAN_POINT('Ctrl Pts',(6.4215827929502,36.37600742197,-3.27194700381427));
#27318=CARTESIAN_POINT('Ctrl Pts',(4.90565273067095,36.24900742197,-1.18544827339454));
#27319=CARTESIAN_POINT('Ctrl Pts',(2.45282636533548,36.12200742197,-0.388476675857653));
#27320=CARTESIAN_POINT('Ctrl Pts',(-5.4576963861738E-19,35.9950074219701,
0.408494921679244));
#27321=CARTESIAN_POINT('Ctrl Pts',(-2.45282636533542,35.86800742197,-0.388476675857653));
#27322=CARTESIAN_POINT('Ctrl Pts',(-4.90565273067089,35.7410074219701,-1.18544827339454));
#27323=CARTESIAN_POINT('Ctrl Pts',(-6.42158279295009,35.61400742197,-3.27194700381427));
#27324=CARTESIAN_POINT('Ctrl Pts',(-7.9375128552292,35.4870074219701,-5.35844573423412));
#27325=CARTESIAN_POINT('Ctrl Pts',(-7.93751285522927,35.3600074219701,-7.93750000000004));
#27326=CARTESIAN_POINT('Ctrl Pts',(-7.93751285522931,35.2330074219701,-10.5165542657659));
#27327=CARTESIAN_POINT('Ctrl Pts',(-6.42158279295003,35.1060074219702,-12.6030529961857));
#27328=CARTESIAN_POINT('Ctrl Pts',(-4.90565273067089,34.9790074219701,-14.6895517266055));
#27329=CARTESIAN_POINT('Ctrl Pts',(-2.45282636533548,34.8520074219702,-15.4865233241423));
#27330=CARTESIAN_POINT('Ctrl Pts',(0.,34.7250074219701,-16.2834949216792));
#27331=CARTESIAN_POINT('Ctrl Pts',(2.45282636533548,34.5980074219702,-15.4865233241423));
#27332=CARTESIAN_POINT('Ctrl Pts',(4.90565273067095,34.4710074219701,-14.6895517266055));
#27333=CARTESIAN_POINT('Ctrl Pts',(6.4215827929502,34.3440074219702,-12.6030529961857));
#27334=CARTESIAN_POINT('Ctrl Pts',(7.93751285522931,34.21700742197,-10.5165542657659));
#27335=CARTESIAN_POINT('Ctrl Pts',(7.93751285522939,34.0900074219701,-7.93750000000004));
#27336=CARTESIAN_POINT('Ctrl Pts',(7.93751285522926,33.9630074219701,-5.35844573423412));
#27337=CARTESIAN_POINT('Ctrl Pts',(6.4215827929502,33.8360074219702,-3.27194700381427));
#27338=CARTESIAN_POINT('Ctrl Pts',(4.90565273067095,33.7090074219701,-1.18544827339454));
#27339=CARTESIAN_POINT('Ctrl Pts',(2.45282636533548,33.5820074219701,-0.388476675857653));
#27340=CARTESIAN_POINT('Ctrl Pts',(0.,33.4550074219701,0.408494921679244));
#27341=CARTESIAN_POINT('Ctrl Pts',(-2.45282636533548,33.3280074219701,-0.388476675857653));
#27342=CARTESIAN_POINT('Ctrl Pts',(-4.90565273067095,33.20100742197,-1.18544827339454));
#27343=CARTESIAN_POINT('Ctrl Pts',(-6.42158279295003,33.07400742197,-3.27194700381427));
#27344=CARTESIAN_POINT('Ctrl Pts',(-7.93751285522931,32.9470074219701,-5.35844573423412));
#27345=CARTESIAN_POINT('Ctrl Pts',(-7.93751285522927,32.82000742197,-7.93750000000004));
#27346=CARTESIAN_POINT('Ctrl Pts',(-7.9375128552292,32.69300742197,-10.5165542657659));
#27347=CARTESIAN_POINT('Ctrl Pts',(-6.42158279295003,32.5660074219702,-12.6030529961857));
#27348=CARTESIAN_POINT('Ctrl Pts',(-4.90565273067089,32.4390074219701,-14.6895517266055));
#27349=CARTESIAN_POINT('Ctrl Pts',(-2.45282636533548,32.3120074219702,-15.4865233241423));
#27350=CARTESIAN_POINT('Ctrl Pts',(-1.16736848626568E-13,32.1850074219701,
-16.2834949216792));
#27351=CARTESIAN_POINT('Ctrl Pts',(2.45282636533548,32.0580074219702,-15.4865233241423));
#27352=CARTESIAN_POINT('Ctrl Pts',(4.90565273067083,31.9310074219701,-14.6895517266055));
#27353=CARTESIAN_POINT('Ctrl Pts',(6.4215827929502,31.8040074219701,-12.6030529961857));
#27354=CARTESIAN_POINT('Ctrl Pts',(7.93751285522931,31.67700742197,-10.5165542657659));
#27355=CARTESIAN_POINT('Ctrl Pts',(7.93751285522933,31.5500074219701,-7.93750000000004));
#27356=CARTESIAN_POINT('Ctrl Pts',(7.93751285522926,31.4230074219701,-5.35844573423412));
#27357=CARTESIAN_POINT('Ctrl Pts',(6.42158279295026,31.2960074219702,-3.27194700381427));
#27358=CARTESIAN_POINT('Ctrl Pts',(4.90565273067083,31.16900742197,-1.18544827339454));
#27359=CARTESIAN_POINT('Ctrl Pts',(2.45282636533548,31.04200742197,-0.388476675857653));
#27360=CARTESIAN_POINT('Ctrl Pts',(0.,30.9150074219701,0.408494921679244));
#27361=CARTESIAN_POINT('Ctrl Pts',(-2.45282636533548,30.7880074219701,-0.388476675857653));
#27362=CARTESIAN_POINT('Ctrl Pts',(-4.90565273067095,30.6610074219701,-1.18544827339454));
#27363=CARTESIAN_POINT('Ctrl Pts',(-6.42158279295003,30.53400742197,-3.27194700381427));
#27364=CARTESIAN_POINT('Ctrl Pts',(-7.93751285522926,30.40700742197,-5.35844573423412));
#27365=CARTESIAN_POINT('Ctrl Pts',(-7.93751285522922,30.28000742197,-7.93750000000004));
#27366=CARTESIAN_POINT('Ctrl Pts',(-7.93751285522931,30.15300742197,-10.5165542657659));
#27367=CARTESIAN_POINT('Ctrl Pts',(-6.42158279294998,30.0260074219701,-12.6030529961857));
#27368=CARTESIAN_POINT('Ctrl Pts',(-4.90565273067095,29.89900742197,-14.6895517266055));
#27369=CARTESIAN_POINT('Ctrl Pts',(-2.45282636533542,29.7720074219701,-15.4865233241423));
#27370=CARTESIAN_POINT('Ctrl Pts',(0.,29.64500742197,-16.2834949216792));
#27371=CARTESIAN_POINT('Ctrl Pts',(2.45282636533548,29.5180074219701,-15.4865233241423));
#27372=CARTESIAN_POINT('Ctrl Pts',(4.905652730671,29.3910074219701,-14.6895517266055));
#27373=CARTESIAN_POINT('Ctrl Pts',(6.4215827929502,29.2640074219701,-12.6030529961857));
#27374=CARTESIAN_POINT('Ctrl Pts',(7.93751285522931,29.1370074219701,-10.5165542657659));
#27375=CARTESIAN_POINT('Ctrl Pts',(7.93751285522922,29.0100074219701,-7.93750000000004));
#27376=CARTESIAN_POINT('Ctrl Pts',(7.93751285522931,28.88300742197,-5.35844573423412));
#27377=CARTESIAN_POINT('Ctrl Pts',(6.42158279295014,28.7560074219701,-3.27194700381427));
#27378=CARTESIAN_POINT('Ctrl Pts',(4.90565273067095,28.62900742197,-1.18544827339454));
#27379=CARTESIAN_POINT('Ctrl Pts',(2.45282636533548,28.5020074219701,-0.388476675857653));
#27380=CARTESIAN_POINT('Ctrl Pts',(1.16736848626568E-13,28.3750074219701,
0.408494921679244));
#27381=CARTESIAN_POINT('Ctrl Pts',(-2.45282636533548,28.2480074219701,-0.388476675857653));
#27382=CARTESIAN_POINT('Ctrl Pts',(-4.90565273067083,28.12100742197,-1.18544827339454));
#27383=CARTESIAN_POINT('Ctrl Pts',(-6.42158279294998,27.9940074219702,-3.27194700381427));
#27384=CARTESIAN_POINT('Ctrl Pts',(-7.93751285522926,27.8670074219701,-5.35844573423412));
#27385=CARTESIAN_POINT('Ctrl Pts',(-7.93751285522922,27.7400074219701,-7.93750000000004));
#27386=CARTESIAN_POINT('Ctrl Pts',(-7.93751285522931,27.6130074219701,-10.5165542657659));
#27387=CARTESIAN_POINT('Ctrl Pts',(-6.42158279295009,27.4860074219701,-12.6030529961857));
#27388=CARTESIAN_POINT('Ctrl Pts',(-4.90565273067083,27.35900742197,-14.6895517266055));
#27389=CARTESIAN_POINT('Ctrl Pts',(-2.45282636533542,27.2320074219702,-15.4865233241423));
#27390=CARTESIAN_POINT('Ctrl Pts',(1.16736848626568E-13,27.1050074219701,
-16.2834949216792));
#27391=CARTESIAN_POINT('Ctrl Pts',(2.45282636533548,26.9780074219701,-15.4865233241423));
#27392=CARTESIAN_POINT('Ctrl Pts',(4.90565273067089,26.8510074219701,-14.6895517266055));
#27393=CARTESIAN_POINT('Ctrl Pts',(6.42158279295014,26.7240074219702,-12.6030529961857));
#27394=CARTESIAN_POINT('Ctrl Pts',(7.93751285522926,26.59700742197,-10.5165542657659));
#27395=CARTESIAN_POINT('Ctrl Pts',(7.93751285522927,26.47000742197,-7.93750000000004));
#27396=CARTESIAN_POINT('Ctrl Pts',(7.93751285522931,26.3430074219701,-5.35844573423412));
#27397=CARTESIAN_POINT('Ctrl Pts',(6.4215827929502,26.2160074219701,-3.27194700381427));
#27398=CARTESIAN_POINT('Ctrl Pts',(4.905652730671,26.0890074219702,-1.18544827339454));
#27399=CARTESIAN_POINT('Ctrl Pts',(2.45282636533548,25.9620074219701,-0.388476675857653));
#27400=CARTESIAN_POINT('Ctrl Pts',(0.,25.8350074219701,0.408494921679244));
#27401=CARTESIAN_POINT('Ctrl Pts',(-2.45282636533548,25.7080074219701,-0.388476675857653));
#27402=CARTESIAN_POINT('Ctrl Pts',(-4.90565273067095,25.5810074219699,-1.18544827339454));
#27403=CARTESIAN_POINT('Ctrl Pts',(-6.42158279294998,25.4540074219701,-3.27194700381427));
#27404=CARTESIAN_POINT('Ctrl Pts',(-7.93751285522926,25.32700742197,-5.35844573423412));
#27405=CARTESIAN_POINT('Ctrl Pts',(-7.93751285522916,25.2000074219701,-7.93750000000004));
#27406=CARTESIAN_POINT('Ctrl Pts',(-7.93751285522931,25.07300742197,-10.5165542657659));
#27407=CARTESIAN_POINT('Ctrl Pts',(-6.42158279295009,24.9460074219701,-12.6030529961857));
#27408=CARTESIAN_POINT('Ctrl Pts',(-4.90565273067095,24.8190074219701,-14.6895517266055));
#27409=CARTESIAN_POINT('Ctrl Pts',(-2.45282636533537,24.6920074219702,-15.4865233241423));
#27410=CARTESIAN_POINT('Ctrl Pts',(0.,24.56500742197,-16.2834949216792));
#27411=CARTESIAN_POINT('Ctrl Pts',(2.45282636533548,24.4380074219702,-15.4865233241423));
#27412=CARTESIAN_POINT('Ctrl Pts',(4.90565273067089,24.3110074219699,-14.6895517266055));
#27413=CARTESIAN_POINT('Ctrl Pts',(6.42158279295003,24.1840074219703,-12.6030529961857));
#27414=CARTESIAN_POINT('Ctrl Pts',(7.93751285522937,24.05700742197,-10.5165542657659));
#27415=CARTESIAN_POINT('Ctrl Pts',(7.93751285522927,23.9300074219701,-7.93750000000004));
#27416=CARTESIAN_POINT('Ctrl Pts',(7.9375128552292,23.80300742197,-5.35844573423412));
#27417=CARTESIAN_POINT('Ctrl Pts',(6.42158279295009,23.6760074219701,-3.27194700381427));
#27418=CARTESIAN_POINT('Ctrl Pts',(4.90565273067089,23.5490074219701,-1.18544827339454));
#27419=CARTESIAN_POINT('Ctrl Pts',(2.45282636533553,23.4220074219701,-0.388476675857653));
#27420=CARTESIAN_POINT('Ctrl Pts',(1.09153927723476E-18,23.29500742197,
0.408494921679244));
#27421=CARTESIAN_POINT('Ctrl Pts',(-2.45282636533542,23.1680074219701,-0.388476675857653));
#27422=CARTESIAN_POINT('Ctrl Pts',(-4.90565273067095,23.0410074219701,-1.18544827339454));
#27423=CARTESIAN_POINT('Ctrl Pts',(-6.42158279295009,22.9140074219701,-3.27194700381427));
#27424=CARTESIAN_POINT('Ctrl Pts',(-7.93751285522931,22.78700742197,-5.35844573423412));
#27425=CARTESIAN_POINT('Ctrl Pts',(-7.93751285522927,22.6600074219701,-7.93750000000004));
#27426=CARTESIAN_POINT('Ctrl Pts',(-7.93751285522926,22.53300742197,-10.5165542657659));
#27427=CARTESIAN_POINT('Ctrl Pts',(-6.42158279295009,22.4060074219703,-12.6030529961857));
#27428=CARTESIAN_POINT('Ctrl Pts',(-4.90565273067095,22.27900742197,-14.6895517266055));
#27429=CARTESIAN_POINT('Ctrl Pts',(-2.45282636533548,22.1520074219702,-15.4865233241423));
#27430=CARTESIAN_POINT('Ctrl Pts',(0.,22.02500742197,-16.2834949216792));
#27431=CARTESIAN_POINT('Ctrl Pts',(2.45282636533548,21.8980074219703,-15.4865233241423));
#27432=CARTESIAN_POINT('Ctrl Pts',(4.90565273067095,21.77100742197,-14.6895517266055));
#27433=CARTESIAN_POINT('Ctrl Pts',(6.42158279295009,21.6440074219702,-12.6030529961857));
#27434=CARTESIAN_POINT('Ctrl Pts',(7.93751285522926,21.5170074219701,-10.5165542657659));
#27435=CARTESIAN_POINT('Ctrl Pts',(7.93751285522927,21.3900074219701,-7.93750000000004));
#27436=CARTESIAN_POINT('Ctrl Pts',(7.93751285522931,21.26300742197,-5.35844573423412));
#27437=CARTESIAN_POINT('Ctrl Pts',(6.42158279295009,21.13600742197,-3.27194700381427));
#27438=CARTESIAN_POINT('Ctrl Pts',(5.62930008354685,21.0696323914868,-2.18146340668965));
#27439=CARTESIAN_POINT('Ctrl Pts',(4.52145020702022,20.9998588479374,-1.41365156886918));
#27440=CARTESIAN_POINT('Ctrl Pts',(0.0471929759279855,20.7180654494099,
1.68729896628553));
#27441=CARTESIAN_POINT('Ctrl Pts',(-4.42706425516419,20.4362720508822,4.78824950144024));
#27442=CARTESIAN_POINT('Ctrl Pts',(6.56268467749999,20.5962500034686,-7.93750000000004));
#27443=CARTESIAN_POINT('Ctrl Pts',(6.56268467749997,20.4692500034686,-5.80515448811441));
#27444=CARTESIAN_POINT('Ctrl Pts',(5.3093234328217,20.3422500034686,-4.08005073111972));
#27445=CARTESIAN_POINT('Ctrl Pts',(4.65426916952368,20.2758749724933,-3.1784458861888));
#27446=CARTESIAN_POINT('Ctrl Pts',(3.7383059945976,20.2061014284303,-2.54362398482789));
#27447=CARTESIAN_POINT('Origin',(-2.53888687851145E-9,74.888750003468,-7.9374999999999));
#27448=CARTESIAN_POINT('Ctrl Pts',(6.56268467749999,19.9612500034686,-7.93750000000004));
#27449=CARTESIAN_POINT('Ctrl Pts',(6.56268467750003,19.8342500034686,-5.80515448811441));
#27450=CARTESIAN_POINT('Ctrl Pts',(5.30932343282159,19.7072500034685,-4.08005073111972));
#27451=CARTESIAN_POINT('Ctrl Pts',(4.6542690872318,19.6408749641548,-3.17844577292378));
#27452=CARTESIAN_POINT('Ctrl Pts',(3.73830577091051,19.5711014113908,-2.54362382979823));
#27453=CARTESIAN_POINT('Ctrl Pts',(-7.93749999999999,73.7775000069372,-7.93749999999999));
#27454=CARTESIAN_POINT('Ctrl Pts',(-7.93749999999997,73.6505000069372,-10.5165500888487));
#27455=CARTESIAN_POINT('Ctrl Pts',(-6.42157239285113,73.5235000069373,-12.6030454400715));
#27456=CARTESIAN_POINT('Ctrl Pts',(-4.90564478570226,73.3965000069372,-14.6895407912943));
#27457=CARTESIAN_POINT('Ctrl Pts',(-2.45282239285111,73.2695000069373,-15.4865110980928));
#27458=CARTESIAN_POINT('Ctrl Pts',(0.,73.1425000069373,-16.2834814048913));
#27459=CARTESIAN_POINT('Ctrl Pts',(2.45282239285127,73.0155000069373,-15.4865110980928));
#27460=CARTESIAN_POINT('Ctrl Pts',(4.90564478570231,72.8885000069371,-14.6895407912943));
#27461=CARTESIAN_POINT('Ctrl Pts',(6.42157239285118,72.7615000069373,-12.6030454400715));
#27462=CARTESIAN_POINT('Ctrl Pts',(7.93750000000003,72.6345000069371,-10.5165500888487));
#27463=CARTESIAN_POINT('Ctrl Pts',(7.9375000000001,72.5075000069372,-7.93749999999999));
#27464=CARTESIAN_POINT('Ctrl Pts',(7.93749999999997,72.3805000069372,-5.35844991115131));
#27465=CARTESIAN_POINT('Ctrl Pts',(6.42157239285124,72.2535000069372,-3.27195455992851));
#27466=CARTESIAN_POINT('Ctrl Pts',(4.90564478570231,72.1265000069371,-1.18545920870573));
#27467=CARTESIAN_POINT('Ctrl Pts',(2.45282239285116,71.9995000069372,-0.38848890190718));
#27468=CARTESIAN_POINT('Ctrl Pts',(0.,71.8725000069372,0.408481404891264));
#27469=CARTESIAN_POINT('Ctrl Pts',(-2.45282239285105,71.7455000069372,-0.38848890190718));
#27470=CARTESIAN_POINT('Ctrl Pts',(-4.90564478570226,71.6185000069372,-1.18545920870573));
#27471=CARTESIAN_POINT('Ctrl Pts',(-6.42157239285113,71.4915000069372,-3.2719545599284));
#27472=CARTESIAN_POINT('Ctrl Pts',(-7.93750000000003,71.3645000069373,-5.35844991115131));
#27473=CARTESIAN_POINT('Ctrl Pts',(-7.93749999999999,71.2375000069373,-7.93749999999999));
#27474=CARTESIAN_POINT('Ctrl Pts',(-7.93750000000003,71.1105000069372,-10.5165500888487));
#27475=CARTESIAN_POINT('Ctrl Pts',(-6.42157239285113,70.9835000069373,-12.6030454400715));
#27476=CARTESIAN_POINT('Ctrl Pts',(-4.90564478570226,70.8565000069373,-14.6895407912943));
#27477=CARTESIAN_POINT('Ctrl Pts',(-2.45282239285105,70.7295000069373,-15.4865110980928));
#27478=CARTESIAN_POINT('Ctrl Pts',(0.,70.6025000069372,-16.2834814048913));
#27479=CARTESIAN_POINT('Ctrl Pts',(2.45282239285127,70.4755000069374,-15.4865110980928));
#27480=CARTESIAN_POINT('Ctrl Pts',(4.90564478570231,70.3485000069372,-14.6895407912943));
#27481=CARTESIAN_POINT('Ctrl Pts',(6.42157239285118,70.2215000069373,-12.6030454400715));
#27482=CARTESIAN_POINT('Ctrl Pts',(7.93750000000003,70.0945000069371,-10.5165500888487));
#27483=CARTESIAN_POINT('Ctrl Pts',(7.9375000000001,69.9675000069372,-7.93749999999999));
#27484=CARTESIAN_POINT('Ctrl Pts',(7.93749999999997,69.8405000069372,-5.35844991115131));
#27485=CARTESIAN_POINT('Ctrl Pts',(6.42157239285124,69.7135000069371,-3.27195455992851));
#27486=CARTESIAN_POINT('Ctrl Pts',(4.90564478570231,69.5865000069372,-1.18545920870573));
#27487=CARTESIAN_POINT('Ctrl Pts',(2.45282239285122,69.4595000069373,-0.38848890190718));
#27488=CARTESIAN_POINT('Ctrl Pts',(-5.83678785436452E-14,69.3325000069372,
0.408481404891264));
#27489=CARTESIAN_POINT('Ctrl Pts',(-2.45282239285111,69.2055000069372,-0.38848890190718));
#27490=CARTESIAN_POINT('Ctrl Pts',(-4.90564478570231,69.0785000069372,-1.18545920870573));
#27491=CARTESIAN_POINT('Ctrl Pts',(-6.42157239285113,68.9515000069372,-3.2719545599284));
#27492=CARTESIAN_POINT('Ctrl Pts',(-7.93750000000003,68.8245000069372,-5.35844991115131));
#27493=CARTESIAN_POINT('Ctrl Pts',(-7.93749999999999,68.6975000069372,-7.93749999999999));
#27494=CARTESIAN_POINT('Ctrl Pts',(-7.93749999999991,68.5705000069372,-10.5165500888487));
#27495=CARTESIAN_POINT('Ctrl Pts',(-6.42157239285113,68.4435000069374,-12.6030454400715));
#27496=CARTESIAN_POINT('Ctrl Pts',(-4.90564478570231,68.3165000069372,-14.6895407912943));
#27497=CARTESIAN_POINT('Ctrl Pts',(-2.45282239285116,68.1895000069373,-15.4865110980928));
#27498=CARTESIAN_POINT('Ctrl Pts',(-1.1673575708729E-13,68.0625000069372,
-16.2834814048913));
#27499=CARTESIAN_POINT('Ctrl Pts',(2.45282239285116,67.9355000069373,-15.4865110980928));
#27500=CARTESIAN_POINT('Ctrl Pts',(4.90564478570231,67.8085000069373,-14.6895407912943));
#27501=CARTESIAN_POINT('Ctrl Pts',(6.42157239285124,67.6815000069373,-12.6030454400715));
#27502=CARTESIAN_POINT('Ctrl Pts',(7.93750000000003,67.5545000069373,-10.5165500888487));
#27503=CARTESIAN_POINT('Ctrl Pts',(7.93749999999999,67.4275000069372,-7.93749999999999));
#27504=CARTESIAN_POINT('Ctrl Pts',(7.93750000000009,67.3005000069372,-5.35844991115131));
#27505=CARTESIAN_POINT('Ctrl Pts',(6.42157239285113,67.1735000069372,-3.27195455992851));
#27506=CARTESIAN_POINT('Ctrl Pts',(4.9056447857022,67.0465000069371,-1.18545920870573));
#27507=CARTESIAN_POINT('Ctrl Pts',(2.45282239285116,66.9195000069373,-0.38848890190718));
#27508=CARTESIAN_POINT('Ctrl Pts',(5.83678785436452E-14,66.7925000069371,
0.408481404891264));
#27509=CARTESIAN_POINT('Ctrl Pts',(-2.45282239285122,66.6655000069371,-0.38848890190718));
#27510=CARTESIAN_POINT('Ctrl Pts',(-4.9056447857022,66.5385000069372,-1.18545920870573));
#27511=CARTESIAN_POINT('Ctrl Pts',(-6.42157239285113,66.4115000069373,-3.2719545599284));
#27512=CARTESIAN_POINT('Ctrl Pts',(-7.93749999999997,66.2845000069373,-5.35844991115131));
#27513=CARTESIAN_POINT('Ctrl Pts',(-7.93749999999999,66.1575000069372,-7.93749999999999));
#27514=CARTESIAN_POINT('Ctrl Pts',(-7.93750000000003,66.0305000069372,-10.5165500888487));
#27515=CARTESIAN_POINT('Ctrl Pts',(-6.42157239285107,65.9035000069373,-12.6030454400715));
#27516=CARTESIAN_POINT('Ctrl Pts',(-4.9056447857022,65.7765000069371,-14.6895407912943));
#27517=CARTESIAN_POINT('Ctrl Pts',(-2.45282239285116,65.6495000069373,-15.4865110980928));
#27518=CARTESIAN_POINT('Ctrl Pts',(1.1673575708729E-13,65.5225000069372,
-16.2834814048913));
#27519=CARTESIAN_POINT('Ctrl Pts',(2.45282239285105,65.3955000069373,-15.4865110980928));
#27520=CARTESIAN_POINT('Ctrl Pts',(4.90564478570237,65.2685000069372,-14.6895407912943));
#27521=CARTESIAN_POINT('Ctrl Pts',(6.42157239285124,65.1415000069373,-12.6030454400715));
#27522=CARTESIAN_POINT('Ctrl Pts',(7.93749999999991,65.0145000069372,-10.5165500888487));
#27523=CARTESIAN_POINT('Ctrl Pts',(7.93749999999999,64.8875000069373,-7.93749999999999));
#27524=CARTESIAN_POINT('Ctrl Pts',(7.93750000000003,64.7605000069372,-5.35844991115131));
#27525=CARTESIAN_POINT('Ctrl Pts',(6.42157239285113,64.6335000069372,-3.2719545599284));
#27526=CARTESIAN_POINT('Ctrl Pts',(4.90564478570231,64.5065000069371,-1.18545920870573));
#27527=CARTESIAN_POINT('Ctrl Pts',(2.45282239285116,64.3795000069372,-0.38848890190718));
#27528=CARTESIAN_POINT('Ctrl Pts',(1.1673575708729E-13,64.2525000069372,
0.408481404891264));
#27529=CARTESIAN_POINT('Ctrl Pts',(-2.45282239285116,64.1255000069372,-0.38848890190718));
#27530=CARTESIAN_POINT('Ctrl Pts',(-4.90564478570231,63.9985000069371,-1.18545920870573));
#27531=CARTESIAN_POINT('Ctrl Pts',(-6.42157239285107,63.8715000069372,-3.2719545599284));
#27532=CARTESIAN_POINT('Ctrl Pts',(-7.93749999999997,63.7445000069372,-5.35844991115131));
#27533=CARTESIAN_POINT('Ctrl Pts',(-7.93749999999999,63.6175000069372,-7.93749999999999));
#27534=CARTESIAN_POINT('Ctrl Pts',(-7.93750000000003,63.4905000069372,-10.5165500888487));
#27535=CARTESIAN_POINT('Ctrl Pts',(-6.42157239285118,63.3635000069373,-12.6030454400715));
#27536=CARTESIAN_POINT('Ctrl Pts',(-4.9056447857022,63.2365000069372,-14.6895407912943));
#27537=CARTESIAN_POINT('Ctrl Pts',(-2.45282239285116,63.1095000069373,-15.4865110980928));
#27538=CARTESIAN_POINT('Ctrl Pts',(0.,62.9825000069372,-16.2834814048913));
#27539=CARTESIAN_POINT('Ctrl Pts',(2.45282239285111,62.8555000069373,-15.4865110980928));
#27540=CARTESIAN_POINT('Ctrl Pts',(4.90564478570226,62.7285000069371,-14.6895407912943));
#27541=CARTESIAN_POINT('Ctrl Pts',(6.42157239285113,62.6015000069373,-12.6030454400715));
#27542=CARTESIAN_POINT('Ctrl Pts',(7.93750000000003,62.4745000069372,-10.5165500888487));
#27543=CARTESIAN_POINT('Ctrl Pts',(7.93750000000004,62.3475000069372,-7.93749999999999));
#27544=CARTESIAN_POINT('Ctrl Pts',(7.93750000000003,62.2205000069372,-5.35844991115131));
#27545=CARTESIAN_POINT('Ctrl Pts',(6.42157239285118,62.0935000069373,-3.2719545599284));
#27546=CARTESIAN_POINT('Ctrl Pts',(4.90564478570226,61.9665000069372,-1.18545920870573));
#27547=CARTESIAN_POINT('Ctrl Pts',(2.45282239285116,61.8395000069372,-0.38848890190718));
#27548=CARTESIAN_POINT('Ctrl Pts',(0.,61.7125000069371,0.408481404891264));
#27549=CARTESIAN_POINT('Ctrl Pts',(-2.45282239285116,61.5855000069373,-0.38848890190718));
#27550=CARTESIAN_POINT('Ctrl Pts',(-4.90564478570231,61.4585000069373,-1.18545920870573));
#27551=CARTESIAN_POINT('Ctrl Pts',(-6.42157239285113,61.3315000069372,-3.2719545599284));
#27552=CARTESIAN_POINT('Ctrl Pts',(-7.93749999999997,61.2045000069371,-5.35844991115131));
#27553=CARTESIAN_POINT('Ctrl Pts',(-7.93749999999993,61.0775000069371,-7.93749999999999));
#27554=CARTESIAN_POINT('Ctrl Pts',(-7.93750000000003,60.9505000069371,-10.5165500888487));
#27555=CARTESIAN_POINT('Ctrl Pts',(-6.42157239285113,60.8235000069373,-12.6030454400715));
#27556=CARTESIAN_POINT('Ctrl Pts',(-4.90564478570231,60.6965000069371,-14.6895407912943));
#27557=CARTESIAN_POINT('Ctrl Pts',(-2.45282239285111,60.5695000069374,-15.4865110980928));
#27558=CARTESIAN_POINT('Ctrl Pts',(0.,60.4425000069371,-16.2834814048913));
#27559=CARTESIAN_POINT('Ctrl Pts',(2.45282239285116,60.3155000069373,-15.4865110980928));
#27560=CARTESIAN_POINT('Ctrl Pts',(4.90564478570237,60.1885000069372,-14.6895407912943));
#27561=CARTESIAN_POINT('Ctrl Pts',(6.42157239285113,60.0615000069373,-12.6030454400715));
#27562=CARTESIAN_POINT('Ctrl Pts',(7.93749999999997,59.9345000069372,-10.5165500888487));
#27563=CARTESIAN_POINT('Ctrl Pts',(7.93750000000004,59.8075000069372,-7.93749999999999));
#27564=CARTESIAN_POINT('Ctrl Pts',(7.93750000000003,59.6805000069371,-5.35844991115131));
#27565=CARTESIAN_POINT('Ctrl Pts',(6.42157239285118,59.5535000069372,-3.2719545599284));
#27566=CARTESIAN_POINT('Ctrl Pts',(4.90564478570226,59.4265000069372,-1.18545920870573));
#27567=CARTESIAN_POINT('Ctrl Pts',(2.45282239285116,59.2995000069371,-0.38848890190718));
#27568=CARTESIAN_POINT('Ctrl Pts',(1.1673575708729E-13,59.1725000069372,
0.408481404891264));
#27569=CARTESIAN_POINT('Ctrl Pts',(-2.45282239285116,59.0455000069372,-0.38848890190718));
#27570=CARTESIAN_POINT('Ctrl Pts',(-4.90564478570231,58.9185000069372,-1.18545920870573));
#27571=CARTESIAN_POINT('Ctrl Pts',(-6.42157239285113,58.7915000069372,-3.2719545599284));
#27572=CARTESIAN_POINT('Ctrl Pts',(-7.93750000000003,58.6645000069372,-5.35844991115131));
#27573=CARTESIAN_POINT('Ctrl Pts',(-7.93750000000004,58.5375000069372,-7.93749999999999));
#27574=CARTESIAN_POINT('Ctrl Pts',(-7.93749999999997,58.4105000069373,-10.5165500888487));
#27575=CARTESIAN_POINT('Ctrl Pts',(-6.42157239285113,58.2835000069372,-12.6030454400715));
#27576=CARTESIAN_POINT('Ctrl Pts',(-4.90564478570231,58.1565000069371,-14.6895407912943));
#27577=CARTESIAN_POINT('Ctrl Pts',(-2.45282239285122,58.0295000069373,-15.4865110980928));
#27578=CARTESIAN_POINT('Ctrl Pts',(5.83678785436452E-14,57.9025000069372,
-16.2834814048913));
#27579=CARTESIAN_POINT('Ctrl Pts',(2.45282239285116,57.7755000069372,-15.4865110980928));
#27580=CARTESIAN_POINT('Ctrl Pts',(4.90564478570231,57.6485000069371,-14.6895407912943));
#27581=CARTESIAN_POINT('Ctrl Pts',(6.42157239285118,57.5215000069373,-12.6030454400715));
#27582=CARTESIAN_POINT('Ctrl Pts',(7.93749999999997,57.3945000069372,-10.5165500888487));
#27583=CARTESIAN_POINT('Ctrl Pts',(7.9375000000001,57.2675000069372,-7.93749999999999));
#27584=CARTESIAN_POINT('Ctrl Pts',(7.93750000000003,57.1405000069372,-5.35844991115131));
#27585=CARTESIAN_POINT('Ctrl Pts',(6.42157239285124,57.0135000069372,-3.2719545599284));
#27586=CARTESIAN_POINT('Ctrl Pts',(4.90564478570237,56.8865000069372,-1.18545920870573));
#27587=CARTESIAN_POINT('Ctrl Pts',(2.45282239285105,56.7595000069371,-0.38848890190718));
#27588=CARTESIAN_POINT('Ctrl Pts',(0.,56.6325000069371,0.408481404891264));
#27589=CARTESIAN_POINT('Ctrl Pts',(-2.45282239285116,56.5055000069372,-0.38848890190718));
#27590=CARTESIAN_POINT('Ctrl Pts',(-4.90564478570226,56.3785000069372,-1.18545920870573));
#27591=CARTESIAN_POINT('Ctrl Pts',(-6.42157239285113,56.2515000069372,-3.2719545599284));
#27592=CARTESIAN_POINT('Ctrl Pts',(-7.93749999999991,56.1245000069371,-5.35844991115131));
#27593=CARTESIAN_POINT('Ctrl Pts',(-7.93749999999999,55.9975000069372,-7.93749999999999));
#27594=CARTESIAN_POINT('Ctrl Pts',(-7.93749999999997,55.8705000069372,-10.5165500888487));
#27595=CARTESIAN_POINT('Ctrl Pts',(-6.42157239285113,55.7435000069373,-12.6030454400715));
#27596=CARTESIAN_POINT('Ctrl Pts',(-4.90564478570231,55.6165000069373,-14.6895407912943));
#27597=CARTESIAN_POINT('Ctrl Pts',(-2.45282239285116,55.4895000069373,-15.4865110980928));
#27598=CARTESIAN_POINT('Ctrl Pts',(0.,55.3625000069372,-16.2834814048913));
#27599=CARTESIAN_POINT('Ctrl Pts',(2.45282239285116,55.2355000069373,-15.4865110980928));
#27600=CARTESIAN_POINT('Ctrl Pts',(4.90564478570231,55.1085000069371,-14.6895407912943));
#27601=CARTESIAN_POINT('Ctrl Pts',(6.42157239285118,54.9815000069373,-12.6030454400715));
#27602=CARTESIAN_POINT('Ctrl Pts',(7.93750000000009,54.8545000069371,-10.5165500888487));
#27603=CARTESIAN_POINT('Ctrl Pts',(7.9375000000001,54.7275000069372,-7.93750000000004));
#27604=CARTESIAN_POINT('Ctrl Pts',(7.93749999999991,54.6005000069371,-5.35844991115131));
#27605=CARTESIAN_POINT('Ctrl Pts',(6.42157239285124,54.4735000069372,-3.27195455992846));
#27606=CARTESIAN_POINT('Ctrl Pts',(4.90564478570231,54.3465000069372,-1.18545920870573));
#27607=CARTESIAN_POINT('Ctrl Pts',(2.45282239285111,54.2195000069373,-0.388488901907236));
#27608=CARTESIAN_POINT('Ctrl Pts',(0.,54.0925000069371,0.408481404891264));
#27609=CARTESIAN_POINT('Ctrl Pts',(-2.45282239285111,53.9655000069372,-0.388488901907236));
#27610=CARTESIAN_POINT('Ctrl Pts',(-4.90564478570226,53.8385000069372,-1.18545920870573));
#27611=CARTESIAN_POINT('Ctrl Pts',(-6.42157239285113,53.7115000069372,-3.27195455992846));
#27612=CARTESIAN_POINT('Ctrl Pts',(-7.93750000000003,53.5845000069372,-5.35844991115131));
#27613=CARTESIAN_POINT('Ctrl Pts',(-7.93749999999999,53.4575000069372,-7.93750000000004));
#27614=CARTESIAN_POINT('Ctrl Pts',(-7.93749999999997,53.3305000069372,-10.5165500888487));
#27615=CARTESIAN_POINT('Ctrl Pts',(-6.42157239285113,53.2035000069373,-12.6030454400715));
#27616=CARTESIAN_POINT('Ctrl Pts',(-4.90564478570231,53.0765000069372,-14.6895407912943));
#27617=CARTESIAN_POINT('Ctrl Pts',(-2.45282239285116,52.9495000069372,-15.4865110980928));
#27618=CARTESIAN_POINT('Ctrl Pts',(0.,52.8225000069372,-16.2834814048913));
#27619=CARTESIAN_POINT('Ctrl Pts',(2.45282239285116,52.6955000069374,-15.4865110980928));
#27620=CARTESIAN_POINT('Ctrl Pts',(4.90564478570231,52.5685000069372,-14.6895407912943));
#27621=CARTESIAN_POINT('Ctrl Pts',(6.42157239285124,52.4415000069373,-12.6030454400715));
#27622=CARTESIAN_POINT('Ctrl Pts',(7.93749999999997,52.3145000069372,-10.5165500888487));
#27623=CARTESIAN_POINT('Ctrl Pts',(7.9375000000001,52.1875000069372,-7.93750000000004));
#27624=CARTESIAN_POINT('Ctrl Pts',(7.93750000000009,52.0605000069371,-5.35844991115131));
#27625=CARTESIAN_POINT('Ctrl Pts',(6.42157239285124,51.9335000069372,-3.27195455992846));
#27626=CARTESIAN_POINT('Ctrl Pts',(4.90564478570231,51.8065000069371,-1.18545920870573));
#27627=CARTESIAN_POINT('Ctrl Pts',(2.45282239285116,51.6795000069372,-0.388488901907236));
#27628=CARTESIAN_POINT('Ctrl Pts',(0.,51.5525000069372,0.408481404891264));
#27629=CARTESIAN_POINT('Ctrl Pts',(-2.45282239285122,51.4255000069372,-0.388488901907236));
#27630=CARTESIAN_POINT('Ctrl Pts',(-4.90564478570226,51.2985000069372,-1.18545920870573));
#27631=CARTESIAN_POINT('Ctrl Pts',(-6.42157239285113,51.1715000069372,-3.27195455992846));
#27632=CARTESIAN_POINT('Ctrl Pts',(-7.93750000000003,51.0445000069372,-5.35844991115131));
#27633=CARTESIAN_POINT('Ctrl Pts',(-7.93749999999999,50.9175000069372,-7.93750000000004));
#27634=CARTESIAN_POINT('Ctrl Pts',(-7.93749999999997,50.7905000069372,-10.5165500888487));
#27635=CARTESIAN_POINT('Ctrl Pts',(-6.42157239285107,50.6635000069373,-12.6030454400715));
#27636=CARTESIAN_POINT('Ctrl Pts',(-4.90564478570237,50.5365000069371,-14.6895407912943));
#27637=CARTESIAN_POINT('Ctrl Pts',(-2.45282239285116,50.4095000069373,-15.4865110980928));
#27638=CARTESIAN_POINT('Ctrl Pts',(0.,50.2825000069372,-16.2834814048913));
#27639=CARTESIAN_POINT('Ctrl Pts',(2.45282239285105,50.1555000069373,-15.4865110980928));
#27640=CARTESIAN_POINT('Ctrl Pts',(4.90564478570231,50.0285000069372,-14.6895407912943));
#27641=CARTESIAN_POINT('Ctrl Pts',(6.42157239285124,49.9015000069373,-12.6030454400715));
#27642=CARTESIAN_POINT('Ctrl Pts',(7.93750000000003,49.7745000069372,-10.5165500888487));
#27643=CARTESIAN_POINT('Ctrl Pts',(7.93749999999999,49.6475000069372,-7.93750000000004));
#27644=CARTESIAN_POINT('Ctrl Pts',(7.93750000000009,49.5205000069372,-5.35844991115131));
#27645=CARTESIAN_POINT('Ctrl Pts',(6.42157239285113,49.3935000069372,-3.27195455992846));
#27646=CARTESIAN_POINT('Ctrl Pts',(4.90564478570231,49.2665000069372,-1.18545920870573));
#27647=CARTESIAN_POINT('Ctrl Pts',(2.45282239285116,49.1395000069372,-0.388488901907236));
#27648=CARTESIAN_POINT('Ctrl Pts',(0.,49.0125000069372,0.408481404891264));
#27649=CARTESIAN_POINT('Ctrl Pts',(-2.45282239285116,48.8855000069372,-0.388488901907236));
#27650=CARTESIAN_POINT('Ctrl Pts',(-4.90564478570226,48.7585000069371,-1.18545920870573));
#27651=CARTESIAN_POINT('Ctrl Pts',(-6.42157239285107,48.6315000069372,-3.27195455992846));
#27652=CARTESIAN_POINT('Ctrl Pts',(-7.93750000000003,48.5045000069372,-5.35844991115131));
#27653=CARTESIAN_POINT('Ctrl Pts',(-7.93749999999999,48.3775000069372,-7.93750000000004));
#27654=CARTESIAN_POINT('Ctrl Pts',(-7.93750000000003,48.2505000069372,-10.5165500888487));
#27655=CARTESIAN_POINT('Ctrl Pts',(-6.42157239285107,48.1235000069373,-12.6030454400715));
#27656=CARTESIAN_POINT('Ctrl Pts',(-4.90564478570226,47.9965000069372,-14.6895407912943));
#27657=CARTESIAN_POINT('Ctrl Pts',(-2.45282239285116,47.8695000069373,-15.4865110980928));
#27658=CARTESIAN_POINT('Ctrl Pts',(0.,47.7425000069372,-16.2834814048913));
#27659=CARTESIAN_POINT('Ctrl Pts',(2.45282239285111,47.6155000069373,-15.4865110980928));
#27660=CARTESIAN_POINT('Ctrl Pts',(4.90564478570231,47.4885000069371,-14.6895407912943));
#27661=CARTESIAN_POINT('Ctrl Pts',(6.42157239285113,47.3615000069373,-12.6030454400715));
#27662=CARTESIAN_POINT('Ctrl Pts',(7.93750000000003,47.2345000069372,-10.5165500888487));
#27663=CARTESIAN_POINT('Ctrl Pts',(7.93750000000004,47.1075000069372,-7.93750000000004));
#27664=CARTESIAN_POINT('Ctrl Pts',(7.93749999999997,46.9805000069371,-5.35844991115131));
#27665=CARTESIAN_POINT('Ctrl Pts',(6.42157239285118,46.8535000069372,-3.27195455992846));
#27666=CARTESIAN_POINT('Ctrl Pts',(4.90564478570231,46.7265000069371,-1.18545920870573));
#27667=CARTESIAN_POINT('Ctrl Pts',(2.45282239285116,46.5995000069372,-0.388488901907236));
#27668=CARTESIAN_POINT('Ctrl Pts',(-5.83678785436452E-14,46.4725000069372,
0.408481404891264));
#27669=CARTESIAN_POINT('Ctrl Pts',(-2.45282239285116,46.3455000069373,-0.388488901907236));
#27670=CARTESIAN_POINT('Ctrl Pts',(-4.90564478570231,46.2185000069372,-1.18545920870573));
#27671=CARTESIAN_POINT('Ctrl Pts',(-6.42157239285107,46.0915000069372,-3.27195455992846));
#27672=CARTESIAN_POINT('Ctrl Pts',(-7.93749999999997,45.9645000069371,-5.35844991115131));
#27673=CARTESIAN_POINT('Ctrl Pts',(-7.93749999999993,45.8375000069371,-7.93750000000004));
#27674=CARTESIAN_POINT('Ctrl Pts',(-7.93749999999991,45.7105000069371,-10.5165500888487));
#27675=CARTESIAN_POINT('Ctrl Pts',(-6.42157239285113,45.5835000069373,-12.6030454400715));
#27676=CARTESIAN_POINT('Ctrl Pts',(-4.90564478570231,45.4565000069371,-14.6895407912943));
#27677=CARTESIAN_POINT('Ctrl Pts',(-2.45282239285111,45.3295000069374,-15.4865110980928));
#27678=CARTESIAN_POINT('Ctrl Pts',(-5.83678785436452E-14,45.2025000069371,
-16.2834814048912));
#27679=CARTESIAN_POINT('Ctrl Pts',(2.45282239285116,45.0755000069373,-15.4865110980928));
#27680=CARTESIAN_POINT('Ctrl Pts',(4.90564478570237,44.9485000069372,-14.6895407912943));
#27681=CARTESIAN_POINT('Ctrl Pts',(6.42157239285113,44.8215000069374,-12.6030454400715));
#27682=CARTESIAN_POINT('Ctrl Pts',(7.93750000000003,44.6945000069372,-10.5165500888487));
#27683=CARTESIAN_POINT('Ctrl Pts',(7.93750000000004,44.5675000069372,-7.93750000000004));
#27684=CARTESIAN_POINT('Ctrl Pts',(7.93750000000009,44.4405000069371,-5.35844991115131));
#27685=CARTESIAN_POINT('Ctrl Pts',(6.42157239285118,44.3135000069372,-3.27195455992846));
#27686=CARTESIAN_POINT('Ctrl Pts',(4.9056447857022,44.1865000069372,-1.18545920870573));
#27687=CARTESIAN_POINT('Ctrl Pts',(2.45282239285116,44.0595000069372,-0.388488901907236));
#27688=CARTESIAN_POINT('Ctrl Pts',(0.,43.9325000069372,0.408481404891264));
#27689=CARTESIAN_POINT('Ctrl Pts',(-2.45282239285116,43.8055000069373,-0.388488901907236));
#27690=CARTESIAN_POINT('Ctrl Pts',(-4.9056447857022,43.6785000069372,-1.18545920870573));
#27691=CARTESIAN_POINT('Ctrl Pts',(-6.42157239285113,43.5515000069372,-3.27195455992846));
#27692=CARTESIAN_POINT('Ctrl Pts',(-7.93749999999997,43.4245000069372,-5.35844991115131));
#27693=CARTESIAN_POINT('Ctrl Pts',(-7.93749999999993,43.2975000069372,-7.93750000000004));
#27694=CARTESIAN_POINT('Ctrl Pts',(-7.93750000000003,43.1705000069372,-10.5165500888487));
#27695=CARTESIAN_POINT('Ctrl Pts',(-6.42157239285113,43.0435000069372,-12.6030454400715));
#27696=CARTESIAN_POINT('Ctrl Pts',(-4.90564478570231,42.9165000069372,-14.6895407912943));
#27697=CARTESIAN_POINT('Ctrl Pts',(-2.45282239285116,42.7895000069373,-15.4865110980928));
#27698=CARTESIAN_POINT('Ctrl Pts',(1.1673575708729E-13,42.6625000069372,
-16.2834814048912));
#27699=CARTESIAN_POINT('Ctrl Pts',(2.45282239285116,42.5355000069372,-15.4865110980928));
#27700=CARTESIAN_POINT('Ctrl Pts',(4.90564478570237,42.4085000069371,-14.6895407912943));
#27701=CARTESIAN_POINT('Ctrl Pts',(6.42157239285118,42.2815000069373,-12.6030454400715));
#27702=CARTESIAN_POINT('Ctrl Pts',(7.93749999999991,42.1545000069372,-10.5165500888487));
#27703=CARTESIAN_POINT('Ctrl Pts',(7.9375000000001,42.0275000069373,-7.93750000000004));
#27704=CARTESIAN_POINT('Ctrl Pts',(7.93750000000003,41.9005000069372,-5.35844991115131));
#27705=CARTESIAN_POINT('Ctrl Pts',(6.42157239285124,41.7735000069372,-3.27195455992846));
#27706=CARTESIAN_POINT('Ctrl Pts',(4.90564478570231,41.6465000069372,-1.18545920870573));
#27707=CARTESIAN_POINT('Ctrl Pts',(2.45282239285105,41.5195000069371,-0.388488901907236));
#27708=CARTESIAN_POINT('Ctrl Pts',(1.1673575708729E-13,41.3925000069372,
0.408481404891264));
#27709=CARTESIAN_POINT('Ctrl Pts',(-2.45282239285116,41.2655000069372,-0.388488901907236));
#27710=CARTESIAN_POINT('Ctrl Pts',(-4.90564478570231,41.1385000069372,-1.18545920870573));
#27711=CARTESIAN_POINT('Ctrl Pts',(-6.42157239285113,41.0115000069372,-3.27195455992846));
#27712=CARTESIAN_POINT('Ctrl Pts',(-7.93749999999997,40.8845000069371,-5.35844991115131));
#27713=CARTESIAN_POINT('Ctrl Pts',(-7.93749999999999,40.7575000069372,-7.93750000000004));
#27714=CARTESIAN_POINT('Ctrl Pts',(-7.93750000000003,40.6305000069372,-10.5165500888487));
#27715=CARTESIAN_POINT('Ctrl Pts',(-6.42157239285113,40.5035000069373,-12.6030454400715));
#27716=CARTESIAN_POINT('Ctrl Pts',(-4.9056447857022,40.3765000069371,-14.6895407912943));
#27717=CARTESIAN_POINT('Ctrl Pts',(-2.45282239285116,40.2495000069373,-15.4865110980928));
#27718=CARTESIAN_POINT('Ctrl Pts',(0.,40.1225000069371,-16.2834814048912));
#27719=CARTESIAN_POINT('Ctrl Pts',(2.45282239285116,39.9955000069373,-15.4865110980928));
#27720=CARTESIAN_POINT('Ctrl Pts',(4.90564478570226,39.868500006937,-14.6895407912943));
#27721=CARTESIAN_POINT('Ctrl Pts',(6.42157239285118,39.7415000069373,-12.6030454400715));
#27722=CARTESIAN_POINT('Ctrl Pts',(7.93750000000009,39.6145000069371,-10.5165500888487));
#27723=CARTESIAN_POINT('Ctrl Pts',(7.9375000000001,39.4875000069372,-7.93750000000004));
#27724=CARTESIAN_POINT('Ctrl Pts',(7.93750000000003,39.3605000069371,-5.35844991115131));
#27725=CARTESIAN_POINT('Ctrl Pts',(6.42157239285124,39.2335000069372,-3.27195455992846));
#27726=CARTESIAN_POINT('Ctrl Pts',(4.90564478570226,39.1065000069372,-1.18545920870573));
#27727=CARTESIAN_POINT('Ctrl Pts',(2.45282239285111,38.9795000069372,-0.388488901907236));
#27728=CARTESIAN_POINT('Ctrl Pts',(0.,38.8525000069371,0.408481404891264));
#27729=CARTESIAN_POINT('Ctrl Pts',(-2.45282239285111,38.7255000069372,-0.388488901907236));
#27730=CARTESIAN_POINT('Ctrl Pts',(-4.90564478570231,38.5985000069372,-1.18545920870573));
#27731=CARTESIAN_POINT('Ctrl Pts',(-6.42157239285113,38.4715000069372,-3.27195455992846));
#27732=CARTESIAN_POINT('Ctrl Pts',(-7.93749999999997,38.3445000069371,-5.35844991115131));
#27733=CARTESIAN_POINT('Ctrl Pts',(-7.93749999999999,38.2175000069373,-7.93750000000004));
#27734=CARTESIAN_POINT('Ctrl Pts',(-7.93750000000003,38.0905000069372,-10.5165500888487));
#27735=CARTESIAN_POINT('Ctrl Pts',(-6.42157239285113,37.9635000069373,-12.6030454400715));
#27736=CARTESIAN_POINT('Ctrl Pts',(-4.90564478570231,37.8365000069372,-14.6895407912943));
#27737=CARTESIAN_POINT('Ctrl Pts',(-2.45282239285116,37.7095000069373,-15.4865110980927));
#27738=CARTESIAN_POINT('Ctrl Pts',(0.,37.5825000069371,-16.2834814048912));
#27739=CARTESIAN_POINT('Ctrl Pts',(2.45282239285116,37.4555000069374,-15.4865110980927));
#27740=CARTESIAN_POINT('Ctrl Pts',(4.90564478570237,37.3285000069371,-14.6895407912943));
#27741=CARTESIAN_POINT('Ctrl Pts',(6.42157239285124,37.2015000069372,-12.6030454400715));
#27742=CARTESIAN_POINT('Ctrl Pts',(7.93750000000009,37.0745000069372,-10.5165500888487));
#27743=CARTESIAN_POINT('Ctrl Pts',(7.9375000000001,36.9475000069372,-7.93750000000004));
#27744=CARTESIAN_POINT('Ctrl Pts',(7.93750000000003,36.8205000069372,-5.35844991115131));
#27745=CARTESIAN_POINT('Ctrl Pts',(6.42157239285124,36.6935000069371,-3.27195455992846));
#27746=CARTESIAN_POINT('Ctrl Pts',(4.90564478570226,36.5665000069371,-1.18545920870573));
#27747=CARTESIAN_POINT('Ctrl Pts',(2.45282239285116,36.4395000069373,-0.388488901907236));
#27748=CARTESIAN_POINT('Ctrl Pts',(0.,36.3125000069372,0.408481404891264));
#27749=CARTESIAN_POINT('Ctrl Pts',(-2.45282239285111,36.1855000069372,-0.388488901907236));
#27750=CARTESIAN_POINT('Ctrl Pts',(-4.90564478570231,36.0585000069371,-1.18545920870573));
#27751=CARTESIAN_POINT('Ctrl Pts',(-6.42157239285113,35.9315000069372,-3.27195455992846));
#27752=CARTESIAN_POINT('Ctrl Pts',(-7.93750000000003,35.8045000069372,-5.35844991115131));
#27753=CARTESIAN_POINT('Ctrl Pts',(-7.93749999999999,35.6775000069372,-7.93750000000004));
#27754=CARTESIAN_POINT('Ctrl Pts',(-7.93749999999997,35.5505000069372,-10.5165500888487));
#27755=CARTESIAN_POINT('Ctrl Pts',(-6.42157239285107,35.4235000069373,-12.6030454400715));
#27756=CARTESIAN_POINT('Ctrl Pts',(-4.90564478570231,35.2965000069372,-14.6895407912943));
#27757=CARTESIAN_POINT('Ctrl Pts',(-2.45282239285116,35.1695000069372,-15.4865110980927));
#27758=CARTESIAN_POINT('Ctrl Pts',(1.1673575708729E-13,35.0425000069372,
-16.2834814048912));
#27759=CARTESIAN_POINT('Ctrl Pts',(2.45282239285116,34.9155000069373,-15.4865110980927));
#27760=CARTESIAN_POINT('Ctrl Pts',(4.90564478570231,34.7885000069371,-14.6895407912943));
#27761=CARTESIAN_POINT('Ctrl Pts',(6.42157239285124,34.6615000069373,-12.6030454400715));
#27762=CARTESIAN_POINT('Ctrl Pts',(7.93749999999997,34.5345000069371,-10.5165500888487));
#27763=CARTESIAN_POINT('Ctrl Pts',(7.93750000000004,34.4075000069372,-7.93750000000004));
#27764=CARTESIAN_POINT('Ctrl Pts',(7.93750000000003,34.2805000069372,-5.35844991115131));
#27765=CARTESIAN_POINT('Ctrl Pts',(6.42157239285124,34.1535000069372,-3.27195455992846));
#27766=CARTESIAN_POINT('Ctrl Pts',(4.90564478570237,34.0265000069372,-1.18545920870573));
#27767=CARTESIAN_POINT('Ctrl Pts',(2.45282239285116,33.8995000069372,-0.388488901907236));
#27768=CARTESIAN_POINT('Ctrl Pts',(0.,33.7725000069372,0.408481404891264));
#27769=CARTESIAN_POINT('Ctrl Pts',(-2.45282239285116,33.6455000069371,-0.388488901907236));
#27770=CARTESIAN_POINT('Ctrl Pts',(-4.90564478570226,33.5185000069371,-1.18545920870573));
#27771=CARTESIAN_POINT('Ctrl Pts',(-6.42157239285107,33.3915000069372,-3.27195455992846));
#27772=CARTESIAN_POINT('Ctrl Pts',(-7.93749999999991,33.2645000069372,-5.35844991115131));
#27773=CARTESIAN_POINT('Ctrl Pts',(-7.93749999999999,33.1375000069372,-7.93750000000004));
#27774=CARTESIAN_POINT('Ctrl Pts',(-7.93749999999997,33.0105000069372,-10.5165500888487));
#27775=CARTESIAN_POINT('Ctrl Pts',(-6.42157239285107,32.8835000069373,-12.6030454400715));
#27776=CARTESIAN_POINT('Ctrl Pts',(-4.90564478570231,32.7565000069372,-14.6895407912943));
#27777=CARTESIAN_POINT('Ctrl Pts',(-2.45282239285116,32.6295000069373,-15.4865110980927));
#27778=CARTESIAN_POINT('Ctrl Pts',(0.,32.5025000069372,-16.2834814048912));
#27779=CARTESIAN_POINT('Ctrl Pts',(2.45282239285111,32.3755000069373,-15.4865110980927));
#27780=CARTESIAN_POINT('Ctrl Pts',(4.90564478570231,32.2485000069372,-14.6895407912943));
#27781=CARTESIAN_POINT('Ctrl Pts',(6.42157239285124,32.1215000069373,-12.6030454400715));
#27782=CARTESIAN_POINT('Ctrl Pts',(7.93750000000009,31.9945000069372,-10.5165500888487));
#27783=CARTESIAN_POINT('Ctrl Pts',(7.93750000000004,31.8675000069372,-7.93750000000004));
#27784=CARTESIAN_POINT('Ctrl Pts',(7.93749999999991,31.7405000069372,-5.35844991115131));
#27785=CARTESIAN_POINT('Ctrl Pts',(6.42157239285118,31.6135000069372,-3.27195455992846));
#27786=CARTESIAN_POINT('Ctrl Pts',(4.90564478570231,31.4865000069371,-1.18545920870573));
#27787=CARTESIAN_POINT('Ctrl Pts',(2.45282239285116,31.3595000069372,-0.388488901907236));
#27788=CARTESIAN_POINT('Ctrl Pts',(0.,31.2325000069371,0.408481404891264));
#27789=CARTESIAN_POINT('Ctrl Pts',(-2.45282239285116,31.1055000069372,-0.388488901907236));
#27790=CARTESIAN_POINT('Ctrl Pts',(-4.90564478570226,30.9785000069371,-1.18545920870573));
#27791=CARTESIAN_POINT('Ctrl Pts',(-6.42157239285107,30.8515000069372,-3.27195455992846));
#27792=CARTESIAN_POINT('Ctrl Pts',(-7.93750000000003,30.7245000069372,-5.35844991115131));
#27793=CARTESIAN_POINT('Ctrl Pts',(-7.93749999999993,30.5975000069372,-7.93750000000004));
#27794=CARTESIAN_POINT('Ctrl Pts',(-7.93749999999997,30.4705000069371,-10.5165500888487));
#27795=CARTESIAN_POINT('Ctrl Pts',(-6.42157239285107,30.3435000069373,-12.6030454400715));
#27796=CARTESIAN_POINT('Ctrl Pts',(-4.90564478570226,30.2165000069371,-14.6895407912943));
#27797=CARTESIAN_POINT('Ctrl Pts',(-2.45282239285111,30.0895000069373,-15.4865110980927));
#27798=CARTESIAN_POINT('Ctrl Pts',(0.,29.9625000069372,-16.2834814048912));
#27799=CARTESIAN_POINT('Ctrl Pts',(2.45282239285116,29.8355000069373,-15.4865110980927));
#27800=CARTESIAN_POINT('Ctrl Pts',(4.9056447857022,29.7085000069372,-14.6895407912943));
#27801=CARTESIAN_POINT('Ctrl Pts',(6.42157239285113,29.5815000069373,-12.6030454400715));
#27802=CARTESIAN_POINT('Ctrl Pts',(7.93750000000003,29.4545000069372,-10.5165500888487));
#27803=CARTESIAN_POINT('Ctrl Pts',(7.9375000000001,29.3275000069372,-7.93750000000004));
#27804=CARTESIAN_POINT('Ctrl Pts',(7.93750000000009,29.2005000069372,-5.35844991115131));
#27805=CARTESIAN_POINT('Ctrl Pts',(6.42157239285118,29.0735000069372,-3.27195455992846));
#27806=CARTESIAN_POINT('Ctrl Pts',(4.90564478570231,28.9465000069371,-1.18545920870573));
#27807=CARTESIAN_POINT('Ctrl Pts',(2.45282239285116,28.8195000069372,-0.388488901907236));
#27808=CARTESIAN_POINT('Ctrl Pts',(-1.1673575708729E-13,28.6925000069372,
0.408481404891264));
#27809=CARTESIAN_POINT('Ctrl Pts',(-2.45282239285116,28.5655000069372,-0.388488901907236));
#27810=CARTESIAN_POINT('Ctrl Pts',(-4.90564478570237,28.4385000069371,-1.18545920870573));
#27811=CARTESIAN_POINT('Ctrl Pts',(-6.42157239285102,28.3115000069372,-3.27195455992846));
#27812=CARTESIAN_POINT('Ctrl Pts',(-7.93750000000003,28.1845000069372,-5.35844991115131));
#27813=CARTESIAN_POINT('Ctrl Pts',(-7.93749999999988,28.0575000069372,-7.93750000000004));
#27814=CARTESIAN_POINT('Ctrl Pts',(-7.93749999999997,27.9305000069372,-10.5165500888487));
#27815=CARTESIAN_POINT('Ctrl Pts',(-6.42157239285113,27.8035000069373,-12.6030454400715));
#27816=CARTESIAN_POINT('Ctrl Pts',(-4.90564478570237,27.6765000069372,-14.6895407912943));
#27817=CARTESIAN_POINT('Ctrl Pts',(-2.45282239285111,27.5495000069373,-15.4865110980927));
#27818=CARTESIAN_POINT('Ctrl Pts',(0.,27.4225000069372,-16.2834814048912));
#27819=CARTESIAN_POINT('Ctrl Pts',(2.45282239285116,27.2955000069372,-15.4865110980927));
#27820=CARTESIAN_POINT('Ctrl Pts',(4.90564478570231,27.1685000069371,-14.6895407912943));
#27821=CARTESIAN_POINT('Ctrl Pts',(6.42157239285118,27.0415000069373,-12.6030454400715));
#27822=CARTESIAN_POINT('Ctrl Pts',(7.93750000000003,26.9145000069372,-10.5165500888487));
#27823=CARTESIAN_POINT('Ctrl Pts',(7.9375000000001,26.7875000069372,-7.93750000000004));
#27824=CARTESIAN_POINT('Ctrl Pts',(7.93750000000009,26.6605000069372,-5.35844991115131));
#27825=CARTESIAN_POINT('Ctrl Pts',(6.42157239285124,26.5335000069372,-3.27195455992846));
#27826=CARTESIAN_POINT('Ctrl Pts',(4.90564478570231,26.4065000069372,-1.18545920870573));
#27827=CARTESIAN_POINT('Ctrl Pts',(2.45282239285122,26.2795000069371,-0.388488901907236));
#27828=CARTESIAN_POINT('Ctrl Pts',(0.,26.1525000069371,0.408481404891264));
#27829=CARTESIAN_POINT('Ctrl Pts',(-2.45282239285116,26.0255000069372,-0.388488901907236));
#27830=CARTESIAN_POINT('Ctrl Pts',(-4.9056447857022,25.8985000069372,-1.18545920870573));
#27831=CARTESIAN_POINT('Ctrl Pts',(-6.42157239285113,25.7715000069371,-3.27195455992846));
#27832=CARTESIAN_POINT('Ctrl Pts',(-7.93750000000003,25.6445000069371,-5.35844991115131));
#27833=CARTESIAN_POINT('Ctrl Pts',(-7.93749999999999,25.5175000069372,-7.93750000000004));
#27834=CARTESIAN_POINT('Ctrl Pts',(-7.93750000000003,25.3905000069371,-10.5165500888487));
#27835=CARTESIAN_POINT('Ctrl Pts',(-6.42157239285113,25.2635000069372,-12.6030454400715));
#27836=CARTESIAN_POINT('Ctrl Pts',(-4.90564478570226,25.1365000069371,-14.6895407912943));
#27837=CARTESIAN_POINT('Ctrl Pts',(-2.45282239285116,25.0095000069373,-15.4865110980927));
#27838=CARTESIAN_POINT('Ctrl Pts',(0.,24.8825000069371,-16.2834814048912));
#27839=CARTESIAN_POINT('Ctrl Pts',(2.45282239285116,24.7555000069373,-15.4865110980927));
#27840=CARTESIAN_POINT('Ctrl Pts',(4.90564478570231,24.6285000069372,-14.6895407912943));
#27841=CARTESIAN_POINT('Ctrl Pts',(6.42157239285124,24.5015000069373,-12.6030454400715));
#27842=CARTESIAN_POINT('Ctrl Pts',(7.93750000000003,24.3745000069371,-10.5165500888487));
#27843=CARTESIAN_POINT('Ctrl Pts',(7.9375000000001,24.2475000069372,-7.93750000000004));
#27844=CARTESIAN_POINT('Ctrl Pts',(7.93749999999997,24.1205000069371,-5.35844991115131));
#27845=CARTESIAN_POINT('Ctrl Pts',(6.42157239285124,23.9935000069372,-3.27195455992846));
#27846=CARTESIAN_POINT('Ctrl Pts',(4.90564478570231,23.8665000069372,-1.18545920870573));
#27847=CARTESIAN_POINT('Ctrl Pts',(2.45282239285111,23.7395000069371,-0.388488901907236));
#27848=CARTESIAN_POINT('Ctrl Pts',(0.,23.612500006937,0.408481404891264));
#27849=CARTESIAN_POINT('Ctrl Pts',(-2.45282239285111,23.4855000069372,-0.388488901907236));
#27850=CARTESIAN_POINT('Ctrl Pts',(-4.90564478570231,23.3585000069372,-1.18545920870573));
#27851=CARTESIAN_POINT('Ctrl Pts',(-6.42157239285113,23.2315000069372,-3.27195455992846));
#27852=CARTESIAN_POINT('Ctrl Pts',(-7.93749999999997,23.1045000069372,-5.35844991115131));
#27853=CARTESIAN_POINT('Ctrl Pts',(-7.93749999999999,22.9775000069372,-7.93750000000004));
#27854=CARTESIAN_POINT('Ctrl Pts',(-7.93749999999991,22.8505000069371,-10.5165500888487));
#27855=CARTESIAN_POINT('Ctrl Pts',(-6.42157239285113,22.7235000069373,-12.6030454400715));
#27856=CARTESIAN_POINT('Ctrl Pts',(-4.9056447857022,22.5965000069371,-14.6895407912943));
#27857=CARTESIAN_POINT('Ctrl Pts',(-2.45282239285116,22.4695000069373,-15.4865110980927));
#27858=CARTESIAN_POINT('Ctrl Pts',(0.,22.3425000069372,-16.2834814048912));
#27859=CARTESIAN_POINT('Ctrl Pts',(2.45282239285116,22.2155000069373,-15.4865110980927));
#27860=CARTESIAN_POINT('Ctrl Pts',(4.90564478570226,22.0885000069371,-14.6895407912943));
#27861=CARTESIAN_POINT('Ctrl Pts',(6.42157239285124,21.9615000069372,-12.6030454400715));
#27862=CARTESIAN_POINT('Ctrl Pts',(7.93750000000003,21.8345000069372,-10.5165500888487));
#27863=CARTESIAN_POINT('Ctrl Pts',(7.93749999999999,21.7075000069372,-7.93750000000004));
#27864=CARTESIAN_POINT('Ctrl Pts',(7.93750000000014,21.5805000069372,-5.35844991115131));
#27865=CARTESIAN_POINT('Ctrl Pts',(6.42157239285124,21.4535000069371,-3.27195455992846));
#27866=CARTESIAN_POINT('Ctrl Pts',(4.9056447857022,21.3265000069371,-1.18545920870573));
#27867=CARTESIAN_POINT('Ctrl Pts',(2.45282239285116,21.1995000069373,-0.388488901907236));
#27868=CARTESIAN_POINT('Ctrl Pts',(0.,21.0725000069371,0.408481404891264));
#27869=CARTESIAN_POINT('Ctrl Pts',(-2.45282239285111,20.9455000069371,-0.388488901907236));
#27870=CARTESIAN_POINT('Ctrl Pts',(-4.90564478570231,20.8185000069372,-1.18545920870573));
#27871=CARTESIAN_POINT('Ctrl Pts',(-6.42157239285113,20.6915000069372,-3.27195455992846));
#27872=CARTESIAN_POINT('Ctrl Pts',(-7.93749999999997,20.5645000069371,-5.35844991115131));
#27873=CARTESIAN_POINT('Ctrl Pts',(-7.93749999999999,20.4375000069372,-7.93750000000004));
#27874=CARTESIAN_POINT('Ctrl Pts',(-7.93750000000003,20.3105000069372,-10.5165500888487));
#27875=CARTESIAN_POINT('Ctrl Pts',(-6.42157239285107,20.1835000069373,-12.6030454400715));
#27876=CARTESIAN_POINT('Ctrl Pts',(-4.90564478570231,20.0565000069372,-14.6895407912943));
#27877=CARTESIAN_POINT('Ctrl Pts',(-2.45282239285116,19.9295000069372,-15.4865110980927));
#27878=CARTESIAN_POINT('Ctrl Pts',(1.1673575708729E-13,19.8025000069371,
-16.2834814048912));
#27879=CARTESIAN_POINT('Ctrl Pts',(2.45282239285122,19.6755000069374,-15.4865110980927));
#27880=CARTESIAN_POINT('Ctrl Pts',(4.90564478570237,19.5485000069371,-14.6895407912943));
#27881=CARTESIAN_POINT('Ctrl Pts',(6.42157239285124,19.4215000069373,-12.6030454400715));
#27882=CARTESIAN_POINT('Ctrl Pts',(7.93749999999991,19.2945000069371,-10.5165500888487));
#27883=CARTESIAN_POINT('Ctrl Pts',(7.93749999999999,19.1675000069371,-7.93750000000004));
#27884=CARTESIAN_POINT('Ctrl Pts',(7.93750000000003,19.0405000069371,-5.35844991115131));
#27885=CARTESIAN_POINT('Ctrl Pts',(6.42157239285124,18.9135000069372,-3.27195455992846));
#27886=CARTESIAN_POINT('Ctrl Pts',(5.62929016097025,18.8471249089612,-2.18147162005691));
#27887=CARTESIAN_POINT('Ctrl Pts',(4.52144069443246,18.7773512949848,-1.41366061688136));
#27888=CARTESIAN_POINT('Ctrl Pts',(-6.56268467750004,74.5712500034686,-7.93749999999999));
#27889=CARTESIAN_POINT('Ctrl Pts',(-6.56268467750003,74.4442500034686,-10.0698455118856));
#27890=CARTESIAN_POINT('Ctrl Pts',(-5.30932343282159,74.3172500034687,-11.7949492688802));
#27891=CARTESIAN_POINT('Ctrl Pts',(-4.05596218814306,74.1902500034686,-13.5200530258749));
#27892=CARTESIAN_POINT('Ctrl Pts',(-2.02798109407148,74.0632500034687,-14.1789840269267));
#27893=CARTESIAN_POINT('Ctrl Pts',(1.1673575708729E-13,73.9362500034685,
-14.8379150279786));
#27894=CARTESIAN_POINT('Ctrl Pts',(2.0279810940716,73.8092500034687,-14.1789840269267));
#27895=CARTESIAN_POINT('Ctrl Pts',(4.05596218814324,73.6822500034687,-13.5200530258749));
#27896=CARTESIAN_POINT('Ctrl Pts',(5.30932343282159,73.5552500034686,-11.7949492688802));
#27897=CARTESIAN_POINT('Ctrl Pts',(6.56268467750003,73.4282500034686,-10.0698455118856));
#27898=CARTESIAN_POINT('Ctrl Pts',(6.5626846775001,73.3012500034686,-7.93749999999999));
#27899=CARTESIAN_POINT('Ctrl Pts',(6.56268467750003,73.1742500034686,-5.80515448811441));
#27900=CARTESIAN_POINT('Ctrl Pts',(5.30932343282164,73.0472500034686,-4.08005073111967));
#27901=CARTESIAN_POINT('Ctrl Pts',(4.05596218814318,72.9202500034686,-2.35494697412514));
#27902=CARTESIAN_POINT('Ctrl Pts',(2.02798109407154,72.7932500034686,-1.69601597307328));
#27903=CARTESIAN_POINT('Ctrl Pts',(1.1673575708729E-13,72.6662500034686,
-1.0370849720215));
#27904=CARTESIAN_POINT('Ctrl Pts',(-2.02798109407165,72.5392500034687,-1.69601597307328));
#27905=CARTESIAN_POINT('Ctrl Pts',(-4.05596218814312,72.4122500034686,-2.35494697412514));
#27906=CARTESIAN_POINT('Ctrl Pts',(-5.30932343282153,72.2852500034685,-4.08005073111967));
#27907=CARTESIAN_POINT('Ctrl Pts',(-6.56268467750008,72.1582500034687,-5.80515448811441));
#27908=CARTESIAN_POINT('Ctrl Pts',(-6.56268467750004,72.0312500034686,-7.93749999999999));
#27909=CARTESIAN_POINT('Ctrl Pts',(-6.56268467750003,71.9042500034686,-10.0698455118856));
#27910=CARTESIAN_POINT('Ctrl Pts',(-5.30932343282159,71.7772500034686,-11.7949492688802));
#27911=CARTESIAN_POINT('Ctrl Pts',(-4.05596218814318,71.6502500034686,-13.5200530258749));
#27912=CARTESIAN_POINT('Ctrl Pts',(-2.0279810940716,71.5232500034686,-14.1789840269267));
#27913=CARTESIAN_POINT('Ctrl Pts',(0.,71.3962500034686,-14.8379150279786));
#27914=CARTESIAN_POINT('Ctrl Pts',(2.02798109407165,71.2692500034687,-14.1789840269267));
#27915=CARTESIAN_POINT('Ctrl Pts',(4.05596218814312,71.1422500034685,-13.5200530258749));
#27916=CARTESIAN_POINT('Ctrl Pts',(5.30932343282159,71.0152500034686,-11.7949492688802));
#27917=CARTESIAN_POINT('Ctrl Pts',(6.56268467750003,70.8882500034686,-10.0698455118856));
#27918=CARTESIAN_POINT('Ctrl Pts',(6.56268467749999,70.7612500034687,-7.93749999999999));
#27919=CARTESIAN_POINT('Ctrl Pts',(6.56268467750003,70.6342500034686,-5.80515448811441));
#27920=CARTESIAN_POINT('Ctrl Pts',(5.30932343282164,70.5072500034686,-4.08005073111967));
#27921=CARTESIAN_POINT('Ctrl Pts',(4.05596218814324,70.3802500034686,-2.35494697412514));
#27922=CARTESIAN_POINT('Ctrl Pts',(2.0279810940716,70.2532500034686,-1.69601597307328));
#27923=CARTESIAN_POINT('Ctrl Pts',(0.,70.1262500034686,-1.0370849720215));
#27924=CARTESIAN_POINT('Ctrl Pts',(-2.0279810940716,69.9992500034686,-1.69601597307328));
#27925=CARTESIAN_POINT('Ctrl Pts',(-4.05596218814312,69.8722500034686,-2.35494697412514));
#27926=CARTESIAN_POINT('Ctrl Pts',(-5.30932343282159,69.7452500034687,-4.08005073111967));
#27927=CARTESIAN_POINT('Ctrl Pts',(-6.56268467749997,69.6182500034686,-5.80515448811441));
#27928=CARTESIAN_POINT('Ctrl Pts',(-6.56268467749999,69.4912500034686,-7.93749999999999));
#27929=CARTESIAN_POINT('Ctrl Pts',(-6.56268467749997,69.3642500034686,-10.0698455118856));
#27930=CARTESIAN_POINT('Ctrl Pts',(-5.30932343282153,69.2372500034686,-11.7949492688802));
#27931=CARTESIAN_POINT('Ctrl Pts',(-4.05596218814312,69.1102500034686,-13.5200530258749));
#27932=CARTESIAN_POINT('Ctrl Pts',(-2.02798109407154,68.9832500034687,-14.1789840269267));
#27933=CARTESIAN_POINT('Ctrl Pts',(0.,68.8562500034686,-14.8379150279786));
#27934=CARTESIAN_POINT('Ctrl Pts',(2.02798109407165,68.7292500034686,-14.1789840269267));
#27935=CARTESIAN_POINT('Ctrl Pts',(4.05596218814312,68.6022500034686,-13.5200530258749));
#27936=CARTESIAN_POINT('Ctrl Pts',(5.30932343282164,68.4752500034687,-11.7949492688802));
#27937=CARTESIAN_POINT('Ctrl Pts',(6.56268467749997,68.3482500034685,-10.0698455118856));
#27938=CARTESIAN_POINT('Ctrl Pts',(6.56268467749999,68.2212500034686,-7.93749999999999));
#27939=CARTESIAN_POINT('Ctrl Pts',(6.56268467750003,68.0942500034685,-5.80515448811441));
#27940=CARTESIAN_POINT('Ctrl Pts',(5.3093234328217,67.9672500034686,-4.08005073111967));
#27941=CARTESIAN_POINT('Ctrl Pts',(4.05596218814312,67.8402500034685,-2.35494697412514));
#27942=CARTESIAN_POINT('Ctrl Pts',(2.0279810940716,67.7132500034686,-1.69601597307328));
#27943=CARTESIAN_POINT('Ctrl Pts',(1.1673575708729E-13,67.5862500034684,
-1.0370849720215));
#27944=CARTESIAN_POINT('Ctrl Pts',(-2.0279810940716,67.4592500034686,-1.69601597307328));
#27945=CARTESIAN_POINT('Ctrl Pts',(-4.05596218814312,67.3322500034685,-2.35494697412514));
#27946=CARTESIAN_POINT('Ctrl Pts',(-5.30932343282153,67.2052500034686,-4.08005073111967));
#27947=CARTESIAN_POINT('Ctrl Pts',(-6.56268467750003,67.0782500034685,-5.80515448811441));
#27948=CARTESIAN_POINT('Ctrl Pts',(-6.56268467749999,66.9512500034686,-7.93749999999999));
#27949=CARTESIAN_POINT('Ctrl Pts',(-6.56268467749997,66.8242500034685,-10.0698455118856));
#27950=CARTESIAN_POINT('Ctrl Pts',(-5.30932343282153,66.6972500034686,-11.7949492688802));
#27951=CARTESIAN_POINT('Ctrl Pts',(-4.05596218814312,66.5702500034686,-13.5200530258749));
#27952=CARTESIAN_POINT('Ctrl Pts',(-2.02798109407165,66.4432500034688,-14.1789840269267));
#27953=CARTESIAN_POINT('Ctrl Pts',(0.,66.3162500034685,-14.8379150279786));
#27954=CARTESIAN_POINT('Ctrl Pts',(2.02798109407154,66.1892500034688,-14.1789840269267));
#27955=CARTESIAN_POINT('Ctrl Pts',(4.05596218814312,66.0622500034686,-13.5200530258749));
#27956=CARTESIAN_POINT('Ctrl Pts',(5.30932343282164,65.9352500034686,-11.7949492688802));
#27957=CARTESIAN_POINT('Ctrl Pts',(6.56268467750008,65.8082500034686,-10.0698455118856));
#27958=CARTESIAN_POINT('Ctrl Pts',(6.56268467749999,65.6812500034686,-7.93749999999999));
#27959=CARTESIAN_POINT('Ctrl Pts',(6.56268467749991,65.5542500034687,-5.80515448811441));
#27960=CARTESIAN_POINT('Ctrl Pts',(5.3093234328217,65.4272500034686,-4.08005073111967));
#27961=CARTESIAN_POINT('Ctrl Pts',(4.05596218814324,65.3002500034687,-2.35494697412514));
#27962=CARTESIAN_POINT('Ctrl Pts',(2.0279810940716,65.1732500034686,-1.69601597307328));
#27963=CARTESIAN_POINT('Ctrl Pts',(0.,65.0462500034686,-1.0370849720215));
#27964=CARTESIAN_POINT('Ctrl Pts',(-2.0279810940716,64.9192500034686,-1.69601597307328));
#27965=CARTESIAN_POINT('Ctrl Pts',(-4.05596218814312,64.7922500034686,-2.35494697412514));
#27966=CARTESIAN_POINT('Ctrl Pts',(-5.30932343282153,64.6652500034686,-4.08005073111967));
#27967=CARTESIAN_POINT('Ctrl Pts',(-6.56268467750003,64.5382500034686,-5.80515448811441));
#27968=CARTESIAN_POINT('Ctrl Pts',(-6.56268467749999,64.4112500034687,-7.93749999999999));
#27969=CARTESIAN_POINT('Ctrl Pts',(-6.56268467749997,64.2842500034685,-10.0698455118856));
#27970=CARTESIAN_POINT('Ctrl Pts',(-5.30932343282148,64.1572500034686,-11.7949492688802));
#27971=CARTESIAN_POINT('Ctrl Pts',(-4.05596218814312,64.0302500034686,-13.5200530258749));
#27972=CARTESIAN_POINT('Ctrl Pts',(-2.02798109407165,63.9032500034688,-14.1789840269267));
#27973=CARTESIAN_POINT('Ctrl Pts',(0.,63.7762500034686,-14.8379150279786));
#27974=CARTESIAN_POINT('Ctrl Pts',(2.0279810940716,63.6492500034688,-14.1789840269267));
#27975=CARTESIAN_POINT('Ctrl Pts',(4.05596218814312,63.5222500034685,-13.5200530258749));
#27976=CARTESIAN_POINT('Ctrl Pts',(5.3093234328217,63.3952500034686,-11.7949492688802));
#27977=CARTESIAN_POINT('Ctrl Pts',(6.56268467749997,63.2682500034685,-10.0698455118856));
#27978=CARTESIAN_POINT('Ctrl Pts',(6.56268467750004,63.1412500034686,-7.93749999999999));
#27979=CARTESIAN_POINT('Ctrl Pts',(6.56268467750003,63.0142500034686,-5.80515448811441));
#27980=CARTESIAN_POINT('Ctrl Pts',(5.30932343282164,62.8872500034686,-4.08005073111967));
#27981=CARTESIAN_POINT('Ctrl Pts',(4.05596218814312,62.7602500034686,-2.35494697412514));
#27982=CARTESIAN_POINT('Ctrl Pts',(2.02798109407165,62.6332500034686,-1.69601597307328));
#27983=CARTESIAN_POINT('Ctrl Pts',(0.,62.5062500034686,-1.0370849720215));
#27984=CARTESIAN_POINT('Ctrl Pts',(-2.02798109407154,62.3792500034686,-1.69601597307328));
#27985=CARTESIAN_POINT('Ctrl Pts',(-4.05596218814324,62.2522500034685,-2.35494697412514));
#27986=CARTESIAN_POINT('Ctrl Pts',(-5.30932343282148,62.1252500034686,-4.08005073111967));
#27987=CARTESIAN_POINT('Ctrl Pts',(-6.56268467750003,61.9982500034685,-5.80515448811441));
#27988=CARTESIAN_POINT('Ctrl Pts',(-6.5626846775001,61.8712500034687,-7.93749999999999));
#27989=CARTESIAN_POINT('Ctrl Pts',(-6.56268467750008,61.7442500034686,-10.0698455118856));
#27990=CARTESIAN_POINT('Ctrl Pts',(-5.30932343282148,61.6172500034687,-11.7949492688802));
#27991=CARTESIAN_POINT('Ctrl Pts',(-4.05596218814312,61.4902500034686,-13.5200530258749));
#27992=CARTESIAN_POINT('Ctrl Pts',(-2.0279810940716,61.3632500034687,-14.1789840269267));
#27993=CARTESIAN_POINT('Ctrl Pts',(0.,61.2362500034686,-14.8379150279786));
#27994=CARTESIAN_POINT('Ctrl Pts',(2.0279810940716,61.1092500034687,-14.1789840269267));
#27995=CARTESIAN_POINT('Ctrl Pts',(4.05596218814318,60.9822500034686,-13.5200530258749));
#27996=CARTESIAN_POINT('Ctrl Pts',(5.3093234328217,60.8552500034686,-11.7949492688802));
#27997=CARTESIAN_POINT('Ctrl Pts',(6.56268467750003,60.7282500034687,-10.0698455118856));
#27998=CARTESIAN_POINT('Ctrl Pts',(6.5626846775001,60.6012500034686,-7.93749999999999));
#27999=CARTESIAN_POINT('Ctrl Pts',(6.56268467750008,60.4742500034686,-5.80515448811441));
#28000=CARTESIAN_POINT('Ctrl Pts',(5.30932343282159,60.3472500034687,-4.08005073111967));
#28001=CARTESIAN_POINT('Ctrl Pts',(4.05596218814312,60.2202500034686,-2.35494697412514));
#28002=CARTESIAN_POINT('Ctrl Pts',(2.02798109407165,60.0932500034686,-1.69601597307328));
#28003=CARTESIAN_POINT('Ctrl Pts',(0.,59.9662500034686,-1.0370849720215));
#28004=CARTESIAN_POINT('Ctrl Pts',(-2.02798109407165,59.8392500034686,-1.69601597307317));
#28005=CARTESIAN_POINT('Ctrl Pts',(-4.05596218814306,59.7122500034685,-2.35494697412514));
#28006=CARTESIAN_POINT('Ctrl Pts',(-5.30932343282148,59.5852500034686,-4.08005073111967));
#28007=CARTESIAN_POINT('Ctrl Pts',(-6.56268467750003,59.4582500034686,-5.80515448811441));
#28008=CARTESIAN_POINT('Ctrl Pts',(-6.56268467750004,59.3312500034686,-7.93749999999999));
#28009=CARTESIAN_POINT('Ctrl Pts',(-6.56268467749991,59.2042500034686,-10.0698455118856));
#28010=CARTESIAN_POINT('Ctrl Pts',(-5.30932343282148,59.0772500034686,-11.7949492688802));
#28011=CARTESIAN_POINT('Ctrl Pts',(-4.05596218814312,58.9502500034686,-13.5200530258749));
#28012=CARTESIAN_POINT('Ctrl Pts',(-2.0279810940716,58.8232500034687,-14.1789840269267));
#28013=CARTESIAN_POINT('Ctrl Pts',(0.,58.6962500034686,-14.8379150279786));
#28014=CARTESIAN_POINT('Ctrl Pts',(2.0279810940716,58.5692500034687,-14.1789840269267));
#28015=CARTESIAN_POINT('Ctrl Pts',(4.05596218814318,58.4422500034685,-13.5200530258749));
#28016=CARTESIAN_POINT('Ctrl Pts',(5.30932343282159,58.3152500034686,-11.7949492688802));
#28017=CARTESIAN_POINT('Ctrl Pts',(6.56268467750003,58.1882500034686,-10.0698455118856));
#28018=CARTESIAN_POINT('Ctrl Pts',(6.5626846775001,58.0612500034686,-7.93749999999999));
#28019=CARTESIAN_POINT('Ctrl Pts',(6.56268467749997,57.9342500034686,-5.80515448811441));
#28020=CARTESIAN_POINT('Ctrl Pts',(5.30932343282164,57.8072500034686,-4.08005073111967));
#28021=CARTESIAN_POINT('Ctrl Pts',(4.05596218814318,57.6802500034686,-2.35494697412514));
#28022=CARTESIAN_POINT('Ctrl Pts',(2.02798109407154,57.5532500034686,-1.69601597307317));
#28023=CARTESIAN_POINT('Ctrl Pts',(0.,57.4262500034686,-1.0370849720215));
#28024=CARTESIAN_POINT('Ctrl Pts',(-2.0279810940716,57.2992500034686,-1.69601597307317));
#28025=CARTESIAN_POINT('Ctrl Pts',(-4.05596218814318,57.1722500034686,-2.35494697412514));
#28026=CARTESIAN_POINT('Ctrl Pts',(-5.30932343282148,57.0452500034685,-4.08005073111967));
#28027=CARTESIAN_POINT('Ctrl Pts',(-6.56268467749997,56.9182500034686,-5.80515448811441));
#28028=CARTESIAN_POINT('Ctrl Pts',(-6.56268467750004,56.7912500034686,-7.93749999999999));
#28029=CARTESIAN_POINT('Ctrl Pts',(-6.56268467750003,56.6642500034685,-10.0698455118856));
#28030=CARTESIAN_POINT('Ctrl Pts',(-5.30932343282159,56.5372500034686,-11.7949492688802));
#28031=CARTESIAN_POINT('Ctrl Pts',(-4.05596218814312,56.4102500034685,-13.5200530258749));
#28032=CARTESIAN_POINT('Ctrl Pts',(-2.0279810940716,56.2832500034686,-14.1789840269267));
#28033=CARTESIAN_POINT('Ctrl Pts',(0.,56.1562500034686,-14.8379150279786));
#28034=CARTESIAN_POINT('Ctrl Pts',(2.02798109407165,56.0292500034687,-14.1789840269267));
#28035=CARTESIAN_POINT('Ctrl Pts',(4.05596218814318,55.9022500034686,-13.5200530258749));
#28036=CARTESIAN_POINT('Ctrl Pts',(5.30932343282148,55.7752500034686,-11.7949492688802));
#28037=CARTESIAN_POINT('Ctrl Pts',(6.56268467750003,55.6482500034686,-10.0698455118856));
#28038=CARTESIAN_POINT('Ctrl Pts',(6.5626846775001,55.5212500034686,-7.93749999999999));
#28039=CARTESIAN_POINT('Ctrl Pts',(6.56268467750008,55.3942500034686,-5.80515448811441));
#28040=CARTESIAN_POINT('Ctrl Pts',(5.30932343282153,55.2672500034686,-4.08005073111967));
#28041=CARTESIAN_POINT('Ctrl Pts',(4.05596218814318,55.1402500034686,-2.35494697412514));
#28042=CARTESIAN_POINT('Ctrl Pts',(2.0279810940716,55.0132500034686,-1.69601597307317));
#28043=CARTESIAN_POINT('Ctrl Pts',(-5.83678785436452E-14,54.8862500034686,
-1.0370849720215));
#28044=CARTESIAN_POINT('Ctrl Pts',(-2.0279810940716,54.7592500034686,-1.69601597307323));
#28045=CARTESIAN_POINT('Ctrl Pts',(-4.05596218814318,54.6322500034686,-2.35494697412514));
#28046=CARTESIAN_POINT('Ctrl Pts',(-5.30932343282159,54.5052500034687,-4.08005073111972));
#28047=CARTESIAN_POINT('Ctrl Pts',(-6.56268467749997,54.3782500034686,-5.80515448811441));
#28048=CARTESIAN_POINT('Ctrl Pts',(-6.56268467749999,54.2512500034685,-7.93750000000004));
#28049=CARTESIAN_POINT('Ctrl Pts',(-6.56268467750003,54.1242500034686,-10.0698455118856));
#28050=CARTESIAN_POINT('Ctrl Pts',(-5.30932343282153,53.9972500034686,-11.7949492688803));
#28051=CARTESIAN_POINT('Ctrl Pts',(-4.05596218814318,53.8702500034686,-13.5200530258749));
#28052=CARTESIAN_POINT('Ctrl Pts',(-2.02798109407154,53.7432500034686,-14.1789840269267));
#28053=CARTESIAN_POINT('Ctrl Pts',(0.,53.6162500034685,-14.8379150279786));
#28054=CARTESIAN_POINT('Ctrl Pts',(2.02798109407165,53.4892500034686,-14.1789840269267));
#28055=CARTESIAN_POINT('Ctrl Pts',(4.05596218814312,53.3622500034686,-13.5200530258749));
#28056=CARTESIAN_POINT('Ctrl Pts',(5.30932343282153,53.2352500034686,-11.7949492688803));
#28057=CARTESIAN_POINT('Ctrl Pts',(6.56268467750003,53.1082500034686,-10.0698455118856));
#28058=CARTESIAN_POINT('Ctrl Pts',(6.56268467749999,52.9812500034686,-7.93750000000004));
#28059=CARTESIAN_POINT('Ctrl Pts',(6.56268467749997,52.8542500034685,-5.80515448811441));
#28060=CARTESIAN_POINT('Ctrl Pts',(5.30932343282159,52.7272500034686,-4.08005073111972));
#28061=CARTESIAN_POINT('Ctrl Pts',(4.05596218814318,52.6002500034685,-2.35494697412514));
#28062=CARTESIAN_POINT('Ctrl Pts',(2.0279810940716,52.4732500034685,-1.69601597307323));
#28063=CARTESIAN_POINT('Ctrl Pts',(0.,52.3462500034685,-1.0370849720215));
#28064=CARTESIAN_POINT('Ctrl Pts',(-2.0279810940716,52.2192500034686,-1.69601597307323));
#28065=CARTESIAN_POINT('Ctrl Pts',(-4.05596218814318,52.0922500034686,-2.35494697412514));
#28066=CARTESIAN_POINT('Ctrl Pts',(-5.30932343282153,51.9652500034687,-4.08005073111972));
#28067=CARTESIAN_POINT('Ctrl Pts',(-6.56268467749997,51.8382500034685,-5.80515448811441));
#28068=CARTESIAN_POINT('Ctrl Pts',(-6.56268467749999,51.7112500034686,-7.93750000000004));
#28069=CARTESIAN_POINT('Ctrl Pts',(-6.56268467750003,51.5842500034685,-10.0698455118856));
#28070=CARTESIAN_POINT('Ctrl Pts',(-5.30932343282153,51.4572500034685,-11.7949492688803));
#28071=CARTESIAN_POINT('Ctrl Pts',(-4.05596218814306,51.3302500034686,-13.5200530258749));
#28072=CARTESIAN_POINT('Ctrl Pts',(-2.02798109407154,51.2032500034688,-14.1789840269267));
#28073=CARTESIAN_POINT('Ctrl Pts',(1.1673575708729E-13,51.0762500034686,
-14.8379150279786));
#28074=CARTESIAN_POINT('Ctrl Pts',(2.02798109407154,50.9492500034687,-14.1789840269267));
#28075=CARTESIAN_POINT('Ctrl Pts',(4.05596218814324,50.8222500034686,-13.5200530258749));
#28076=CARTESIAN_POINT('Ctrl Pts',(5.30932343282153,50.6952500034686,-11.7949492688803));
#28077=CARTESIAN_POINT('Ctrl Pts',(6.56268467750003,50.5682500034685,-10.0698455118856));
#28078=CARTESIAN_POINT('Ctrl Pts',(6.56268467749999,50.4412500034686,-7.93750000000004));
#28079=CARTESIAN_POINT('Ctrl Pts',(6.56268467750003,50.3142500034686,-5.80515448811441));
#28080=CARTESIAN_POINT('Ctrl Pts',(5.30932343282159,50.1872500034685,-4.08005073111972));
#28081=CARTESIAN_POINT('Ctrl Pts',(4.05596218814318,50.0602500034686,-2.35494697412514));
#28082=CARTESIAN_POINT('Ctrl Pts',(2.0279810940716,49.9332500034686,-1.69601597307323));
#28083=CARTESIAN_POINT('Ctrl Pts',(1.1673575708729E-13,49.8062500034686,
-1.0370849720215));
#28084=CARTESIAN_POINT('Ctrl Pts',(-2.0279810940716,49.6792500034686,-1.69601597307323));
#28085=CARTESIAN_POINT('Ctrl Pts',(-4.05596218814312,49.5522500034686,-2.35494697412514));
#28086=CARTESIAN_POINT('Ctrl Pts',(-5.30932343282153,49.4252500034686,-4.08005073111972));
#28087=CARTESIAN_POINT('Ctrl Pts',(-6.56268467750008,49.2982500034686,-5.80515448811441));
#28088=CARTESIAN_POINT('Ctrl Pts',(-6.56268467749999,49.1712500034686,-7.93750000000004));
#28089=CARTESIAN_POINT('Ctrl Pts',(-6.56268467750003,49.0442500034686,-10.0698455118856));
#28090=CARTESIAN_POINT('Ctrl Pts',(-5.30932343282148,48.9172500034685,-11.7949492688803));
#28091=CARTESIAN_POINT('Ctrl Pts',(-4.05596218814318,48.7902500034686,-13.5200530258749));
#28092=CARTESIAN_POINT('Ctrl Pts',(-2.02798109407165,48.6632500034687,-14.1789840269267));
#28093=CARTESIAN_POINT('Ctrl Pts',(0.,48.5362500034685,-14.8379150279786));
#28094=CARTESIAN_POINT('Ctrl Pts',(2.0279810940716,48.4092500034688,-14.1789840269267));
#28095=CARTESIAN_POINT('Ctrl Pts',(4.05596218814312,48.2822500034686,-13.5200530258749));
#28096=CARTESIAN_POINT('Ctrl Pts',(5.30932343282159,48.1552500034686,-11.7949492688803));
#28097=CARTESIAN_POINT('Ctrl Pts',(6.56268467750008,48.0282500034685,-10.0698455118856));
#28098=CARTESIAN_POINT('Ctrl Pts',(6.56268467750004,47.9012500034686,-7.93750000000004));
#28099=CARTESIAN_POINT('Ctrl Pts',(6.56268467750003,47.7742500034685,-5.80515448811441));
#28100=CARTESIAN_POINT('Ctrl Pts',(5.30932343282159,47.6472500034686,-4.08005073111972));
#28101=CARTESIAN_POINT('Ctrl Pts',(4.05596218814324,47.5202500034686,-2.35494697412514));
#28102=CARTESIAN_POINT('Ctrl Pts',(2.02798109407165,47.3932500034687,-1.69601597307323));
#28103=CARTESIAN_POINT('Ctrl Pts',(0.,47.2662500034685,-1.0370849720215));
#28104=CARTESIAN_POINT('Ctrl Pts',(-2.02798109407154,47.1392500034686,-1.69601597307323));
#28105=CARTESIAN_POINT('Ctrl Pts',(-4.05596218814312,47.0122500034686,-2.35494697412514));
#28106=CARTESIAN_POINT('Ctrl Pts',(-5.30932343282148,46.8852500034686,-4.08005073111972));
#28107=CARTESIAN_POINT('Ctrl Pts',(-6.56268467749991,46.7582500034686,-5.80515448811441));
#28108=CARTESIAN_POINT('Ctrl Pts',(-6.56268467749999,46.6312500034686,-7.93750000000004));
#28109=CARTESIAN_POINT('Ctrl Pts',(-6.56268467749997,46.5042500034685,-10.0698455118856));
#28110=CARTESIAN_POINT('Ctrl Pts',(-5.30932343282148,46.3772500034686,-11.7949492688803));
#28111=CARTESIAN_POINT('Ctrl Pts',(-4.05596218814312,46.2502500034686,-13.5200530258749));
#28112=CARTESIAN_POINT('Ctrl Pts',(-2.0279810940716,46.1232500034687,-14.1789840269267));
#28113=CARTESIAN_POINT('Ctrl Pts',(0.,45.9962500034685,-14.8379150279786));
#28114=CARTESIAN_POINT('Ctrl Pts',(2.0279810940716,45.8692500034687,-14.1789840269267));
#28115=CARTESIAN_POINT('Ctrl Pts',(4.05596218814312,45.7422500034686,-13.5200530258749));
#28116=CARTESIAN_POINT('Ctrl Pts',(5.30932343282159,45.6152500034686,-11.7949492688803));
#28117=CARTESIAN_POINT('Ctrl Pts',(6.56268467749997,45.4882500034686,-10.0698455118856));
#28118=CARTESIAN_POINT('Ctrl Pts',(6.5626846775001,45.3612500034686,-7.93750000000004));
#28119=CARTESIAN_POINT('Ctrl Pts',(6.56268467750003,45.2342500034686,-5.80515448811441));
#28120=CARTESIAN_POINT('Ctrl Pts',(5.30932343282153,45.1072500034687,-4.08005073111972));
#28121=CARTESIAN_POINT('Ctrl Pts',(4.05596218814312,44.9802500034686,-2.35494697412514));
#28122=CARTESIAN_POINT('Ctrl Pts',(2.02798109407165,44.8532500034686,-1.69601597307323));
#28123=CARTESIAN_POINT('Ctrl Pts',(0.,44.7262500034686,-1.0370849720215));
#28124=CARTESIAN_POINT('Ctrl Pts',(-2.02798109407154,44.5992500034686,-1.69601597307323));
#28125=CARTESIAN_POINT('Ctrl Pts',(-4.05596218814312,44.4722500034685,-2.35494697412514));
#28126=CARTESIAN_POINT('Ctrl Pts',(-5.30932343282148,44.3452500034686,-4.08005073111972));
#28127=CARTESIAN_POINT('Ctrl Pts',(-6.56268467750003,44.2182500034685,-5.80515448811441));
#28128=CARTESIAN_POINT('Ctrl Pts',(-6.56268467750004,44.0912500034686,-7.93750000000004));
#28129=CARTESIAN_POINT('Ctrl Pts',(-6.56268467749997,43.9642500034686,-10.0698455118856));
#28130=CARTESIAN_POINT('Ctrl Pts',(-5.30932343282148,43.8372500034686,-11.7949492688803));
#28131=CARTESIAN_POINT('Ctrl Pts',(-4.05596218814312,43.7102500034686,-13.5200530258749));
#28132=CARTESIAN_POINT('Ctrl Pts',(-2.0279810940716,43.5832500034687,-14.1789840269267));
#28133=CARTESIAN_POINT('Ctrl Pts',(0.,43.4562500034686,-14.8379150279786));
#28134=CARTESIAN_POINT('Ctrl Pts',(2.0279810940716,43.3292500034687,-14.1789840269267));
#28135=CARTESIAN_POINT('Ctrl Pts',(4.05596218814312,43.2022500034685,-13.5200530258749));
#28136=CARTESIAN_POINT('Ctrl Pts',(5.30932343282159,43.0752500034686,-11.7949492688803));
#28137=CARTESIAN_POINT('Ctrl Pts',(6.56268467750008,42.9482500034686,-10.0698455118856));
#28138=CARTESIAN_POINT('Ctrl Pts',(6.5626846775001,42.8212500034686,-7.93750000000004));
#28139=CARTESIAN_POINT('Ctrl Pts',(6.56268467750003,42.6942500034686,-5.80515448811441));
#28140=CARTESIAN_POINT('Ctrl Pts',(5.30932343282153,42.5672500034686,-4.08005073111972));
#28141=CARTESIAN_POINT('Ctrl Pts',(4.05596218814324,42.4402500034686,-2.35494697412514));
#28142=CARTESIAN_POINT('Ctrl Pts',(2.02798109407165,42.3132500034686,-1.69601597307323));
#28143=CARTESIAN_POINT('Ctrl Pts',(0.,42.1862500034686,-1.0370849720215));
#28144=CARTESIAN_POINT('Ctrl Pts',(-2.0279810940716,42.0592500034685,-1.69601597307323));
#28145=CARTESIAN_POINT('Ctrl Pts',(-4.05596218814312,41.9322500034686,-2.35494697412514));
#28146=CARTESIAN_POINT('Ctrl Pts',(-5.30932343282148,41.8052500034685,-4.08005073111972));
#28147=CARTESIAN_POINT('Ctrl Pts',(-6.56268467750003,41.6782500034686,-5.80515448811441));
#28148=CARTESIAN_POINT('Ctrl Pts',(-6.56268467750004,41.5512500034686,-7.93750000000004));
#28149=CARTESIAN_POINT('Ctrl Pts',(-6.56268467749997,41.4242500034686,-10.0698455118856));
#28150=CARTESIAN_POINT('Ctrl Pts',(-5.30932343282153,41.2972500034686,-11.7949492688803));
#28151=CARTESIAN_POINT('Ctrl Pts',(-4.05596218814312,41.1702500034685,-13.5200530258749));
#28152=CARTESIAN_POINT('Ctrl Pts',(-2.0279810940716,41.0432500034686,-14.1789840269267));
#28153=CARTESIAN_POINT('Ctrl Pts',(0.,40.9162500034686,-14.8379150279786));
#28154=CARTESIAN_POINT('Ctrl Pts',(2.02798109407165,40.7892500034687,-14.1789840269267));
#28155=CARTESIAN_POINT('Ctrl Pts',(4.05596218814312,40.6622500034685,-13.5200530258749));
#28156=CARTESIAN_POINT('Ctrl Pts',(5.30932343282153,40.5352500034686,-11.7949492688803));
#28157=CARTESIAN_POINT('Ctrl Pts',(6.56268467749997,40.4082500034686,-10.0698455118856));
#28158=CARTESIAN_POINT('Ctrl Pts',(6.5626846775001,40.2812500034686,-7.93750000000004));
#28159=CARTESIAN_POINT('Ctrl Pts',(6.56268467750008,40.1542500034685,-5.80515448811441));
#28160=CARTESIAN_POINT('Ctrl Pts',(5.30932343282153,40.0272500034686,-4.08005073111972));
#28161=CARTESIAN_POINT('Ctrl Pts',(4.05596218814312,39.9002500034686,-2.35494697412514));
#28162=CARTESIAN_POINT('Ctrl Pts',(2.0279810940716,39.7732500034685,-1.69601597307323));
#28163=CARTESIAN_POINT('Ctrl Pts',(0.,39.6462500034686,-1.0370849720215));
#28164=CARTESIAN_POINT('Ctrl Pts',(-2.0279810940716,39.5192500034686,-1.69601597307323));
#28165=CARTESIAN_POINT('Ctrl Pts',(-4.05596218814324,39.3922500034686,-2.35494697412514));
#28166=CARTESIAN_POINT('Ctrl Pts',(-5.30932343282148,39.2652500034686,-4.08005073111972));
#28167=CARTESIAN_POINT('Ctrl Pts',(-6.56268467749991,39.1382500034686,-5.80515448811441));
#28168=CARTESIAN_POINT('Ctrl Pts',(-6.56268467749999,39.0112500034685,-7.93750000000004));
#28169=CARTESIAN_POINT('Ctrl Pts',(-6.56268467750008,38.8842500034686,-10.0698455118856));
#28170=CARTESIAN_POINT('Ctrl Pts',(-5.30932343282153,38.7572500034686,-11.7949492688803));
#28171=CARTESIAN_POINT('Ctrl Pts',(-4.05596218814312,38.6302500034686,-13.5200530258749));
#28172=CARTESIAN_POINT('Ctrl Pts',(-2.02798109407154,38.5032500034686,-14.1789840269267));
#28173=CARTESIAN_POINT('Ctrl Pts',(0.,38.3762500034685,-14.8379150279786));
#28174=CARTESIAN_POINT('Ctrl Pts',(2.02798109407165,38.2492500034686,-14.1789840269267));
#28175=CARTESIAN_POINT('Ctrl Pts',(4.05596218814318,38.1222500034686,-13.5200530258749));
#28176=CARTESIAN_POINT('Ctrl Pts',(5.30932343282153,37.9952500034686,-11.7949492688803));
#28177=CARTESIAN_POINT('Ctrl Pts',(6.56268467750003,37.8682500034686,-10.0698455118856));
#28178=CARTESIAN_POINT('Ctrl Pts',(6.56268467749999,37.7412500034686,-7.93750000000004));
#28179=CARTESIAN_POINT('Ctrl Pts',(6.56268467750008,37.6142500034686,-5.80515448811441));
#28180=CARTESIAN_POINT('Ctrl Pts',(5.30932343282159,37.4872500034686,-4.08005073111972));
#28181=CARTESIAN_POINT('Ctrl Pts',(4.05596218814312,37.3602500034685,-2.35494697412514));
#28182=CARTESIAN_POINT('Ctrl Pts',(2.0279810940716,37.2332500034685,-1.69601597307323));
#28183=CARTESIAN_POINT('Ctrl Pts',(-1.1673575708729E-13,37.1062500034685,
-1.0370849720215));
#28184=CARTESIAN_POINT('Ctrl Pts',(-2.0279810940716,36.9792500034686,-1.69601597307323));
#28185=CARTESIAN_POINT('Ctrl Pts',(-4.05596218814306,36.8522500034687,-2.35494697412514));
#28186=CARTESIAN_POINT('Ctrl Pts',(-5.30932343282153,36.7252500034687,-4.08005073111972));
#28187=CARTESIAN_POINT('Ctrl Pts',(-6.56268467750003,36.5982500034685,-5.80515448811441));
#28188=CARTESIAN_POINT('Ctrl Pts',(-6.56268467749999,36.4712500034686,-7.93750000000004));
#28189=CARTESIAN_POINT('Ctrl Pts',(-6.56268467749991,36.3442500034685,-10.0698455118856));
#28190=CARTESIAN_POINT('Ctrl Pts',(-5.30932343282153,36.2172500034686,-11.7949492688803));
#28191=CARTESIAN_POINT('Ctrl Pts',(-4.05596218814312,36.0902500034685,-13.5200530258749));
#28192=CARTESIAN_POINT('Ctrl Pts',(-2.02798109407154,35.9632500034688,-14.1789840269267));
#28193=CARTESIAN_POINT('Ctrl Pts',(0.,35.8362500034686,-14.8379150279786));
#28194=CARTESIAN_POINT('Ctrl Pts',(2.02798109407165,35.7092500034686,-14.1789840269267));
#28195=CARTESIAN_POINT('Ctrl Pts',(4.05596218814318,35.5822500034686,-13.5200530258749));
#28196=CARTESIAN_POINT('Ctrl Pts',(5.30932343282153,35.4552500034687,-11.7949492688803));
#28197=CARTESIAN_POINT('Ctrl Pts',(6.56268467750003,35.3282500034686,-10.0698455118856));
#28198=CARTESIAN_POINT('Ctrl Pts',(6.56268467749999,35.2012500034686,-7.93750000000004));
#28199=CARTESIAN_POINT('Ctrl Pts',(6.56268467749997,35.0742500034685,-5.80515448811441));
#28200=CARTESIAN_POINT('Ctrl Pts',(5.30932343282159,34.9472500034685,-4.08005073111972));
#28201=CARTESIAN_POINT('Ctrl Pts',(4.05596218814318,34.8202500034686,-2.35494697412514));
#28202=CARTESIAN_POINT('Ctrl Pts',(2.0279810940716,34.6932500034686,-1.69601597307323));
#28203=CARTESIAN_POINT('Ctrl Pts',(0.,34.5662500034686,-1.0370849720215));
#28204=CARTESIAN_POINT('Ctrl Pts',(-2.0279810940716,34.4392500034686,-1.69601597307323));
#28205=CARTESIAN_POINT('Ctrl Pts',(-4.05596218814318,34.3122500034686,-2.35494697412514));
#28206=CARTESIAN_POINT('Ctrl Pts',(-5.30932343282153,34.1852500034686,-4.08005073111972));
#28207=CARTESIAN_POINT('Ctrl Pts',(-6.56268467749997,34.0582500034686,-5.80515448811441));
#28208=CARTESIAN_POINT('Ctrl Pts',(-6.56268467749999,33.9312500034686,-7.93750000000004));
#28209=CARTESIAN_POINT('Ctrl Pts',(-6.56268467750003,33.8042500034686,-10.0698455118856));
#28210=CARTESIAN_POINT('Ctrl Pts',(-5.30932343282148,33.6772500034685,-11.7949492688803));
#28211=CARTESIAN_POINT('Ctrl Pts',(-4.05596218814306,33.5502500034685,-13.5200530258749));
#28212=CARTESIAN_POINT('Ctrl Pts',(-2.02798109407154,33.4232500034688,-14.1789840269267));
#28213=CARTESIAN_POINT('Ctrl Pts',(0.,33.2962500034685,-14.8379150279786));
#28214=CARTESIAN_POINT('Ctrl Pts',(2.02798109407165,33.1692500034688,-14.1789840269267));
#28215=CARTESIAN_POINT('Ctrl Pts',(4.05596218814318,33.0422500034686,-13.5200530258749));
#28216=CARTESIAN_POINT('Ctrl Pts',(5.30932343282159,32.9152500034686,-11.7949492688803));
#28217=CARTESIAN_POINT('Ctrl Pts',(6.56268467750003,32.7882500034685,-10.0698455118856));
#28218=CARTESIAN_POINT('Ctrl Pts',(6.56268467750004,32.6612500034686,-7.93750000000004));
#28219=CARTESIAN_POINT('Ctrl Pts',(6.56268467750008,32.5342500034685,-5.80515448811441));
#28220=CARTESIAN_POINT('Ctrl Pts',(5.30932343282159,32.4072500034686,-4.08005073111972));
#28221=CARTESIAN_POINT('Ctrl Pts',(4.05596218814318,32.2802500034685,-2.35494697412514));
#28222=CARTESIAN_POINT('Ctrl Pts',(2.02798109407165,32.1532500034687,-1.69601597307323));
#28223=CARTESIAN_POINT('Ctrl Pts',(0.,32.0262500034685,-1.0370849720215));
#28224=CARTESIAN_POINT('Ctrl Pts',(-2.02798109407154,31.8992500034685,-1.69601597307323));
#28225=CARTESIAN_POINT('Ctrl Pts',(-4.05596218814318,31.7722500034685,-2.35494697412514));
#28226=CARTESIAN_POINT('Ctrl Pts',(-5.30932343282148,31.6452500034686,-4.08005073111972));
#28227=CARTESIAN_POINT('Ctrl Pts',(-6.56268467749997,31.5182500034685,-5.80515448811441));
#28228=CARTESIAN_POINT('Ctrl Pts',(-6.56268467749999,31.3912500034687,-7.93750000000004));
#28229=CARTESIAN_POINT('Ctrl Pts',(-6.56268467750003,31.2642500034685,-10.0698455118856));
#28230=CARTESIAN_POINT('Ctrl Pts',(-5.30932343282148,31.1372500034686,-11.7949492688803));
#28231=CARTESIAN_POINT('Ctrl Pts',(-4.05596218814318,31.0102500034686,-13.5200530258749));
#28232=CARTESIAN_POINT('Ctrl Pts',(-2.0279810940716,30.8832500034687,-14.1789840269267));
#28233=CARTESIAN_POINT('Ctrl Pts',(0.,30.7562500034685,-14.8379150279786));
#28234=CARTESIAN_POINT('Ctrl Pts',(2.0279810940716,30.6292500034687,-14.1789840269267));
#28235=CARTESIAN_POINT('Ctrl Pts',(4.05596218814312,30.5022500034686,-13.5200530258749));
#28236=CARTESIAN_POINT('Ctrl Pts',(5.30932343282159,30.3752500034686,-11.7949492688803));
#28237=CARTESIAN_POINT('Ctrl Pts',(6.56268467750003,30.2482500034686,-10.0698455118856));
#28238=CARTESIAN_POINT('Ctrl Pts',(6.5626846775001,30.1212500034686,-7.93750000000004));
#28239=CARTESIAN_POINT('Ctrl Pts',(6.56268467750003,29.9942500034686,-5.80515448811441));
#28240=CARTESIAN_POINT('Ctrl Pts',(5.30932343282159,29.8672500034686,-4.08005073111972));
#28241=CARTESIAN_POINT('Ctrl Pts',(4.05596218814318,29.7402500034686,-2.35494697412514));
#28242=CARTESIAN_POINT('Ctrl Pts',(2.02798109407165,29.6132500034686,-1.69601597307323));
#28243=CARTESIAN_POINT('Ctrl Pts',(0.,29.4862500034686,-1.0370849720215));
#28244=CARTESIAN_POINT('Ctrl Pts',(-2.02798109407154,29.3592500034686,-1.69601597307323));
#28245=CARTESIAN_POINT('Ctrl Pts',(-4.05596218814312,29.2322500034686,-2.35494697412503));
#28246=CARTESIAN_POINT('Ctrl Pts',(-5.30932343282159,29.1052500034686,-4.08005073111972));
#28247=CARTESIAN_POINT('Ctrl Pts',(-6.56268467749997,28.9782500034685,-5.80515448811441));
#28248=CARTESIAN_POINT('Ctrl Pts',(-6.56268467749993,28.8512500034686,-7.93750000000004));
#28249=CARTESIAN_POINT('Ctrl Pts',(-6.56268467750003,28.7242500034685,-10.0698455118856));
#28250=CARTESIAN_POINT('Ctrl Pts',(-5.30932343282159,28.5972500034687,-11.7949492688803));
#28251=CARTESIAN_POINT('Ctrl Pts',(-4.05596218814306,28.4702500034686,-13.5200530258749));
#28252=CARTESIAN_POINT('Ctrl Pts',(-2.0279810940716,28.3432500034687,-14.1789840269267));
#28253=CARTESIAN_POINT('Ctrl Pts',(1.1673575708729E-13,28.2162500034685,
-14.8379150279786));
#28254=CARTESIAN_POINT('Ctrl Pts',(2.0279810940716,28.0892500034687,-14.1789840269267));
#28255=CARTESIAN_POINT('Ctrl Pts',(4.05596218814324,27.9622500034685,-13.5200530258749));
#28256=CARTESIAN_POINT('Ctrl Pts',(5.30932343282159,27.8352500034685,-11.7949492688803));
#28257=CARTESIAN_POINT('Ctrl Pts',(6.56268467750003,27.7082500034685,-10.0698455118856));
#28258=CARTESIAN_POINT('Ctrl Pts',(6.5626846775001,27.5812500034686,-7.93750000000004));
#28259=CARTESIAN_POINT('Ctrl Pts',(6.56268467750003,27.4542500034686,-5.80515448811441));
#28260=CARTESIAN_POINT('Ctrl Pts',(5.30932343282153,27.3272500034686,-4.08005073111972));
#28261=CARTESIAN_POINT('Ctrl Pts',(4.05596218814312,27.2002500034686,-2.35494697412514));
#28262=CARTESIAN_POINT('Ctrl Pts',(2.02798109407165,27.0732500034686,-1.69601597307323));
#28263=CARTESIAN_POINT('Ctrl Pts',(1.1673575708729E-13,26.9462500034685,
-1.0370849720215));
#28264=CARTESIAN_POINT('Ctrl Pts',(-2.02798109407148,26.8192500034686,-1.69601597307323));
#28265=CARTESIAN_POINT('Ctrl Pts',(-4.05596218814312,26.6922500034685,-2.35494697412503));
#28266=CARTESIAN_POINT('Ctrl Pts',(-5.30932343282159,26.5652500034685,-4.08005073111972));
#28267=CARTESIAN_POINT('Ctrl Pts',(-6.56268467750008,26.4382500034685,-5.80515448811441));
#28268=CARTESIAN_POINT('Ctrl Pts',(-6.56268467750004,26.3112500034686,-7.93750000000004));
#28269=CARTESIAN_POINT('Ctrl Pts',(-6.56268467749997,26.1842500034686,-10.0698455118856));
#28270=CARTESIAN_POINT('Ctrl Pts',(-5.30932343282159,26.0572500034686,-11.7949492688803));
#28271=CARTESIAN_POINT('Ctrl Pts',(-4.05596218814318,25.9302500034685,-13.5200530258749));
#28272=CARTESIAN_POINT('Ctrl Pts',(-2.0279810940716,25.8032500034687,-14.1789840269267));
#28273=CARTESIAN_POINT('Ctrl Pts',(0.,25.6762500034686,-14.8379150279786));
#28274=CARTESIAN_POINT('Ctrl Pts',(2.02798109407165,25.5492500034687,-14.1789840269267));
#28275=CARTESIAN_POINT('Ctrl Pts',(4.05596218814312,25.4222500034686,-13.5200530258749));
#28276=CARTESIAN_POINT('Ctrl Pts',(5.30932343282153,25.2952500034686,-11.7949492688803));
#28277=CARTESIAN_POINT('Ctrl Pts',(6.56268467750008,25.1682500034686,-10.0698455118856));
#28278=CARTESIAN_POINT('Ctrl Pts',(6.5626846775001,25.0412500034685,-7.93750000000004));
#28279=CARTESIAN_POINT('Ctrl Pts',(6.56268467750003,24.9142500034686,-5.80515448811441));
#28280=CARTESIAN_POINT('Ctrl Pts',(5.30932343282153,24.7872500034686,-4.08005073111972));
#28281=CARTESIAN_POINT('Ctrl Pts',(4.05596218814324,24.6602500034686,-2.35494697412514));
#28282=CARTESIAN_POINT('Ctrl Pts',(2.02798109407171,24.5332500034686,-1.69601597307323));
#28283=CARTESIAN_POINT('Ctrl Pts',(0.,24.4062500034686,-1.0370849720215));
#28284=CARTESIAN_POINT('Ctrl Pts',(-2.0279810940716,24.2792500034685,-1.69601597307323));
#28285=CARTESIAN_POINT('Ctrl Pts',(-4.05596218814312,24.1522500034685,-2.35494697412503));
#28286=CARTESIAN_POINT('Ctrl Pts',(-5.30932343282159,24.0252500034685,-4.08005073111972));
#28287=CARTESIAN_POINT('Ctrl Pts',(-6.56268467749991,23.8982500034686,-5.80515448811441));
#28288=CARTESIAN_POINT('Ctrl Pts',(-6.56268467749999,23.7712500034686,-7.93750000000004));
#28289=CARTESIAN_POINT('Ctrl Pts',(-6.56268467749997,23.6442500034686,-10.0698455118856));
#28290=CARTESIAN_POINT('Ctrl Pts',(-5.30932343282164,23.5172500034686,-11.7949492688803));
#28291=CARTESIAN_POINT('Ctrl Pts',(-4.05596218814312,23.3902500034686,-13.5200530258749));
#28292=CARTESIAN_POINT('Ctrl Pts',(-2.02798109407154,23.2632500034686,-14.1789840269267));
#28293=CARTESIAN_POINT('Ctrl Pts',(0.,23.1362500034685,-14.8379150279786));
#28294=CARTESIAN_POINT('Ctrl Pts',(2.02798109407165,23.0092500034686,-14.1789840269267));
#28295=CARTESIAN_POINT('Ctrl Pts',(4.05596218814312,22.8822500034685,-13.5200530258749));
#28296=CARTESIAN_POINT('Ctrl Pts',(5.30932343282153,22.7552500034686,-11.7949492688803));
#28297=CARTESIAN_POINT('Ctrl Pts',(6.56268467749997,22.6282500034686,-10.0698455118856));
#28298=CARTESIAN_POINT('Ctrl Pts',(6.5626846775001,22.5012500034686,-7.93750000000004));
#28299=CARTESIAN_POINT('Ctrl Pts',(6.56268467750003,22.3742500034686,-5.80515448811441));
#28300=CARTESIAN_POINT('Ctrl Pts',(5.30932343282159,22.2472500034686,-4.08005073111972));
#28301=CARTESIAN_POINT('Ctrl Pts',(4.05596218814312,22.1202500034686,-2.35494697412503));
#28302=CARTESIAN_POINT('Ctrl Pts',(2.0279810940716,21.9932500034685,-1.69601597307323));
#28303=CARTESIAN_POINT('Ctrl Pts',(0.,21.8662500034686,-1.0370849720215));
#28304=CARTESIAN_POINT('Ctrl Pts',(-2.0279810940716,21.7392500034686,-1.69601597307323));
#28305=CARTESIAN_POINT('Ctrl Pts',(-4.05596218814312,21.6122500034686,-2.35494697412503));
#28306=CARTESIAN_POINT('Ctrl Pts',(-5.30932343282153,21.4852500034687,-4.08005073111972));
#28307=CARTESIAN_POINT('Ctrl Pts',(-6.56268467750003,21.3582500034686,-5.80515448811441));
#28308=CARTESIAN_POINT('Ctrl Pts',(-6.56268467749999,21.2312500034685,-7.93750000000004));
#28309=CARTESIAN_POINT('Ctrl Pts',(-6.56268467749997,21.1042500034685,-10.0698455118856));
#28310=CARTESIAN_POINT('Ctrl Pts',(-5.30932343282164,20.9772500034686,-11.7949492688803));
#28311=CARTESIAN_POINT('Ctrl Pts',(-4.05596218814312,20.8502500034685,-13.5200530258749));
#28312=CARTESIAN_POINT('Ctrl Pts',(-2.02798109407154,20.7232500034687,-14.1789840269267));
#28313=CARTESIAN_POINT('Ctrl Pts',(0.,20.5962500034686,-14.8379150279786));
#28314=CARTESIAN_POINT('Ctrl Pts',(2.02798109407171,20.4692500034686,-14.1789840269267));
#28315=CARTESIAN_POINT('Ctrl Pts',(4.05596218814324,20.3422500034686,-13.5200530258749));
#28316=CARTESIAN_POINT('Ctrl Pts',(5.30932343282159,20.2152500034686,-11.7949492688803));
#28317=CARTESIAN_POINT('Ctrl Pts',(6.56268467750008,20.0882500034685,-10.0698455118856));
#28318=CARTESIAN_POINT('Ctrl Pts',(6.56268467749999,19.9612500034686,-7.93750000000004));
#28319=CARTESIAN_POINT('Ctrl Pts',(6.56268467750003,19.8342500034686,-5.80515448811441));
#28320=CARTESIAN_POINT('Ctrl Pts',(5.30932343282159,19.7072500034685,-4.08005073111972));
#28321=CARTESIAN_POINT('Ctrl Pts',(4.65426850829619,19.6408749054927,-3.17844497608727));
#28322=CARTESIAN_POINT('Ctrl Pts',(3.73830419723802,19.5711012915162,-2.54362273914156));
#28323=CARTESIAN_POINT('Ctrl Pts',(-4.37003557241966,17.7638095496546,-15.102482089171));
#28324=CARTESIAN_POINT('Ctrl Pts',(-4.2103702834995,18.1928079871481,-14.6678643719681));
#28325=CARTESIAN_POINT('Ctrl Pts',(-4.33444454882375,18.8064629622641,-14.587046595076));
#28326=CARTESIAN_POINT('Ctrl Pts',(-4.08157677823063,17.9187863946121,-15.1900626743679));
#28327=CARTESIAN_POINT('Ctrl Pts',(-3.94432134458797,18.3471485010018,-14.8326958966496));
#28328=CARTESIAN_POINT('Ctrl Pts',(-4.00038492834513,18.920735573139,-14.8048348003922));
#28329=CARTESIAN_POINT('Ctrl Pts',(-3.75474604664856,18.0355130533343,-15.2941158606652));
#28330=CARTESIAN_POINT('Ctrl Pts',(-3.63142428276688,18.4451150135817,-15.0057172827804));
#28331=CARTESIAN_POINT('Ctrl Pts',(-3.64549788804367,18.9604219221267,-14.9998486582339));
#28332=CARTESIAN_POINT('Ctrl Pts',(-3.06702447279691,18.1853704931012,-15.4855412059039));
#28333=CARTESIAN_POINT('Ctrl Pts',(-2.96645051654635,18.5378312167901,-15.3082202157406));
#28334=CARTESIAN_POINT('Ctrl Pts',(-2.92607963880819,18.943217221379,-15.3261118803759));
#28335=CARTESIAN_POINT('Ctrl Pts',(-2.70267020745179,18.2245844759334,-15.5753399203331));
#28336=CARTESIAN_POINT('Ctrl Pts',(-2.61131057061418,18.5396307567559,-15.442931788489));
#28337=CARTESIAN_POINT('Ctrl Pts',(-2.55821925230425,18.8884651665,-15.4610221924584));
#28338=CARTESIAN_POINT('Ctrl Pts',(-1.96287492552905,18.2420368665519,-15.7200549564683));
#28339=CARTESIAN_POINT('Ctrl Pts',(-1.89153946623817,18.4751290933259,-15.6554598329745));
#28340=CARTESIAN_POINT('Ctrl Pts',(-1.82891453529875,18.7188972454106,-15.6707363824264));
#28341=CARTESIAN_POINT('Ctrl Pts',(-1.58083481983854,18.222769633288,-15.7776716447618));
#28342=CARTESIAN_POINT('Ctrl Pts',(-1.52010391061206,18.4109075711029,-15.7376927898266));
#28343=CARTESIAN_POINT('Ctrl Pts',(-1.46353132936861,18.6039976265509,-15.7477141627275));
#28344=CARTESIAN_POINT('Ctrl Pts',(-0.800159047972911,18.1403974723434,
-15.8549367200197));
#28345=CARTESIAN_POINT('Ctrl Pts',(-0.765887806043689,18.2357094897268,
-15.8471046363309));
#28346=CARTESIAN_POINT('Ctrl Pts',(-0.72911749444839,18.3301937694425,-15.8501327855033));
#28347=CARTESIAN_POINT('Ctrl Pts',(-0.3987363866075,18.0770350176174,-15.8749999999984));
#28348=CARTESIAN_POINT('Ctrl Pts',(-0.379968212271851,18.1240305159854,
-15.8749999999992));
#28349=CARTESIAN_POINT('Ctrl Pts',(-0.361264584887649,18.1710404017991,
-15.875));
#28350=CARTESIAN_POINT('Ctrl Pts',(4.96157977224833E-14,18.0000000000001,
-15.875));
#28351=CARTESIAN_POINT('Ctrl Pts',(4.96157977224833E-14,18.0000000000001,
-15.875));
#28352=CARTESIAN_POINT('Ctrl Pts',(4.96157977224833E-14,18.0000000000001,
-15.875));
#28353=CARTESIAN_POINT('',(-4.26261338778688,18.0849267018157,-14.875));
#28354=CARTESIAN_POINT('Ctrl Pts',(5.55111512312578E-14,18.0000000000001,
-15.875));
#28355=CARTESIAN_POINT('Ctrl Pts',(-0.733684917776591,18.1419056781966,
-15.875));
#28356=CARTESIAN_POINT('Ctrl Pts',(-1.47554802668037,18.248989994314,-15.8100424832836));
#28357=CARTESIAN_POINT('Ctrl Pts',(-2.37917217060925,18.2923856158391,-15.6165480209598));
#28358=CARTESIAN_POINT('Ctrl Pts',(-2.55900832274013,18.2964779051254,-15.5720852748806));
#28359=CARTESIAN_POINT('Ctrl Pts',(-2.91667689706805,18.2933500475869,-15.4698863303733));
#28360=CARTESIAN_POINT('Ctrl Pts',(-3.09551309904666,18.2860499025369,-15.4117537005875));
#28361=CARTESIAN_POINT('Ctrl Pts',(-3.61925135711828,18.2429598209237,-15.2173122956099));
#28362=CARTESIAN_POINT('Ctrl Pts',(-3.95179505566483,18.1882637114374,-15.0609272799604));
#28363=CARTESIAN_POINT('Ctrl Pts',(-4.26261338778688,18.0849267018157,-14.875));
#28364=CARTESIAN_POINT('Origin',(-5.10514446416555,18.819869818891,-15.875));
#28365=CARTESIAN_POINT('Ctrl Pts',(-4.29373077449685,18.819869818891,-14.6134105960265));
#28366=CARTESIAN_POINT('Ctrl Pts',(-4.05040020405459,17.5517750653647,-14.7699129852744));
#28367=CARTESIAN_POINT('Ctrl Pts',(-4.71244104384512,17.3721875251302,-15.875));
#28368=CARTESIAN_POINT('Ctrl Pts',(-4.85172205446064,18.6399031555503,-14.254528568441));
#28369=CARTESIAN_POINT('Ctrl Pts',(-4.60179941715923,17.4268547635552,-14.4435616230053));
#28370=CARTESIAN_POINT('Ctrl Pts',(-5.32488118024252,17.2060548471653,-15.4482730708507));
#28371=CARTESIAN_POINT('Ctrl Pts',(-5.35047866129627,18.4418014142638,-13.8366896334367));
#28372=CARTESIAN_POINT('Ctrl Pts',(-5.12064004592465,17.2814545873273,-14.047160515657));
#28373=CARTESIAN_POINT('Ctrl Pts',(-5.872239451894,17.0232013062602,-14.9514971234146));
#28374=CARTESIAN_POINT('Ctrl Pts',(-6.01799603717833,18.142003732685,-13.1234105702918));
#28375=CARTESIAN_POINT('Ctrl Pts',(-5.8322275983879,17.0508424851127,-13.3390649200856));
#28376=CARTESIAN_POINT('Ctrl Pts',(-6.60485088974141,16.746464983624,-14.1034251661552));
#28377=CARTESIAN_POINT('Ctrl Pts',(-6.22802018553564,18.0410299920571,-12.8694063525054));
#28378=CARTESIAN_POINT('Ctrl Pts',(-6.05721596844286,16.9724647253111,-13.085858679893));
#28379=CARTESIAN_POINT('Ctrl Pts',(-6.83535589111353,16.6532584546768,-13.8014201512646));
#28380=CARTESIAN_POINT('Ctrl Pts',(-6.6144435597649,17.845539227244,-12.3376218274051));
#28381=CARTESIAN_POINT('Ctrl Pts',(-6.47397956801525,16.8187344562347,-12.5492603262157));
#28382=CARTESIAN_POINT('Ctrl Pts',(-7.25946198077295,16.4728054400627,-13.1691409130384));
#28383=CARTESIAN_POINT('Ctrl Pts',(-6.78984519594626,17.7516276808024,-12.0616732803204));
#28384=CARTESIAN_POINT('Ctrl Pts',(-6.66536331485427,16.7437399954129,-12.2678113800685));
#28385=CARTESIAN_POINT('Ctrl Pts',(-7.45196819832983,16.3861178595998,-12.841044608914));
#28386=CARTESIAN_POINT('Ctrl Pts',(-7.1060232070069,17.5758144266797,-11.4892935205334));
#28387=CARTESIAN_POINT('Ctrl Pts',(-7.01161694949603,16.6021903559506,-11.6791754308633));
#28388=CARTESIAN_POINT('Ctrl Pts',(-7.79897883144068,16.2238287011529,-12.1604985952507));
#28389=CARTESIAN_POINT('Ctrl Pts',(-7.24680107601186,17.4939013437499,-11.1928654121415));
#28390=CARTESIAN_POINT('Ctrl Pts',(-7.1672942491468,16.53538393131,-11.3716926957734));
#28391=CARTESIAN_POINT('Ctrl Pts',(-7.95348488826811,16.1482166253278,-11.8080525767787));
#28392=CARTESIAN_POINT('Ctrl Pts',(-7.49273513776195,17.3468185637659,-10.5780397094536));
#28393=CARTESIAN_POINT('Ctrl Pts',(-7.43969881407854,16.4148594991967,-10.7303703061362));
#28394=CARTESIAN_POINT('Ctrl Pts',(-8.22340161649152,16.0124479046868,-11.0770393394486));
#28395=CARTESIAN_POINT('Ctrl Pts',(-7.59843488959469,17.2812951267938,-10.2569047180054));
#28396=CARTESIAN_POINT('Ctrl Pts',(-7.55776347710441,16.3605717978341,-10.393033282372));
#28397=CARTESIAN_POINT('Ctrl Pts',(-8.33940885518503,15.9519647326955,-10.6952174205744));
#28398=CARTESIAN_POINT('Ctrl Pts',(-7.85078664959267,17.1222147255269,-9.28539995987796));
#28399=CARTESIAN_POINT('Ctrl Pts',(-7.83853818369,16.229043980975,-9.37303471985337));
#28400=CARTESIAN_POINT('Ctrl Pts',(-8.6163691151618,15.8051212845607,-9.5401212122307));
#28401=CARTESIAN_POINT('Ctrl Pts',(-7.93672823551223,17.0646099827074,-8.62351488694819));
#28402=CARTESIAN_POINT('Ctrl Pts',(-7.93663307907031,16.1799952820739,-8.6658176185236));
#28403=CARTESIAN_POINT('Ctrl Pts',(-8.71069143789301,15.751947676348,-8.75315549550617));
#28404=CARTESIAN_POINT('Ctrl Pts',(-7.93768657939644,17.0639797987105,-7.77723195581193));
#28405=CARTESIAN_POINT('Ctrl Pts',(-7.93770957586298,16.1794674107193,-7.76735582075032));
#28406=CARTESIAN_POINT('Ctrl Pts',(-8.71174323535012,15.7513659680398,-7.74694508131947));
#28407=CARTESIAN_POINT('Ctrl Pts',(-7.93240014505282,17.0674607979061,-7.60633724591963));
#28408=CARTESIAN_POINT('Ctrl Pts',(-7.93176509524179,16.1823866550743,-7.58584716868171));
#28409=CARTESIAN_POINT('Ctrl Pts',(-8.70594128558497,15.7545791980315,-7.54375530815316));
#28410=CARTESIAN_POINT('Ctrl Pts',(-7.91102975013305,17.0814770208683,-7.2679859049775));
#28411=CARTESIAN_POINT('Ctrl Pts',(-7.90776940619295,16.1941201670182,-7.22681048952224));
#28412=CARTESIAN_POINT('Ctrl Pts',(-8.68248692160874,15.767517250068,-7.14146355629932));
#28413=CARTESIAN_POINT('Ctrl Pts',(-7.89499158493917,17.0919817317593,-7.10010500886008));
#28414=CARTESIAN_POINT('Ctrl Pts',(-7.88974897820912,16.2029188357821,-7.04867703153029));
#28415=CARTESIAN_POINT('Ctrl Pts',(-8.66488476781423,15.7772139061693,-6.94185713653414));
#28416=CARTESIAN_POINT('Ctrl Pts',(-7.831248853586,17.1334594467781,-6.60022193131186));
#28417=CARTESIAN_POINT('Ctrl Pts',(-7.81819429110638,16.2376097544146,-6.51852828695844));
#28418=CARTESIAN_POINT('Ctrl Pts',(-8.59492605887025,15.8155010279353,-6.34750796554458));
#28419=CARTESIAN_POINT('Ctrl Pts',(-7.76798084410886,17.1743995785599,-6.27196753629823));
#28420=CARTESIAN_POINT('Ctrl Pts',(-7.74705485466677,16.2718853507128,-6.17083955222712));
#28421=CARTESIAN_POINT('Ctrl Pts',(-8.5254883642425,15.8532919184049,-5.95722124393312));
#28422=CARTESIAN_POINT('Ctrl Pts',(-7.60054746639873,17.2799782900503,-5.62509800356719));
#28423=CARTESIAN_POINT('Ctrl Pts',(-7.56012110045393,16.3594808325921,-5.48933294767266));
#28424=CARTESIAN_POINT('Ctrl Pts',(-8.34172744353445,15.9507491910813,-5.1881086499226));
#28425=CARTESIAN_POINT('Ctrl Pts',(-7.49539872629226,17.3451970522154,-5.3043111217849));
#28426=CARTESIAN_POINT('Ctrl Pts',(-7.44265254159941,16.413527382139,-5.15230673839765));
#28427=CARTESIAN_POINT('Ctrl Pts',(-8.22632494925749,16.0109511247932,-4.80670062525685));
#28428=CARTESIAN_POINT('Ctrl Pts',(-7.24864440937974,17.4928269391644,-4.68606340046019));
#28429=CARTESIAN_POINT('Ctrl Pts',(-7.16932337182266,16.5345111926349,-4.50736742998995));
#28430=CARTESIAN_POINT('Ctrl Pts',(-7.95550797735527,16.1472248672498,-4.07161868859358));
#28431=CARTESIAN_POINT('Ctrl Pts',(-7.10730366773621,17.5750930730766,-4.38813130745318));
#28432=CARTESIAN_POINT('Ctrl Pts',(-7.01301294517219,16.6016115427834,-4.19830815404623));
#28433=CARTESIAN_POINT('Ctrl Pts',(-7.80038415841105,16.2231628362877,-3.71738446795083));
#28434=CARTESIAN_POINT('Ctrl Pts',(-6.78976913329141,17.7516792840673,-3.81308262809748));
#28435=CARTESIAN_POINT('Ctrl Pts',(-6.66526779473809,16.7437872397752,-3.60691491129501));
#28436=CARTESIAN_POINT('Ctrl Pts',(-7.45188471830734,16.3861654933836,-3.03366517195585));
#28437=CARTESIAN_POINT('Ctrl Pts',(-6.61357326878162,17.8460111736686,-3.53596957548935));
#28438=CARTESIAN_POINT('Ctrl Pts',(-6.47301642497377,16.8191166151697,-3.32428492883157));
#28439=CARTESIAN_POINT('Ctrl Pts',(-7.25850682191698,16.4732410829151,-2.70418429828093));
#28440=CARTESIAN_POINT('Ctrl Pts',(-6.22536744072326,18.0423400532628,-3.00215586940299));
#28441=CARTESIAN_POINT('Ctrl Pts',(-6.05435246414523,16.9734934471226,-2.7856742472814));
#28442=CARTESIAN_POINT('Ctrl Pts',(-6.83244445950206,16.6544677419447,-2.0694924117879));
#28443=CARTESIAN_POINT('Ctrl Pts',(-6.01671476286826,18.1425966890778,-2.75014226738085));
#28444=CARTESIAN_POINT('Ctrl Pts',(-5.83087248062031,17.0512960564225,-2.53450877806538));
#28445=CARTESIAN_POINT('Ctrl Pts',(-6.6034446698575,16.7470123279823,-1.76985419200821));
#28446=CARTESIAN_POINT('Ctrl Pts',(-5.35036565224163,18.4418170514269,-2.03834618162601));
#28447=CARTESIAN_POINT('Ctrl Pts',(-5.12056163117185,17.2814504145844,-1.82792133257243));
#28448=CARTESIAN_POINT('Ctrl Pts',(-5.87211542254812,17.0232157405731,-0.923545459877607));
#28449=CARTESIAN_POINT('Ctrl Pts',(-4.85205601954726,18.6397954432763,-1.62068622715121));
#28450=CARTESIAN_POINT('Ctrl Pts',(-4.60212559172194,17.4267808683366,-1.4316314270215));
#28451=CARTESIAN_POINT('Ctrl Pts',(-5.32524721431279,17.2059555554684,-0.426981969186781));
#28452=CARTESIAN_POINT('Ctrl Pts',(-4.29373077449685,18.8198698188909,-1.26158940397351));
#28453=CARTESIAN_POINT('Ctrl Pts',(-4.05040020405459,17.5517750653646,-1.10508701472557));
#28454=CARTESIAN_POINT('Ctrl Pts',(-4.71244104384512,17.3721875251301,-1.06752213906266E-15));
#28455=CARTESIAN_POINT('Ctrl Pts',(-4.26261338778693,18.0849267018157,-14.875));
#28456=CARTESIAN_POINT('Ctrl Pts',(-4.36728621357164,18.0345646349843,-14.8238231458034));
#28457=CARTESIAN_POINT('Ctrl Pts',(-4.47066603984279,17.9836961344339,-14.7713160666174));
#28458=CARTESIAN_POINT('Ctrl Pts',(-4.57293726166006,17.9323320438858,-14.7174958178478));
#28459=CARTESIAN_POINT('Ctrl Pts',(-4.67146734523438,17.8828468803716,-14.6656443437476));
#28460=CARTESIAN_POINT('Ctrl Pts',(-4.76896783203404,17.8329013817977,-14.6125734014967));
#28461=CARTESIAN_POINT('Ctrl Pts',(-4.86557698809706,17.7825339109652,-14.5583260017153));
#28462=CARTESIAN_POINT('Ctrl Pts',(-4.95543150101896,17.7356879934228,-14.5078714290509));
#28463=CARTESIAN_POINT('Ctrl Pts',(-5.04451439001857,17.6884769511579,-14.4563988610072));
#28464=CARTESIAN_POINT('Ctrl Pts',(-5.13292189721992,17.6409596293802,-14.4039733608045));
#28465=CARTESIAN_POINT('Ctrl Pts',(-5.21778196059643,17.5953489899085,-14.353651488708));
#28466=CARTESIAN_POINT('Ctrl Pts',(-5.30201934606125,17.549455956929,-14.3024512486777));
#28467=CARTESIAN_POINT('Ctrl Pts',(-5.38571159587319,17.503361604272,-14.2504642311565));
#28468=CARTESIAN_POINT('Ctrl Pts',(-5.46816101792737,17.4579517515669,-14.1992492195087));
#28469=CARTESIAN_POINT('Ctrl Pts',(-5.55008099149818,17.4123461809608,-14.1472700900238));
#28470=CARTESIAN_POINT('Ctrl Pts',(-5.63154386899368,17.3666552413443,-14.0946549924496));
#28471=CARTESIAN_POINT('Ctrl Pts',(-5.70699601269251,17.3243356051166,-14.0459220968665));
#28472=CARTESIAN_POINT('Ctrl Pts',(-5.78205573161066,17.281942771358,-13.996643579046));
#28473=CARTESIAN_POINT('Ctrl Pts',(-5.85678370662441,17.239594274303,-13.9469596296543));
#28474=CARTESIAN_POINT('Ctrl Pts',(-5.86273675107024,17.2362206717781,-13.943001663994));
#28475=CARTESIAN_POINT('Ctrl Pts',(-5.86868769334399,17.2328473673154,-13.9390411472596));
#28476=CARTESIAN_POINT('Ctrl Pts',(-5.87463656592348,17.2294744291862,-13.9350781619607));
#28477=CARTESIAN_POINT('Ctrl Pts',(-5.94218023588408,17.191177992886,-13.8900823131659));
#28478=CARTESIAN_POINT('Ctrl Pts',(-6.00952609799308,17.1528912123609,-13.8447109072821));
#28479=CARTESIAN_POINT('Ctrl Pts',(-6.07672203282712,17.1147265085998,-13.7991041023221));
#28480=CARTESIAN_POINT('Ctrl Pts',(-6.15303774324791,17.0713821234412,-13.7473075802685));
#28481=CARTESIAN_POINT('Ctrl Pts',(-6.2291789019832,17.028143489955,-13.6951247404768));
#28482=CARTESIAN_POINT('Ctrl Pts',(-6.3052620006147,16.9851285038395,-13.6426434530328));
#28483=CARTESIAN_POINT('Ctrl Pts',(-6.37709936525376,16.9445139219139,-13.5930908263568));
#28484=CARTESIAN_POINT('Ctrl Pts',(-6.44888463340197,16.9040987380384,-13.5432721433623));
#28485=CARTESIAN_POINT('Ctrl Pts',(-6.52074248491161,16.8640091075666,-13.493287537862));
#28486=CARTESIAN_POINT('Ctrl Pts',(-6.56132078321264,16.8413703986449,-13.4650611131939));
#28487=CARTESIAN_POINT('Ctrl Pts',(-6.60192274095193,16.8188359974411,-13.4367822566398));
#28488=CARTESIAN_POINT('Ctrl Pts',(-6.64257554275894,16.796432756076,-13.4084730253669));
#28489=CARTESIAN_POINT('Ctrl Pts',(-6.69153287005825,16.7694529964698,-13.3743808044272));
#28490=CARTESIAN_POINT('Ctrl Pts',(-6.74051510505213,16.7426909854859,-13.3402725411418));
#28491=CARTESIAN_POINT('Ctrl Pts',(-6.78965858551745,16.7161549427323,-13.3061343214082));
#28492=CARTESIAN_POINT('Ctrl Pts',(-6.84639050240779,16.6855213661553,-13.2667246860635));
#28493=CARTESIAN_POINT('Ctrl Pts',(-6.90327078439721,16.6552315277651,-13.2273240337237));
#28494=CARTESIAN_POINT('Ctrl Pts',(-6.96040712452314,16.6253536648596,-13.1879499262547));
#28495=CARTESIAN_POINT('Ctrl Pts',(-7.01594310573958,16.5963126652182,-13.1496786668776));
#28496=CARTESIAN_POINT('Ctrl Pts',(-7.07172086790775,16.5676606663574,-13.1114322899907));
#28497=CARTESIAN_POINT('Ctrl Pts',(-7.12782742604058,16.53949584061,-13.0732565035772));
#28498=CARTESIAN_POINT('Ctrl Pts',(-7.18144394311299,16.5125809858982,-13.0367749803451));
#28499=CARTESIAN_POINT('Ctrl Pts',(-7.23536057166625,16.4861109191502,-13.0003578234135));
#28500=CARTESIAN_POINT('Ctrl Pts',(-7.28964430395286,16.4602063421967,-12.9640742821639));
#28501=CARTESIAN_POINT('Ctrl Pts',(-7.33422861681448,16.4389303960745,-12.9342738854951));
#28502=CARTESIAN_POINT('Ctrl Pts',(-7.37906038061696,16.4180364302088,-12.9045640536257));
#28503=CARTESIAN_POINT('Ctrl Pts',(-7.42417289637397,16.3976113139917,-12.8750000000016));
#28504=CARTESIAN_POINT('',(-4.26261338778694,18.0849267018156,-1.));
#28505=CARTESIAN_POINT('Ctrl Pts',(-7.42417289637476,16.3976113139913,-2.99999999999997));
#28506=CARTESIAN_POINT('Ctrl Pts',(-7.36225162017796,16.4256467547421,-2.9594204869925));
#28507=CARTESIAN_POINT('Ctrl Pts',(-7.30094639302506,16.4545320426463,-2.91856077264145));
#28508=CARTESIAN_POINT('Ctrl Pts',(-7.24009139466157,16.4840912218767,-2.87754225192893));
#28509=CARTESIAN_POINT('Ctrl Pts',(-7.17579663629178,16.5153212003063,-2.83420520569084));
#28510=CARTESIAN_POINT('Ctrl Pts',(-7.11200471900219,16.5473033441628,-2.79069093814931));
#28511=CARTESIAN_POINT('Ctrl Pts',(-7.0485616279854,16.5798620319354,-2.7471168659627));
#28512=CARTESIAN_POINT('Ctrl Pts',(-6.98025522115035,16.614916549888,-2.70020256442825));
#28513=CARTESIAN_POINT('Ctrl Pts',(-6.91235344327022,16.6506392229992,-2.6532190682628));
#28514=CARTESIAN_POINT('Ctrl Pts',(-6.84470667791444,16.6868488321288,-2.60628234162304));
#28515=CARTESIAN_POINT('Ctrl Pts',(-6.77705991255867,16.7230584412584,-2.55934561498327));
#28516=CARTESIAN_POINT('Ctrl Pts',(-6.70966889386636,16.7597552671119,-2.51245542708785));
#28517=CARTESIAN_POINT('Ctrl Pts',(-6.64241644149763,16.7967930910134,-2.46569962889185));
#28518=CARTESIAN_POINT('Ctrl Pts',(-6.57233897132334,16.8353867319642,-2.41697979878676));
#28519=CARTESIAN_POINT('Ctrl Pts',(-6.50242163172557,16.8743437912577,-2.36840493401875));
#28520=CARTESIAN_POINT('Ctrl Pts',(-6.43251652697519,16.9135581508364,-2.32002298020697));
#28521=CARTESIAN_POINT('Ctrl Pts',(-6.35931673623709,16.954620715943,-2.26936074449228));
#28522=CARTESIAN_POINT('Ctrl Pts',(-6.28613110409549,16.9959654768125,-2.21890999430885));
#28523=CARTESIAN_POINT('Ctrl Pts',(-6.21280023886862,17.0375148551584,-2.16869022735185));
#28524=CARTESIAN_POINT('Ctrl Pts',(-6.16969661589326,17.0619374326576,-2.13917122612192));
#28525=CARTESIAN_POINT('Ctrl Pts',(-6.1265429451081,17.086431526281,-2.10973137070173));
#28526=CARTESIAN_POINT('Ctrl Pts',(-6.08330688289705,17.1109878358769,-2.08036939653045));
#28527=CARTESIAN_POINT('Ctrl Pts',(-6.0136392668642,17.1505561837009,-2.03305753143629));
#28528=CARTESIAN_POINT('Ctrl Pts',(-5.94390732283454,17.1902010442598,-1.98606424901363));
#28529=CARTESIAN_POINT('Ctrl Pts',(-5.87395832483882,17.2298569422314,-1.93947238083718));
#28530=CARTESIAN_POINT('Ctrl Pts',(-5.79682337542196,17.2735867421107,-1.88809406952459));
#28531=CARTESIAN_POINT('Ctrl Pts',(-5.71935440939585,17.3173647772406,-1.83714744008263));
#28532=CARTESIAN_POINT('Ctrl Pts',(-5.64148146818277,17.3610636873807,-1.7867839666029));
#28533=CARTESIAN_POINT('Ctrl Pts',(-5.56016891276116,17.4066927595241,-1.73419596023313));
#28534=CARTESIAN_POINT('Ctrl Pts',(-5.47841625448937,17.4522357096599,-1.68224347506384));
#28535=CARTESIAN_POINT('Ctrl Pts',(-5.39614987878206,17.4975832947874,-1.6310529385569));
#28536=CARTESIAN_POINT('Ctrl Pts',(-5.31003429924489,17.5450526714348,-1.57746722166816));
#28537=CARTESIAN_POINT('Ctrl Pts',(-5.22335621422618,17.5923081415182,-1.52471609071066));
#28538=CARTESIAN_POINT('Ctrl Pts',(-5.13603166624492,17.6392602637631,-1.47290009966545));
#28539=CARTESIAN_POINT('Ctrl Pts',(-5.04252759392154,17.6895349543925,-1.41741734840933));
#28540=CARTESIAN_POINT('Ctrl Pts',(-4.94828288017069,17.7394619360643,-1.36300648878106));
#28541=CARTESIAN_POINT('Ctrl Pts',(-4.8531872765823,17.7889697057021,-1.30974583887355));
#28542=CARTESIAN_POINT('Ctrl Pts',(-4.75201030281837,17.8416435005015,-1.25307916686139));
#28543=CARTESIAN_POINT('Ctrl Pts',(-4.64987085960817,17.893842962125,-1.19771403654983));
#28544=CARTESIAN_POINT('Ctrl Pts',(-4.54661799837511,17.9455214136771,-1.14370160718567));
#28545=CARTESIAN_POINT('Ctrl Pts',(-4.45291076337046,17.9924222428302,-1.09468257419079));
#28546=CARTESIAN_POINT('Ctrl Pts',(-4.35828650491551,18.0388947361867,-1.04677669805056));
#28547=CARTESIAN_POINT('Ctrl Pts',(-4.26261338778692,18.0849267018156,-1.00000000000002));
#28548=CARTESIAN_POINT('Origin',(-5.10514446416555,18.8198698188909,0.));
#28549=CARTESIAN_POINT('Ctrl Pts',(-4.33449582597651,18.8064455740235,-1.28798683503108));
#28550=CARTESIAN_POINT('Ctrl Pts',(-4.21041218740497,18.1927840286017,-1.2071616648505));
#28551=CARTESIAN_POINT('Ctrl Pts',(-4.3700807197326,17.7637855531036,-0.772531983761533));
#28552=CARTESIAN_POINT('Ctrl Pts',(-4.00042123744047,18.9207316512653,-1.07018515119445));
#28553=CARTESIAN_POINT('Ctrl Pts',(-3.94435406442238,18.3471385657429,-1.04232225428572));
#28554=CARTESIAN_POINT('Ctrl Pts',(-4.08161076289601,17.9187745448053,-0.684948449715675));
#28555=CARTESIAN_POINT('Ctrl Pts',(-3.64551666608151,18.9604224970613,-0.875159857664685));
#28556=CARTESIAN_POINT('Ctrl Pts',(-3.63144227316264,18.4451127783963,-0.869290948000206));
#28557=CARTESIAN_POINT('Ctrl Pts',(-3.75476449736778,18.0355093239667,-0.580889520521902));
#28558=CARTESIAN_POINT('Ctrl Pts',(-2.92607962857381,18.9432173241546,-0.548888115088505));
#28559=CARTESIAN_POINT('Ctrl Pts',(-2.96645048635243,18.5378314306372,-0.566779801034313));
#28560=CARTESIAN_POINT('Ctrl Pts',(-3.06702439599705,18.185370762247,-0.389458929501563));
#28561=CARTESIAN_POINT('Ctrl Pts',(-2.55821923863767,18.8884652562902,-0.413977802884962));
#28562=CARTESIAN_POINT('Ctrl Pts',(-2.61131053681094,18.5396309401508,-0.432068222184205));
#28563=CARTESIAN_POINT('Ctrl Pts',(-2.70267013757716,18.2245847168884,-0.299660180936123));
#28564=CARTESIAN_POINT('Ctrl Pts',(-1.82891451879158,18.7188973096676,-0.204263613546989));
#28565=CARTESIAN_POINT('Ctrl Pts',(-1.89153943192661,18.4751292208516,-0.21954016975466));
#28566=CARTESIAN_POINT('Ctrl Pts',(-1.96287487083709,18.2420370452619,-0.154945093056182));
#28567=CARTESIAN_POINT('Ctrl Pts',(-1.46353131432072,18.6039976779118,-0.127285834606972));
#28568=CARTESIAN_POINT('Ctrl Pts',(-1.52010388032437,18.4109076718901,-0.137307211669863));
#28569=CARTESIAN_POINT('Ctrl Pts',(-1.58083477323453,18.2227697776629,-0.0973283859171704));
#28570=CARTESIAN_POINT('Ctrl Pts',(-0.729117484549751,18.3301937948767,
-0.0248672136816333));
#28571=CARTESIAN_POINT('Ctrl Pts',(-0.765887787240446,18.2357095390217,
-0.027895363559901));
#28572=CARTESIAN_POINT('Ctrl Pts',(-0.800159021641761,18.1403975455722,
-0.0200632859980195));
#28573=CARTESIAN_POINT('Ctrl Pts',(-0.361264579836653,18.1710404144961,
-1.27030416149535E-14));
#28574=CARTESIAN_POINT('Ctrl Pts',(-0.37996820254999,18.1240305403966,-2.39037871064658E-13));
#28575=CARTESIAN_POINT('Ctrl Pts',(-0.398736372182772,18.0770350537363,
-4.65437000046116E-13));
#28576=CARTESIAN_POINT('Ctrl Pts',(9.87716250982808E-14,18.,-2.01661604082304E-14));
#28577=CARTESIAN_POINT('Ctrl Pts',(9.87716250982808E-14,18.,-2.01661604082304E-14));
#28578=CARTESIAN_POINT('Ctrl Pts',(9.87716250982808E-14,18.,-2.01661604082304E-14));
#28579=CARTESIAN_POINT('Ctrl Pts',(-4.26261338778694,18.0849267018156,-1.));
#28580=CARTESIAN_POINT('Ctrl Pts',(-3.95178714242432,18.188266342333,-0.814067986447267));
#28581=CARTESIAN_POINT('Ctrl Pts',(-3.61923443569505,18.2429627164578,-0.657679757707574));
#28582=CARTESIAN_POINT('Ctrl Pts',(-3.09548155756287,18.2860517458272,-0.463235421761033));
#28583=CARTESIAN_POINT('Ctrl Pts',(-2.91664062652111,18.2933512364511,-0.405102243904273));
#28584=CARTESIAN_POINT('Ctrl Pts',(-2.55896263908653,18.2964774327613,-0.302902733783915));
#28585=CARTESIAN_POINT('Ctrl Pts',(-2.37912173967015,18.2923841267789,-0.25843996217478));
#28586=CARTESIAN_POINT('Ctrl Pts',(-1.83693290496405,18.2663432658697,-0.142343866931082));
#28587=CARTESIAN_POINT('Ctrl Pts',(-1.47194228891689,18.2307806146047,-0.0878435449572992));
#28588=CARTESIAN_POINT('Ctrl Pts',(-0.735959210913743,18.1331323295489,
-0.0164961393612659));
#28589=CARTESIAN_POINT('Ctrl Pts',(-0.364750325439687,18.0705479584028,
-6.57768140928924E-16));
#28590=CARTESIAN_POINT('Ctrl Pts',(1.11022302462516E-13,18.,0.));
#28591=CARTESIAN_POINT('Ctrl Pts',(4.3700355726488,17.7638095491918,-0.772517910421123));
#28592=CARTESIAN_POINT('Ctrl Pts',(4.21037028349325,18.1928079867522,-1.2071356280258));
#28593=CARTESIAN_POINT('Ctrl Pts',(4.33444454890457,18.8064629622356,-1.28795340497675));
#28594=CARTESIAN_POINT('Ctrl Pts',(4.08157677842179,17.9187863941712,-0.68493732529669));
#28595=CARTESIAN_POINT('Ctrl Pts',(3.94432134460992,18.3471485006655,-1.0423041033654));
#28596=CARTESIAN_POINT('Ctrl Pts',(4.00038492840469,18.9207355731398,-1.07016519964085));
#28597=CARTESIAN_POINT('Ctrl Pts',(3.75474604679998,18.035513052921,-0.58088413905726));
#28598=CARTESIAN_POINT('Ctrl Pts',(3.63142428278685,18.4451150132921,-0.869282717230128));
#28599=CARTESIAN_POINT('Ctrl Pts',(3.64549788807283,18.9604219221275,-0.875151341779449));
#28600=CARTESIAN_POINT('Ctrl Pts',(3.06702447289767,18.1853704927497,-0.389458793918743));
#28601=CARTESIAN_POINT('Ctrl Pts',(2.96645051656865,18.5378312165733,-0.566779784268469));
#28602=CARTESIAN_POINT('Ctrl Pts',(2.9260796388088,18.9432172213792,-0.54888811962447));
#28603=CARTESIAN_POINT('Ctrl Pts',(2.7026702075431,18.2245844756192,-0.299660079535286));
#28604=CARTESIAN_POINT('Ctrl Pts',(2.61131057064228,18.5396307565727,-0.432068211521341));
#28605=CARTESIAN_POINT('Ctrl Pts',(2.55821925230454,18.8884651665002,-0.413977807541778));
#28606=CARTESIAN_POINT('Ctrl Pts',(1.96287492560049,18.242036866318,-0.15494504346654));
#28607=CARTESIAN_POINT('Ctrl Pts',(1.8915394662703,18.4751290932002,-0.219540167032862));
#28608=CARTESIAN_POINT('Ctrl Pts',(1.82891453529854,18.7188972454107,-0.204263617573607));
#28609=CARTESIAN_POINT('Ctrl Pts',(1.5808348198991,18.2227696331009,-0.0973283551978142));
#28610=CARTESIAN_POINT('Ctrl Pts',(1.52010391064048,18.410907571007,-0.137307210178231));
#28611=CARTESIAN_POINT('Ctrl Pts',(1.46353132936822,18.6039976265544,-0.127285837272504));
#28612=CARTESIAN_POINT('Ctrl Pts',(0.800159048007738,18.1403974722464,-0.0200632799728283));
#28613=CARTESIAN_POINT('Ctrl Pts',(0.765887806062742,18.235709489677,-0.027895363671069));
#28614=CARTESIAN_POINT('Ctrl Pts',(0.729117494448843,18.3301937694396,-0.0248672144968317));
#28615=CARTESIAN_POINT('Ctrl Pts',(0.398736386626917,18.0770350175674,-6.65308014686413E-13));
#28616=CARTESIAN_POINT('Ctrl Pts',(0.379968212283047,18.1240305159575,-3.43198578914328E-13));
#28617=CARTESIAN_POINT('Ctrl Pts',(0.361264584891461,18.1710404017938,-2.11825291438926E-14));
#28618=CARTESIAN_POINT('Ctrl Pts',(9.87716271744808E-14,18.,-2.01661604082304E-14));
#28619=CARTESIAN_POINT('Ctrl Pts',(9.87716271744808E-14,18.,-2.01661604082304E-14));
#28620=CARTESIAN_POINT('Ctrl Pts',(9.87716271744808E-14,18.,-2.01661604082304E-14));
#28621=CARTESIAN_POINT('',(4.26261338778694,18.0849267018156,-1.));
#28622=CARTESIAN_POINT('Ctrl Pts',(1.11022302462516E-13,18.,0.));
#28623=CARTESIAN_POINT('Ctrl Pts',(0.733684917774343,18.141905678209,-8.43898925349459E-15));
#28624=CARTESIAN_POINT('Ctrl Pts',(1.47554802668048,18.248989994314,-0.0649575167164615));
#28625=CARTESIAN_POINT('Ctrl Pts',(2.37917217060933,18.292385615839,-0.258451979040235));
#28626=CARTESIAN_POINT('Ctrl Pts',(2.5590083227402,18.2964779051253,-0.302914725119498));
#28627=CARTESIAN_POINT('Ctrl Pts',(2.91667689706811,18.2933500475868,-0.405113669626746));
#28628=CARTESIAN_POINT('Ctrl Pts',(3.09551309904672,18.2860499025368,-0.463246299412621));
#28629=CARTESIAN_POINT('Ctrl Pts',(3.61925135711831,18.2429598209236,-0.657687704390198));
#28630=CARTESIAN_POINT('Ctrl Pts',(3.95179505566489,18.1882637114373,-0.814072720039597));
#28631=CARTESIAN_POINT('Ctrl Pts',(4.26261338778694,18.0849267018156,-1.));
#28632=CARTESIAN_POINT('Origin',(5.10514446416566,18.8198698188909,0.));
#28633=CARTESIAN_POINT('Ctrl Pts',(4.29373077449695,18.8198698188909,-1.2615894039735));
#28634=CARTESIAN_POINT('Ctrl Pts',(4.05040020405469,17.5517750653646,-1.10508701472556));
#28635=CARTESIAN_POINT('Ctrl Pts',(4.71244104384522,17.3721875251301,-1.06752213906265E-15));
#28636=CARTESIAN_POINT('Ctrl Pts',(4.85172205448711,18.6399031556679,-1.62047143157596));
#28637=CARTESIAN_POINT('Ctrl Pts',(4.60179941708484,17.4268547636714,-1.43143837716499));
#28638=CARTESIAN_POINT('Ctrl Pts',(5.32488118013602,17.2060548471941,-0.426726929314143));
#28639=CARTESIAN_POINT('Ctrl Pts',(5.35047866129667,18.4418014142624,-2.03831036656378));
#28640=CARTESIAN_POINT('Ctrl Pts',(5.12064004592513,17.2814545873287,-1.82783948434398));
#28641=CARTESIAN_POINT('Ctrl Pts',(5.87223945189375,17.0232013062603,-0.923502876585836));
#28642=CARTESIAN_POINT('Ctrl Pts',(6.01799603717822,18.1420037326857,-2.75158942970812));
#28643=CARTESIAN_POINT('Ctrl Pts',(5.8322275983878,17.050842485112,-2.53593507991418));
#28644=CARTESIAN_POINT('Ctrl Pts',(6.60485088974162,16.7464649836239,-1.7715748338448));
#28645=CARTESIAN_POINT('Ctrl Pts',(6.22802018553555,18.0410299920564,-3.00559364749459));
#28646=CARTESIAN_POINT('Ctrl Pts',(6.05721596844273,16.9724647253118,-2.7891413201072));
#28647=CARTESIAN_POINT('Ctrl Pts',(6.83535589111342,16.6532584546769,-2.07357984873547));
#28648=CARTESIAN_POINT('Ctrl Pts',(6.61444355976506,17.8455392272447,-3.53737817259522));
#28649=CARTESIAN_POINT('Ctrl Pts',(6.47397956801548,16.818734456234,-3.32573967378444));
#28650=CARTESIAN_POINT('Ctrl Pts',(7.25946198077314,16.4728054400626,-2.70585908696185));
#28651=CARTESIAN_POINT('Ctrl Pts',(6.78984519594625,17.7516276808024,-3.81332671967964));
#28652=CARTESIAN_POINT('Ctrl Pts',(6.66536331485447,16.7437399954122,-3.60718861993155));
#28653=CARTESIAN_POINT('Ctrl Pts',(7.45196819833014,16.3861178595996,-3.0339553910857));
#28654=CARTESIAN_POINT('Ctrl Pts',(7.10602320700696,17.5758144266797,-4.38570647946684));
#28655=CARTESIAN_POINT('Ctrl Pts',(7.01161694949589,16.6021903559513,-4.19582456913687));
#28656=CARTESIAN_POINT('Ctrl Pts',(7.79897883144043,16.2238287011531,-3.71450140474986));
#28657=CARTESIAN_POINT('Ctrl Pts',(7.24680107601194,17.4939013437499,-4.68213458785877));
#28658=CARTESIAN_POINT('Ctrl Pts',(7.16729424914682,16.53538393131,-4.5033073042272));
#28659=CARTESIAN_POINT('Ctrl Pts',(7.9534848882684,16.1482166253277,-4.0669474232218));
#28660=CARTESIAN_POINT('Ctrl Pts',(7.4927351377619,17.3468185637659,-5.29696029054636));
#28661=CARTESIAN_POINT('Ctrl Pts',(7.43969881407855,16.4148594991966,-5.14462969386339));
#28662=CARTESIAN_POINT('Ctrl Pts',(8.22340161649126,16.0124479046869,-4.79796066055123));
#28663=CARTESIAN_POINT('Ctrl Pts',(7.59843488959468,17.2812951267931,-5.61809528199464));
#28664=CARTESIAN_POINT('Ctrl Pts',(7.55776347710494,16.3605717978334,-5.48196671762775));
#28665=CARTESIAN_POINT('Ctrl Pts',(8.3394088551856,15.9519647326952,-5.17978257942572));
#28666=CARTESIAN_POINT('Ctrl Pts',(7.85078664959272,17.1222147255282,-6.5896000401223));
#28667=CARTESIAN_POINT('Ctrl Pts',(7.83853818368898,16.2290439809763,-6.50196528014747));
#28668=CARTESIAN_POINT('Ctrl Pts',(8.61636911516069,15.8051212845613,-6.33487878776941));
#28669=CARTESIAN_POINT('Ctrl Pts',(7.93672823551223,17.0646099827074,-7.25148511305119));
#28670=CARTESIAN_POINT('Ctrl Pts',(7.93663307907031,16.1799952820739,-7.20918238147577));
#28671=CARTESIAN_POINT('Ctrl Pts',(8.710691437893,15.751947676348,-7.1218445044932));
#28672=CARTESIAN_POINT('Ctrl Pts',(7.93768657939644,17.0639797987105,-8.09776804418832));
#28673=CARTESIAN_POINT('Ctrl Pts',(7.93770957586298,16.1794674107193,-8.10764417924993));
#28674=CARTESIAN_POINT('Ctrl Pts',(8.71174323535012,15.7513659680398,-8.12805491868078));
#28675=CARTESIAN_POINT('Ctrl Pts',(7.93240014505281,17.0674607979061,-8.26866275408054));
#28676=CARTESIAN_POINT('Ctrl Pts',(7.93176509524196,16.1823866550743,-8.28915283131846));
#28677=CARTESIAN_POINT('Ctrl Pts',(8.70594128558497,15.7545791980315,-8.33124469184719));
#28678=CARTESIAN_POINT('Ctrl Pts',(7.91102975013306,17.0814770208683,-8.6070140950225));
#28679=CARTESIAN_POINT('Ctrl Pts',(7.90776940619277,16.1941201670182,-8.64818951047776));
#28680=CARTESIAN_POINT('Ctrl Pts',(8.68248692160874,15.767517250068,-8.7335364437005));
#28681=CARTESIAN_POINT('Ctrl Pts',(7.89499158493914,17.0919817317593,-8.77489499114022));
#28682=CARTESIAN_POINT('Ctrl Pts',(7.8897489782093,16.2029188357821,-8.82632296847022));
#28683=CARTESIAN_POINT('Ctrl Pts',(8.66488476781437,15.7772139061692,-8.9331428634661));
#28684=CARTESIAN_POINT('Ctrl Pts',(7.83124885358606,17.1334594467781,-9.27477806868774));
#28685=CARTESIAN_POINT('Ctrl Pts',(7.81819429110603,16.2376097544146,-9.35647171304077));
#28686=CARTESIAN_POINT('Ctrl Pts',(8.59492605886999,15.8155010279355,-9.52749203445515));
#28687=CARTESIAN_POINT('Ctrl Pts',(7.767980844109,17.1743995785599,-9.6030324637013));
#28688=CARTESIAN_POINT('Ctrl Pts',(7.74705485466677,16.2718853507128,-9.70416044777262));
#28689=CARTESIAN_POINT('Ctrl Pts',(8.52548836424224,15.8532919184051,-9.91777875606642));
#28690=CARTESIAN_POINT('Ctrl Pts',(7.6005474663986,17.2799782900502,-10.2499019964334));
#28691=CARTESIAN_POINT('Ctrl Pts',(7.56012110045394,16.3594808325921,-10.3856670523278));
#28692=CARTESIAN_POINT('Ctrl Pts',(8.34172744353473,15.9507491910812,-10.686891350078));
#28693=CARTESIAN_POINT('Ctrl Pts',(7.49539872629229,17.3451970522147,-10.5706888782151));
#28694=CARTESIAN_POINT('Ctrl Pts',(7.44265254159908,16.413527382139,-10.722693261602));
#28695=CARTESIAN_POINT('Ctrl Pts',(8.22632494925752,16.0109511247932,-11.0682993747428));
#28696=CARTESIAN_POINT('Ctrl Pts',(7.24864440937976,17.4928269391651,-11.1889365995399));
#28697=CARTESIAN_POINT('Ctrl Pts',(7.16932337182303,16.5345111926349,-11.3676325700104));
#28698=CARTESIAN_POINT('Ctrl Pts',(7.95550797735529,16.1472248672497,-11.8033813114068));
#28699=CARTESIAN_POINT('Ctrl Pts',(7.10730366773597,17.5750930730772,-11.4868686925473));
#28700=CARTESIAN_POINT('Ctrl Pts',(7.01301294517187,16.6016115427848,-11.6766918459536));
#28701=CARTESIAN_POINT('Ctrl Pts',(7.80038415841053,16.223162836288,-12.1576155320495));
#28702=CARTESIAN_POINT('Ctrl Pts',(6.78976913329171,17.7516792840666,-12.0619173719021));
#28703=CARTESIAN_POINT('Ctrl Pts',(6.66526779473846,16.7437872397738,-12.2680850887052));
#28704=CARTESIAN_POINT('Ctrl Pts',(7.45188471830793,16.3861654933833,-12.8413348280438));
#28705=CARTESIAN_POINT('Ctrl Pts',(6.61357326878161,17.8460111736693,-12.3390304245107));
#28706=CARTESIAN_POINT('Ctrl Pts',(6.47301642497381,16.819116615169,-12.5507150711689));
#28707=CARTESIAN_POINT('Ctrl Pts',(7.25850682191717,16.473241082915,-13.1708157017191));
#28708=CARTESIAN_POINT('Ctrl Pts',(6.22536744072334,18.0423400532621,-12.872844130597));
#28709=CARTESIAN_POINT('Ctrl Pts',(6.05435246414527,16.9734934471233,-13.0893257527182));
#28710=CARTESIAN_POINT('Ctrl Pts',(6.83244445950195,16.6544677419447,-13.8055075882121));
#28711=CARTESIAN_POINT('Ctrl Pts',(6.01671476286829,18.1425966890777,-13.1248577326192));
#28712=CARTESIAN_POINT('Ctrl Pts',(5.83087248062037,17.0512960564225,-13.3404912219347));
#28713=CARTESIAN_POINT('Ctrl Pts',(6.60344466985757,16.7470123279822,-14.1051458079917));
#28714=CARTESIAN_POINT('Ctrl Pts',(5.35036565224178,18.4418170514269,-13.8366538183739));
#28715=CARTESIAN_POINT('Ctrl Pts',(5.12056163117187,17.2814504145844,-14.0470786674275));
#28716=CARTESIAN_POINT('Ctrl Pts',(5.87211542254819,17.0232157405731,-14.9514545401227));
#28717=CARTESIAN_POINT('Ctrl Pts',(4.85205601950993,18.6397954431123,-14.2543137728728));
#28718=CARTESIAN_POINT('Ctrl Pts',(4.60212559171587,17.4267808681677,-14.4433685730329));
#28719=CARTESIAN_POINT('Ctrl Pts',(5.32524721434875,17.2059555554588,-15.4480180308682));
#28720=CARTESIAN_POINT('Ctrl Pts',(4.29373077449694,18.819869818891,-14.6134105960265));
#28721=CARTESIAN_POINT('Ctrl Pts',(4.05040020405468,17.5517750653647,-14.7699129852744));
#28722=CARTESIAN_POINT('Ctrl Pts',(4.71244104384522,17.3721875251302,-15.875));
#28723=CARTESIAN_POINT('Ctrl Pts',(4.26261338778696,18.0849267018155,-1.00000000000006));
#28724=CARTESIAN_POINT('Ctrl Pts',(4.36728621326876,18.0345646351299,-1.05117685404853));
#28725=CARTESIAN_POINT('Ctrl Pts',(4.47066603924481,17.9836961347291,-1.10368393307799));
#28726=CARTESIAN_POINT('Ctrl Pts',(4.57293726077334,17.9323320443341,-1.15750418168388));
#28727=CARTESIAN_POINT('Ctrl Pts',(4.67146734411905,17.8828468809424,-1.2093556556525));
#28728=CARTESIAN_POINT('Ctrl Pts',(4.76896783069495,17.8329013824936,-1.26242659776644));
#28729=CARTESIAN_POINT('Ctrl Pts',(4.86557698653789,17.7825339117877,-1.31667399740623));
#28730=CARTESIAN_POINT('Ctrl Pts',(4.95543149928796,17.735687994346,-1.36712856995748));
#28731=CARTESIAN_POINT('Ctrl Pts',(5.04451438811836,17.6884769521829,-1.41860113788473));
#28732=CARTESIAN_POINT('Ctrl Pts',(5.13292189515225,17.6409596305071,-1.47102663796827));
#28733=CARTESIAN_POINT('Ctrl Pts',(5.21778195838363,17.5953489911249,-1.52134850995953));
#28734=CARTESIAN_POINT('Ctrl Pts',(5.30201934370471,17.5494559582348,-1.57254874988241));
#28735=CARTESIAN_POINT('Ctrl Pts',(5.38571159337366,17.5033616056665,-1.62453576729421));
#28736=CARTESIAN_POINT('Ctrl Pts',(5.46816101585694,17.4579517527347,-1.6757507791882));
#28737=CARTESIAN_POINT('Ctrl Pts',(5.55008098985025,17.4123461818984,-1.72772990892807));
#28738=CARTESIAN_POINT('Ctrl Pts',(5.63154386776266,17.3666552420496,-1.78034500676327));
#28739=CARTESIAN_POINT('Ctrl Pts',(5.70699601133102,17.3243356058963,-1.82907790225456));
#28740=CARTESIAN_POINT('Ctrl Pts',(5.78205573011926,17.2819427722116,-1.87835641998092));
#28741=CARTESIAN_POINT('Ctrl Pts',(5.85678370500345,17.2395942752292,-1.92804036927623));
#28742=CARTESIAN_POINT('Ctrl Pts',(5.86273674999138,17.2362206723971,-1.93199833529621));
#28743=CARTESIAN_POINT('Ctrl Pts',(5.86868769280685,17.2328473676272,-1.93595885239063));
#28744=CARTESIAN_POINT('Ctrl Pts',(5.87463656592768,17.2294744291908,-1.93992183805002));
#28745=CARTESIAN_POINT('Ctrl Pts',(5.94218023588707,17.1911779928887,-1.98491768684271));
#28746=CARTESIAN_POINT('Ctrl Pts',(6.0095260979954,17.152891212362,-2.03028909272496));
#28747=CARTESIAN_POINT('Ctrl Pts',(6.07672203282924,17.1147265086007,-2.0758958976845));
#28748=CARTESIAN_POINT('Ctrl Pts',(6.15303774329964,17.0713821234137,-2.12769241977143));
#28749=CARTESIAN_POINT('Ctrl Pts',(6.22917890208468,17.0281434898988,-2.17987525959672));
#28750=CARTESIAN_POINT('Ctrl Pts',(6.30526200076612,16.9851285037549,-2.23235654707469));
#28751=CARTESIAN_POINT('Ctrl Pts',(6.37709936544756,16.9445139218052,-2.28190917377949));
#28752=CARTESIAN_POINT('Ctrl Pts',(6.44888463363832,16.9040987379059,-2.33172785680304));
#28753=CARTESIAN_POINT('Ctrl Pts',(6.52074248519078,16.8640091074109,-2.38171246233275));
#28754=CARTESIAN_POINT('Ctrl Pts',(6.56132078339888,16.8413703985416,-2.40993888693603));
#28755=CARTESIAN_POINT('Ctrl Pts',(6.60192274104519,16.8188359973897,-2.43821774342518));
#28756=CARTESIAN_POINT('Ctrl Pts',(6.64257554275894,16.796432756076,-2.46652697463318));
#28757=CARTESIAN_POINT('Ctrl Pts',(6.6915328700589,16.7694529964694,-2.5006191955733));
#28758=CARTESIAN_POINT('Ctrl Pts',(6.74051510505307,16.7426909854853,-2.5347274588589));
#28759=CARTESIAN_POINT('Ctrl Pts',(6.78965858551858,16.7161549427317,-2.56886567859258));
#28760=CARTESIAN_POINT('Ctrl Pts',(6.84639050239587,16.6855213661617,-2.60827531392821));
#28761=CARTESIAN_POINT('Ctrl Pts',(6.90327078437239,16.6552315277783,-2.64767596625816));
#28762=CARTESIAN_POINT('Ctrl Pts',(6.96040712448552,16.6253536648793,-2.68705007371724));
#28763=CARTESIAN_POINT('Ctrl Pts',(7.01594310569148,16.5963126652432,-2.72532133308595));
#28764=CARTESIAN_POINT('Ctrl Pts',(7.07172086784928,16.5676606663874,-2.7635677099645));
#28765=CARTESIAN_POINT('Ctrl Pts',(7.12782742597172,16.5394958406447,-2.80174349637038));
#28766=CARTESIAN_POINT('Ctrl Pts',(7.18144394303668,16.5125809859361,-2.83822501959682));
#28767=CARTESIAN_POINT('Ctrl Pts',(7.2353605715825,16.486110919191,-2.87464217652343));
#28768=CARTESIAN_POINT('Ctrl Pts',(7.28964430386149,16.4602063422403,-2.91092571776942));
#28769=CARTESIAN_POINT('Ctrl Pts',(7.33422861675332,16.438930396103,-2.94072611445956));
#28770=CARTESIAN_POINT('Ctrl Pts',(7.37906038058627,16.4180364302227,-2.97043594635113));
#28771=CARTESIAN_POINT('Ctrl Pts',(7.42417289637392,16.3976113139918,-2.99999999999845));
#28772=CARTESIAN_POINT('',(4.26261338778694,18.0849267018157,-14.875));
#28773=CARTESIAN_POINT('Ctrl Pts',(7.42417289637482,16.3976113139914,-12.875));
#28774=CARTESIAN_POINT('Ctrl Pts',(7.36225161991056,16.4256467548633,-12.915579513499));
#28775=CARTESIAN_POINT('Ctrl Pts',(7.30094639249221,16.4545320429019,-12.9564392282447));
#28776=CARTESIAN_POINT('Ctrl Pts',(7.24009139386733,16.4840912222715,-12.9974577492801));
#28777=CARTESIAN_POINT('Ctrl Pts',(7.1757966350601,16.5153212009266,-13.0407947959681));
#28778=CARTESIAN_POINT('Ctrl Pts',(7.11200471734016,16.547303345018,-13.0843090638802));
#28779=CARTESIAN_POINT('Ctrl Pts',(7.04856162589895,16.5798620330284,-13.1278831363843));
#28780=CARTESIAN_POINT('Ctrl Pts',(6.98025521941957,16.6149165508199,-13.1747974377025));
#28781=CARTESIAN_POINT('Ctrl Pts',(6.91235344189253,16.6506392237579,-13.2217809335886));
#28782=CARTESIAN_POINT('Ctrl Pts',(6.84470667688731,16.686848832706,-13.2687176599199));
#28783=CARTESIAN_POINT('Ctrl Pts',(6.77705991188208,16.7230584416542,-13.3156543862513));
#28784=CARTESIAN_POINT('Ctrl Pts',(6.70966889353779,16.7597552673182,-13.3625445738093));
#28785=CARTESIAN_POINT('Ctrl Pts',(6.64241644150871,16.7967930910297,-13.4093003716696));
#28786=CARTESIAN_POINT('Ctrl Pts',(6.57233897029021,16.8353867325524,-13.4580202023968));
#28787=CARTESIAN_POINT('Ctrl Pts',(6.50242162964476,16.8743437924329,-13.5065950677803));
#28788=CARTESIAN_POINT('Ctrl Pts',(6.43251652384589,16.9135581526054,-13.5549770222157));
#28789=CARTESIAN_POINT('Ctrl Pts',(6.35931673223419,16.9546207182078,-13.605639258428));
#28790=CARTESIAN_POINT('Ctrl Pts',(6.28613109921804,16.9959654795788,-13.6560900091192));
#28791=CARTESIAN_POINT('Ctrl Pts',(6.2128002331182,17.0375148584257,-13.7063097766082));
#28792=CARTESIAN_POINT('Ctrl Pts',(6.1696966120536,17.061937434846,-13.7358287764909));
#28793=CARTESIAN_POINT('Ctrl Pts',(6.12654294318534,17.0864315273824,-13.765268630581));
#28794=CARTESIAN_POINT('Ctrl Pts',(6.08330688290299,17.1109878358836,-13.7946306034417));
#28795=CARTESIAN_POINT('Ctrl Pts',(6.01363926687775,17.1505561837045,-13.8419424685295));
#28796=CARTESIAN_POINT('Ctrl Pts',(5.94390732285264,17.1902010442706,-13.8889357509433));
#28797=CARTESIAN_POINT('Ctrl Pts',(5.87395832485907,17.2298569422537,-13.9355276191119));
#28798=CARTESIAN_POINT('Ctrl Pts',(5.79682337621975,17.2735867417064,-13.9869059298996));
#28799=CARTESIAN_POINT('Ctrl Pts',(5.71935441097595,17.3173647764086,-14.0378525588354));
#28800=CARTESIAN_POINT('Ctrl Pts',(5.64148147055135,17.3610636861213,-14.088216031827));
#28801=CARTESIAN_POINT('Ctrl Pts',(5.56016891604116,17.406692757769,-14.1408040376301));
#28802=CARTESIAN_POINT('Ctrl Pts',(5.47841625868845,17.4522357074098,-14.1927565222537));
#28803=CARTESIAN_POINT('Ctrl Pts',(5.3961498839107,17.4975832920454,-14.2439470582352));
#28804=CARTESIAN_POINT('Ctrl Pts',(5.31003430543961,17.5450526681267,-14.2975327745159));
#28805=CARTESIAN_POINT('Ctrl Pts',(5.22335622149967,17.592308137648,-14.3502839048893));
#28806=CARTESIAN_POINT('Ctrl Pts',(5.13603167461429,17.6392602593379,-14.4020998953737));
#28807=CARTESIAN_POINT('Ctrl Pts',(5.04252760357117,17.6895349493158,-14.457582645966));
#28808=CARTESIAN_POINT('Ctrl Pts',(4.94828289112192,17.7394619303452,-14.5119935049597));
#28809=CARTESIAN_POINT('Ctrl Pts',(4.85318728886316,17.7889696993535,-14.5652541542623));
#28810=CARTESIAN_POINT('Ctrl Pts',(4.75201031666407,17.8416434934051,-14.6219208255467));
#28811=CARTESIAN_POINT('Ctrl Pts',(4.64987087505333,17.8938429542968,-14.6772859551681));
#28812=CARTESIAN_POINT('Ctrl Pts',(4.54661801546361,17.9455214051367,-14.7312983838822));
#28813=CARTESIAN_POINT('Ctrl Pts',(4.45291077487284,17.9924222371858,-14.7803174199895));
#28814=CARTESIAN_POINT('Ctrl Pts',(4.35828651072968,18.0388947333894,-14.8282232991068));
#28815=CARTESIAN_POINT('Ctrl Pts',(4.26261338778695,18.0849267018156,-14.8749999999999));
#28816=CARTESIAN_POINT('Origin',(5.10514446416566,18.819869818891,-15.875));
#28817=CARTESIAN_POINT('Ctrl Pts',(4.33449582574671,18.8064455741005,-14.5870131651188));
#28818=CARTESIAN_POINT('Ctrl Pts',(4.21041218730388,18.1927840291355,-14.6678383352104));
#28819=CARTESIAN_POINT('Ctrl Pts',(4.37008071934207,17.763785553718,-15.1024680157884));
#28820=CARTESIAN_POINT('Ctrl Pts',(4.00042123727896,18.9207316512905,-14.8048148488943));
#28821=CARTESIAN_POINT('Ctrl Pts',(3.94435406431171,18.3471385661789,-14.8326777457735));
#28822=CARTESIAN_POINT('Ctrl Pts',(4.08161076257883,17.9187745453667,-15.190051549908));
#28823=CARTESIAN_POINT('Ctrl Pts',(3.64551666599827,18.9604224970588,-14.9998401423731));
#28824=CARTESIAN_POINT('Ctrl Pts',(3.63144227309245,18.445112778749,-15.0057090520327));
#28825=CARTESIAN_POINT('Ctrl Pts',(3.7547644971397,18.0355093244708,-15.2941104791594));
#28826=CARTESIAN_POINT('Ctrl Pts',(2.92607962857322,18.9432173241542,-15.3261118849119));
#28827=CARTESIAN_POINT('Ctrl Pts',(2.96645048632596,18.5378314308947,-15.3082201989774));
#28828=CARTESIAN_POINT('Ctrl Pts',(3.0670243958767,18.1853707626654,-15.4855410702878));
#28829=CARTESIAN_POINT('Ctrl Pts',(2.55821923863863,18.8884652562898,-15.4610221971148));
#28830=CARTESIAN_POINT('Ctrl Pts',(2.61131053677853,18.53963094037,-15.442931777827));
#28831=CARTESIAN_POINT('Ctrl Pts',(2.702670137469,18.2245847172643,-15.5753398189059));
#28832=CARTESIAN_POINT('Ctrl Pts',(1.82891451879107,18.7188973096673,-15.6707363864532));
#28833=CARTESIAN_POINT('Ctrl Pts',(1.8915394318877,18.4751292210006,-15.655459830255));
#28834=CARTESIAN_POINT('Ctrl Pts',(1.96287487075161,18.2420370455397,-15.7200549068671));
#28835=CARTESIAN_POINT('Ctrl Pts',(1.46353131432253,18.6039976779082,-15.7477141653928));
#28836=CARTESIAN_POINT('Ctrl Pts',(1.5201038802911,18.4109076720057,-15.7376927883366));
#28837=CARTESIAN_POINT('Ctrl Pts',(1.5808347731626,18.2227697778871,-15.7776716140354));
#28838=CARTESIAN_POINT('Ctrl Pts',(0.729117484548387,18.3301937948796,-15.8501327863187));
#28839=CARTESIAN_POINT('Ctrl Pts',(0.765887787217641,18.2357095390798,-15.8471046364417));
#28840=CARTESIAN_POINT('Ctrl Pts',(0.800159021600452,18.1403975456869,-15.8549367139924));
#28841=CARTESIAN_POINT('Ctrl Pts',(0.361264579835011,18.1710404144994,-15.875));
#28842=CARTESIAN_POINT('Ctrl Pts',(0.379968202538298,18.1240305404275,-15.8749999999992));
#28843=CARTESIAN_POINT('Ctrl Pts',(0.3987363721605,18.0770350537944,-15.8749999999984));
#28844=CARTESIAN_POINT('Ctrl Pts',(4.96157966372969E-14,18.0000000000001,
-15.875));
#28845=CARTESIAN_POINT('Ctrl Pts',(4.96157966372969E-14,18.0000000000001,
-15.875));
#28846=CARTESIAN_POINT('Ctrl Pts',(4.96157966372969E-14,18.0000000000001,
-15.875));
#28847=CARTESIAN_POINT('Ctrl Pts',(4.26261338778694,18.0849267018157,-14.875));
#28848=CARTESIAN_POINT('Ctrl Pts',(3.95178714242438,18.188266342333,-15.0609320135528));
#28849=CARTESIAN_POINT('Ctrl Pts',(3.61923443569512,18.2429627164579,-15.2173202422925));
#28850=CARTESIAN_POINT('Ctrl Pts',(3.09548155756297,18.2860517458273,-15.411764578239));
#28851=CARTESIAN_POINT('Ctrl Pts',(2.91664062652119,18.2933512364512,-15.4698977560958));
#28852=CARTESIAN_POINT('Ctrl Pts',(2.55896263908662,18.2964774327613,-15.5720972662161));
#28853=CARTESIAN_POINT('Ctrl Pts',(2.37912173967026,18.2923841267789,-15.6165600378252));
#28854=CARTESIAN_POINT('Ctrl Pts',(1.83693290496417,18.2663432658698,-15.7326561330689));
#28855=CARTESIAN_POINT('Ctrl Pts',(1.47194228891703,18.2307806146048,-15.7871564550427));
#28856=CARTESIAN_POINT('Ctrl Pts',(0.735959210913914,18.1331323295489,-15.8585038606388));
#28857=CARTESIAN_POINT('Ctrl Pts',(0.364750325440251,18.0705479584007,-15.875));
#28858=CARTESIAN_POINT('Ctrl Pts',(5.55111512312578E-14,18.0000000000001,
-15.875));
#28859=CARTESIAN_POINT('Ctrl Pts',(2.65026635155863,16.5230910595128,-15.875));
#28860=CARTESIAN_POINT('Ctrl Pts',(3.93121151026238,17.4113360701453,-15.8749999999999));
#28861=CARTESIAN_POINT('Ctrl Pts',(4.67780976977134,17.9221915136298,-14.60813118344));
#28862=CARTESIAN_POINT('Ctrl Pts',(2.58982177486721,16.6081406311209,-15.875));
#28863=CARTESIAN_POINT('Ctrl Pts',(3.58403517899291,17.5024571546094,-15.875));
#28864=CARTESIAN_POINT('Ctrl Pts',(4.2564307312372,18.1092948426311,-14.8946688271178));
#28865=CARTESIAN_POINT('Ctrl Pts',(2.52003685548928,16.6804128457835,-15.875));
#28866=CARTESIAN_POINT('Ctrl Pts',(3.38378930551504,17.5440516972148,-15.875));
#28867=CARTESIAN_POINT('Ctrl Pts',(4.0035673119342,18.165009724916,-15.0260933099477));
#28868=CARTESIAN_POINT('Ctrl Pts',(2.40146991110847,16.7894204758253,-15.875));
#28869=CARTESIAN_POINT('Ctrl Pts',(3.10682864280578,17.6014533498092,-15.875));
#28870=CARTESIAN_POINT('Ctrl Pts',(3.65204402458872,18.2296067372696,-15.1932422733977));
#28871=CARTESIAN_POINT('Ctrl Pts',(2.35467715083744,16.8290896112474,-15.875));
#28872=CARTESIAN_POINT('Ctrl Pts',(3.01282991317325,17.6202437200566,-15.875));
#28873=CARTESIAN_POINT('Ctrl Pts',(3.5325569900976,18.2454983024018,-15.2442421923076));
#28874=CARTESIAN_POINT('Ctrl Pts',(2.21130584963083,16.9438587854015,-15.875));
#28875=CARTESIAN_POINT('Ctrl Pts',(2.74722464793244,17.6721885860779,-15.875));
#28876=CARTESIAN_POINT('Ctrl Pts',(3.1943476300972,18.2819216705679,-15.3791782895574));
#28877=CARTESIAN_POINT('Ctrl Pts',(2.11176395525861,17.014762601574,-15.875));
#28878=CARTESIAN_POINT('Ctrl Pts',(2.58832028065915,17.7015695819078,-15.875));
#28879=CARTESIAN_POINT('Ctrl Pts',(2.99607057193265,18.2908999426499,-15.4448482866377));
#28880=CARTESIAN_POINT('Ctrl Pts',(1.9075067361548,17.1492444573459,-15.875));
#28881=CARTESIAN_POINT('Ctrl Pts',(2.28363197198804,17.7549714543998,-15.875));
#28882=CARTESIAN_POINT('Ctrl Pts',(2.61932017223037,18.2973683425168,-15.5563761690608));
#28883=CARTESIAN_POINT('Ctrl Pts',(1.8027279134729,17.2127325814033,-15.875));
#28884=CARTESIAN_POINT('Ctrl Pts',(2.13794849055388,17.7789387893468,-15.8749999999995));
#28885=CARTESIAN_POINT('Ctrl Pts',(2.44212041430218,18.2940957945644,-15.6011724680293));
#28886=CARTESIAN_POINT('Ctrl Pts',(1.58907728513264,17.3339130080378,-15.875));
#28887=CARTESIAN_POINT('Ctrl Pts',(1.85327321501529,17.8227171794126,-15.8750000000004));
#28888=CARTESIAN_POINT('Ctrl Pts',(2.0996263813784,18.2799878268499,-15.6775823058619));
#28889=CARTESIAN_POINT('Ctrl Pts',(1.48001425485868,17.3916684380892,-15.875));
#28890=CARTESIAN_POINT('Ctrl Pts',(1.71380729714794,17.8426075850252,-15.8749999999998));
#28891=CARTESIAN_POINT('Ctrl Pts',(1.93430002680071,18.269009952329,-15.7090537912825));
#28892=CARTESIAN_POINT('Ctrl Pts',(1.14923719089035,17.5568620321583,-15.875));
#28893=CARTESIAN_POINT('Ctrl Pts',(1.30369857493354,17.8965847239176,-15.8750000000004));
#28894=CARTESIAN_POINT('Ctrl Pts',(1.45222631610486,18.2281607599578,-15.7886599080685));
#28895=CARTESIAN_POINT('Ctrl Pts',(0.923960370814538,17.6563936138833,-15.875));
#28896=CARTESIAN_POINT('Ctrl Pts',(1.03778172221532,17.9255569355278,-15.8749999999978));
#28897=CARTESIAN_POINT('Ctrl Pts',(1.14890106782412,18.1905780578685,-15.8223795985853));
#28898=CARTESIAN_POINT('Ctrl Pts',(0.466309887646269,17.8396525797121,-15.875));
#28899=CARTESIAN_POINT('Ctrl Pts',(0.514033028281665,17.9714545644638,-15.8750000000021));
#28900=CARTESIAN_POINT('Ctrl Pts',(0.560899725435248,18.1034285976806,-15.8657311564014));
#28901=CARTESIAN_POINT('Ctrl Pts',(0.233960073392275,17.9230862029257,-15.875));
#28902=CARTESIAN_POINT('Ctrl Pts',(0.255450344256121,17.9882387163098,-15.875));
#28903=CARTESIAN_POINT('Ctrl Pts',(0.276905092786154,18.0534927743003,-15.875));
#28904=CARTESIAN_POINT('Ctrl Pts',(6.56253264560329E-14,18.0000000000001,
-15.875));
#28905=CARTESIAN_POINT('Ctrl Pts',(6.56253264560329E-14,18.0000000000001,
-15.875));
#28906=CARTESIAN_POINT('Ctrl Pts',(6.56253264560329E-14,18.0000000000001,
-15.875));
#28907=CARTESIAN_POINT('Origin',(2.57755123502973,16.6150404676651,-12.875));
#28908=CARTESIAN_POINT('Ctrl Pts',(6.18681074697913,13.6646760949928,-15.875));
#28909=CARTESIAN_POINT('Ctrl Pts',(7.42417289637491,16.3976113139914,-15.875));
#28910=CARTESIAN_POINT('Ctrl Pts',(7.4241728963749,16.3976113139913,-12.8749999999999));
#28911=CARTESIAN_POINT('Ctrl Pts',(5.46924488951516,13.9895608039258,-15.875));
#28912=CARTESIAN_POINT('Ctrl Pts',(6.9364443429193,16.3422300389752,-15.8749999999987));
#28913=CARTESIAN_POINT('Ctrl Pts',(7.02429276766003,16.5786608069056,-13.1370575997094));
#28914=CARTESIAN_POINT('Ctrl Pts',(4.82362135451195,14.4304994470984,-15.875));
#28915=CARTESIAN_POINT('Ctrl Pts',(6.3369558752052,16.3976766216994,-15.875));
#28916=CARTESIAN_POINT('Ctrl Pts',(6.59593944537325,16.8198356081028,-13.4464657347114));
#28917=CARTESIAN_POINT('Ctrl Pts',(3.62953325538149,15.4524280214079,-15.875));
#28918=CARTESIAN_POINT('Ctrl Pts',(5.01707693139717,16.7889673744352,-15.875));
#28919=CARTESIAN_POINT('Ctrl Pts',(5.57070135292839,17.4021716501979,-14.1426663720984));
#28920=CARTESIAN_POINT('Ctrl Pts',(3.09339544139825,16.0236820718619,-15.875));
#28921=CARTESIAN_POINT('Ctrl Pts',(4.32161737669038,17.1014577313411,-15.875));
#28922=CARTESIAN_POINT('Ctrl Pts',(4.98189659820059,17.7388522671779,-14.5233265662417));
#28923=CARTESIAN_POINT('Ctrl Pts',(2.57755123502973,16.615040467665,-15.875));
#28924=CARTESIAN_POINT('Ctrl Pts',(3.58858852668408,17.4969722081554,-15.875));
#28925=CARTESIAN_POINT('Ctrl Pts',(4.26261338778696,18.0849267018156,-14.8749999999999));
#28926=CARTESIAN_POINT('Ctrl Pts',(-2.57755123502973,16.6150404676652,-15.875));
#28927=CARTESIAN_POINT('Ctrl Pts',(-3.58858852668405,17.4969722081555,-15.875));
#28928=CARTESIAN_POINT('Ctrl Pts',(-4.26261338778693,18.0849267018157,-14.875));
#28929=CARTESIAN_POINT('Ctrl Pts',(-3.09288471114456,16.0242675681528,-15.875));
#28930=CARTESIAN_POINT('Ctrl Pts',(-4.32097890338961,17.1018022275832,-15.875));
#28931=CARTESIAN_POINT('Ctrl Pts',(-4.98122339764458,17.7391761695861,-14.5236557087854));
#28932=CARTESIAN_POINT('Ctrl Pts',(-3.627647853051,15.4550005401893,-15.875));
#28933=CARTESIAN_POINT('Ctrl Pts',(-5.01362902801974,16.7908754694181,-15.875));
#28934=CARTESIAN_POINT('Ctrl Pts',(-5.56799291687747,17.403710991418,-14.1443060928063));
#28935=CARTESIAN_POINT('Ctrl Pts',(-4.51455185470875,14.6945381515796,-15.875));
#28936=CARTESIAN_POINT('Ctrl Pts',(-5.97317586756606,16.5050589588183,-15.875));
#28937=CARTESIAN_POINT('Ctrl Pts',(-6.33110821894754,16.9702594914345,-13.6264004799583));
#28938=CARTESIAN_POINT('Ctrl Pts',(-4.82417650767969,14.4564823289508,-15.875));
#28939=CARTESIAN_POINT('Ctrl Pts',(-6.28922934917424,16.4389856109726,-15.875));
#28940=CARTESIAN_POINT('Ctrl Pts',(-6.56619762783053,16.8368211352426,-13.4613493294144));
#28941=CARTESIAN_POINT('Ctrl Pts',(-5.48132765779044,14.0221782762144,-15.875));
#28942=CARTESIAN_POINT('Ctrl Pts',(-6.89238296370854,16.3693310552367,-15.875));
#28943=CARTESIAN_POINT('Ctrl Pts',(-7.01312239354118,16.5954930631039,-13.1508837135674));
#28944=CARTESIAN_POINT('Ctrl Pts',(-5.827547276862,13.8273360156432,-15.875));
#28945=CARTESIAN_POINT('Ctrl Pts',(-7.17519783431907,16.3693403474512,-15.875000000002));
#28946=CARTESIAN_POINT('Ctrl Pts',(-7.22390466722361,16.4882846401484,-13.0062438591931));
#28947=CARTESIAN_POINT('Ctrl Pts',(-6.18681074697824,13.6646760949932,-15.875));
#28948=CARTESIAN_POINT('Ctrl Pts',(-7.42417289637423,16.3976113139912,-15.875));
#28949=CARTESIAN_POINT('Ctrl Pts',(-7.42417289637437,16.3976113139916,-12.8750000000003));
#28950=CARTESIAN_POINT('Origin',(-2.57755123502973,16.6150404676652,-12.875));
#28951=CARTESIAN_POINT('Ctrl Pts',(7.10299919046342E-14,18.0000000000001,
-15.875));
#28952=CARTESIAN_POINT('Ctrl Pts',(7.10299919046342E-14,18.0000000000001,
-15.875));
#28953=CARTESIAN_POINT('Ctrl Pts',(7.10299919046342E-14,18.0000000000001,
-15.875));
#28954=CARTESIAN_POINT('Ctrl Pts',(-0.234069005549895,17.9230507329212,
-15.875));
#28955=CARTESIAN_POINT('Ctrl Pts',(-0.255572484264496,17.9883108104968,
-15.875));
#28956=CARTESIAN_POINT('Ctrl Pts',(-0.277021629265281,18.0535866911956,
-15.875));
#28957=CARTESIAN_POINT('Ctrl Pts',(-0.465540714391679,17.8399080016609,
-15.875));
#28958=CARTESIAN_POINT('Ctrl Pts',(-0.513189867278885,17.9714965813304,
-15.8750000000013));
#28959=CARTESIAN_POINT('Ctrl Pts',(-0.559992022757088,18.1032500480137,
-15.865732501886));
#28960=CARTESIAN_POINT('Ctrl Pts',(-0.920922503725983,17.6576622237466,
-15.875));
#28961=CARTESIAN_POINT('Ctrl Pts',(-1.03425506051337,17.9258961394952,-15.8749999999987));
#28962=CARTESIAN_POINT('Ctrl Pts',(-1.14491687502606,18.1900283969107,-15.8227387473914));
#28963=CARTESIAN_POINT('Ctrl Pts',(-1.14500232012262,17.5587569237231,-15.875));
#28964=CARTESIAN_POINT('Ctrl Pts',(-1.29867014733387,17.8971439307737,-15.8750000000008));
#28965=CARTESIAN_POINT('Ctrl Pts',(-1.44648584682184,18.2274660352735,-15.7893261010449));
#28966=CARTESIAN_POINT('Ctrl Pts',(-1.47389755518,17.3948291236,-15.875));
#28967=CARTESIAN_POINT('Ctrl Pts',(-1.70607551178078,17.8436724534546,-15.8749999999996));
#28968=CARTESIAN_POINT('Ctrl Pts',(-1.92517570374991,18.2683328929667,-15.7106973352853));
#28969=CARTESIAN_POINT('Ctrl Pts',(-1.58231605112504,17.3375717912511,-15.875));
#28970=CARTESIAN_POINT('Ctrl Pts',(-1.84452054067363,17.8239944625641,-15.875));
#28971=CARTESIAN_POINT('Ctrl Pts',(-2.08919765818595,18.2793742064832,-15.6796758611809));
#28972=CARTESIAN_POINT('Ctrl Pts',(-1.79616610743275,17.2166198358638,-15.875));
#28973=CARTESIAN_POINT('Ctrl Pts',(-2.12895470680322,17.7803825956827,-15.875));
#28974=CARTESIAN_POINT('Ctrl Pts',(-2.43121242086649,18.2938125595251,-15.6038274824088));
#28975=CARTESIAN_POINT('Ctrl Pts',(-1.90161128728044,17.1529545648422,-15.875));
#28976=CARTESIAN_POINT('Ctrl Pts',(-2.27519611057993,17.7563986700479,-15.875));
#28977=CARTESIAN_POINT('Ctrl Pts',(-2.60895323727161,18.2973410269971,-15.5592038314364));
#28978=CARTESIAN_POINT('Ctrl Pts',(-2.10852690803343,17.0170578688654,-15.875));
#28979=CARTESIAN_POINT('Ctrl Pts',(-2.58317026964648,17.7025162702681,-15.875));
#28980=CARTESIAN_POINT('Ctrl Pts',(-2.98960933272182,18.2911991025238,-15.4469955360255));
#28981=CARTESIAN_POINT('Ctrl Pts',(-2.20977219872288,16.9450430793437,-15.875));
#28982=CARTESIAN_POINT('Ctrl Pts',(-2.74453268668338,17.6727031367294,-15.875));
#28983=CARTESIAN_POINT('Ctrl Pts',(-3.19091502304556,18.2822213950292,-15.3804805124035));
#28984=CARTESIAN_POINT('Ctrl Pts',(-2.35442817124508,16.8293103914149,-15.875));
#28985=CARTESIAN_POINT('Ctrl Pts',(-3.01230037937074,17.6203479307052,-15.875));
#28986=CARTESIAN_POINT('Ctrl Pts',(-3.53187268765323,18.2455993729309,-15.2445526648722));
#28987=CARTESIAN_POINT('Ctrl Pts',(-2.40151582425997,16.7893870879841,-15.875));
#28988=CARTESIAN_POINT('Ctrl Pts',(-3.106895543949,17.6014376117974,-15.875));
#28989=CARTESIAN_POINT('Ctrl Pts',(-3.65212401943686,18.2296036955527,-15.1932231473742));
#28990=CARTESIAN_POINT('Ctrl Pts',(-2.5194290407753,16.6809575628544,-15.875));
#28991=CARTESIAN_POINT('Ctrl Pts',(-3.38240321244847,17.5443315105624,-15.875));
#28992=CARTESIAN_POINT('Ctrl Pts',(-4.0018443914251,18.1652942771662,-15.0268910373232));
#28993=CARTESIAN_POINT('Ctrl Pts',(-2.58809131240417,16.6098149497214,-15.875));
#28994=CARTESIAN_POINT('Ctrl Pts',(-3.5795504098364,17.5033224532898,-15.875));
#28995=CARTESIAN_POINT('Ctrl Pts',(-4.25085054079885,18.1101703713992,-14.8973061650154));
#28996=CARTESIAN_POINT('Ctrl Pts',(-2.64710716057363,16.5274299671713,-15.875));
#28997=CARTESIAN_POINT('Ctrl Pts',(-3.91380212598874,17.4158477301436,-15.875));
#28998=CARTESIAN_POINT('Ctrl Pts',(-4.65725862181919,17.9310735147891,-14.6219520331606));
#28999=CARTESIAN_POINT('Ctrl Pts',(1.34330150810747E-13,18.,-3.25260651745651E-15));
#29000=CARTESIAN_POINT('Ctrl Pts',(1.34330150810747E-13,18.,-3.25260651745651E-15));
#29001=CARTESIAN_POINT('Ctrl Pts',(1.34330150810747E-13,18.,-3.25260651745651E-15));
#29002=CARTESIAN_POINT('Ctrl Pts',(0.234125392939614,17.9230321957875,-3.90312782094782E-15));
#29003=CARTESIAN_POINT('Ctrl Pts',(0.255636569916122,17.9883077450276,-5.57090702034659E-15));
#29004=CARTESIAN_POINT('Ctrl Pts',(0.277092073072303,18.0536000698534,-7.23849759038514E-15));
#29005=CARTESIAN_POINT('Ctrl Pts',(0.466044116165369,17.8397456189194,-3.90312782094782E-15));
#29006=CARTESIAN_POINT('Ctrl Pts',(0.513738375516134,17.9714716147092,2.5996297196232E-12));
#29007=CARTESIAN_POINT('Ctrl Pts',(0.560578310461167,18.1033685423708,-0.00926178509230557));
#29008=CARTESIAN_POINT('Ctrl Pts',(0.923258246822673,17.6566881249403,-3.90312782094782E-15));
#29009=CARTESIAN_POINT('Ctrl Pts',(1.03696511564348,17.9256348627915,-2.63383661051795E-12));
#29010=CARTESIAN_POINT('Ctrl Pts',(1.14797712170856,18.1904491877953,-0.0525350981222591));
#29011=CARTESIAN_POINT('Ctrl Pts',(1.14901068589157,17.5569249384112,-3.90312782094782E-15));
#29012=CARTESIAN_POINT('Ctrl Pts',(1.3034614298748,17.8965907426942,-7.42089362459187E-13));
#29013=CARTESIAN_POINT('Ctrl Pts',(1.45199329102125,18.2280903008762,-0.0863653390068735));
#29014=CARTESIAN_POINT('Ctrl Pts',(1.47823538432377,17.3925817155132,-3.90312782094782E-15));
#29015=CARTESIAN_POINT('Ctrl Pts',(1.71156276414173,17.8429116909266,3.72586727994298E-13));
#29016=CARTESIAN_POINT('Ctrl Pts',(1.93165601447728,18.2688045577474,-0.16547617335809));
#29017=CARTESIAN_POINT('Ctrl Pts',(1.5865002670268,17.3352987442417,-3.90312782094782E-15));
#29018=CARTESIAN_POINT('Ctrl Pts',(1.84994552041935,17.8231970718718,7.48227181606773E-14));
#29019=CARTESIAN_POINT('Ctrl Pts',(2.09567016562423,18.2797417545793,-0.196634467066437));
#29020=CARTESIAN_POINT('Ctrl Pts',(1.79944928043518,17.2146660494541,-3.90312782094782E-15));
#29021=CARTESIAN_POINT('Ctrl Pts',(2.13346302307632,17.7796530524275,-8.44427400896034E-14));
#29022=CARTESIAN_POINT('Ctrl Pts',(2.43668826790097,18.2939422278445,-0.272515027710232));
#29023=CARTESIAN_POINT('Ctrl Pts',(1.90414773824699,17.151340599891,-3.90312782094782E-15));
#29024=CARTESIAN_POINT('Ctrl Pts',(2.27885177250061,17.7557724864729,8.90502107893631E-14));
#29025=CARTESIAN_POINT('Ctrl Pts',(2.61346406100076,18.2973270865418,-0.317051368781859));
#29026=CARTESIAN_POINT('Ctrl Pts',(2.1088743828907,17.0167770117627,-3.90312782094782E-15));
#29027=CARTESIAN_POINT('Ctrl Pts',(2.58377885264389,17.7023930210976,-9.69193503961864E-14));
#29028=CARTESIAN_POINT('Ctrl Pts',(2.99040325834679,18.2911221026525,-0.428311953949879));
#29029=CARTESIAN_POINT('Ctrl Pts',(2.20896418655429,16.9456432686019,-3.90312782094782E-15));
#29030=CARTESIAN_POINT('Ctrl Pts',(2.74317790194251,17.6729570612561,2.28883521929507E-14));
#29031=CARTESIAN_POINT('Ctrl Pts',(3.18920946464565,18.2823326069824,-0.493912463383087));
#29032=CARTESIAN_POINT('Ctrl Pts',(2.3537482518898,16.8298772373725,-3.90312782094782E-15));
#29033=CARTESIAN_POINT('Ctrl Pts',(3.01096091470094,17.6206124704897,-1.71623730517786E-14));
#29034=CARTESIAN_POINT('Ctrl Pts',(3.5301688979625,18.2458140896114,-0.629729813065811));
#29035=CARTESIAN_POINT('Ctrl Pts',(2.40124097545901,16.7896357735171,-3.90312782094782E-15));
#29036=CARTESIAN_POINT('Ctrl Pts',(3.10627843143028,17.601562552945,-1.66557843234476E-14));
#29037=CARTESIAN_POINT('Ctrl Pts',(3.65133078641054,18.2297390382189,-0.681405276743203));
#29038=CARTESIAN_POINT('Ctrl Pts',(2.5189927470668,16.681365157594,-3.90312782094782E-15));
#29039=CARTESIAN_POINT('Ctrl Pts',(3.38133850977177,17.5445513739635,1.81195115538009E-14));
#29040=CARTESIAN_POINT('Ctrl Pts',(4.00051020852894,18.1655490559811,-0.847460814619883));
#29041=CARTESIAN_POINT('Ctrl Pts',(2.58698239764016,16.6108854489588,-3.90312782094782E-15));
#29042=CARTESIAN_POINT('Ctrl Pts',(3.57666092871365,17.5038821817581,-9.64497019840983E-14));
#29043=CARTESIAN_POINT('Ctrl Pts',(4.2472541605191,18.1107431001,-0.975990516500565));
#29044=CARTESIAN_POINT('Ctrl Pts',(2.64500586200195,16.5302897988031,-3.90312782094782E-15));
#29045=CARTESIAN_POINT('Ctrl Pts',(3.90245585433798,17.4187779420453,1.36808593330039E-13));
#29046=CARTESIAN_POINT('Ctrl Pts',(4.64383425604972,17.9368198526809,-1.24406142456628));
#29047=CARTESIAN_POINT('Origin',(2.57755123502973,16.6150404676649,-3.));
#29048=CARTESIAN_POINT('Ctrl Pts',(2.57755123502973,16.6150404676649,-3.90312782094782E-15));
#29049=CARTESIAN_POINT('Ctrl Pts',(3.58858852668408,17.4969722081553,-4.11996825544492E-15));
#29050=CARTESIAN_POINT('Ctrl Pts',(4.26261338778696,18.0849267018155,-1.00000000000006));
#29051=CARTESIAN_POINT('Ctrl Pts',(3.09288471119035,16.0242675681923,-3.90312782094782E-15));
#29052=CARTESIAN_POINT('Ctrl Pts',(4.32097890344208,17.1018022276782,8.76728492794768E-13));
#29053=CARTESIAN_POINT('Ctrl Pts',(4.98122339765377,17.7391761696867,-1.35134429129639));
#29054=CARTESIAN_POINT('Ctrl Pts',(3.62764785305072,15.4550005401872,-3.90312782094782E-15));
#29055=CARTESIAN_POINT('Ctrl Pts',(5.01362902801955,16.7908754694178,-3.67888638612552E-13));
#29056=CARTESIAN_POINT('Ctrl Pts',(5.56799291687799,17.4037109914178,-1.73069390719434));
#29057=CARTESIAN_POINT('Ctrl Pts',(4.51455185471047,14.6945381515792,-3.90312782094782E-15));
#29058=CARTESIAN_POINT('Ctrl Pts',(5.9731758675679,16.5050589588179,1.90369720475917E-13));
#29059=CARTESIAN_POINT('Ctrl Pts',(6.33110821894858,16.9702594914338,-2.2485995200423));
#29060=CARTESIAN_POINT('Ctrl Pts',(4.82417650768106,14.4564823289491,-3.90312782094782E-15));
#29061=CARTESIAN_POINT('Ctrl Pts',(6.2892293491753,16.4389856109718,1.00596761688566E-13));
#29062=CARTESIAN_POINT('Ctrl Pts',(6.56619762783129,16.8368211352422,-2.41365067058626));
#29063=CARTESIAN_POINT('Ctrl Pts',(5.48132765779251,14.0221782762138,-3.90312782094782E-15));
#29064=CARTESIAN_POINT('Ctrl Pts',(6.89238296371062,16.3693310552372,-1.130184358169E-13));
#29065=CARTESIAN_POINT('Ctrl Pts',(7.01312239354269,16.595493063103,-2.72411628643354));
#29066=CARTESIAN_POINT('Ctrl Pts',(5.82754727684479,13.8273360155938,-3.90312782094782E-15));
#29067=CARTESIAN_POINT('Ctrl Pts',(7.17519783432794,16.3693403473953,-1.82423844731643E-12));
#29068=CARTESIAN_POINT('Ctrl Pts',(7.22390466723139,16.4882846401449,-2.868756140798));
#29069=CARTESIAN_POINT('Ctrl Pts',(6.18681074697836,13.6646760949931,-3.90312782094782E-15));
#29070=CARTESIAN_POINT('Ctrl Pts',(7.42417289637432,16.3976113139913,-3.90312782096724E-15));
#29071=CARTESIAN_POINT('Ctrl Pts',(7.42417289637442,16.3976113139915,-2.99999999999976));
#29072=CARTESIAN_POINT('Ctrl Pts',(-6.18681074697897,13.6646760949927,-4.33680868994202E-15));
#29073=CARTESIAN_POINT('Ctrl Pts',(-7.42417289637478,16.3976113139913,-4.33680868994226E-15));
#29074=CARTESIAN_POINT('Ctrl Pts',(-7.42417289637476,16.3976113139913,-3.00000000000003));
#29075=CARTESIAN_POINT('Ctrl Pts',(-5.46924488956975,13.9895608040479,-4.33680868994202E-15));
#29076=CARTESIAN_POINT('Ctrl Pts',(-6.93644434272296,16.3422300407555,6.3950190944217E-13));
#29077=CARTESIAN_POINT('Ctrl Pts',(-7.02429276683661,16.5786608072783,-2.73794240179331));
#29078=CARTESIAN_POINT('Ctrl Pts',(-4.82362135451254,14.4304994470984,-3.90312782094782E-15));
#29079=CARTESIAN_POINT('Ctrl Pts',(-6.33695587520574,16.3976766216994,-2.26478507750015E-13));
#29080=CARTESIAN_POINT('Ctrl Pts',(-6.59593944537465,16.8198356081016,-2.42853426528885));
#29081=CARTESIAN_POINT('Ctrl Pts',(-3.62953325538071,15.4524280214079,-3.90312782094782E-15));
#29082=CARTESIAN_POINT('Ctrl Pts',(-5.01707693139635,16.7889673744352,2.00368435798586E-13));
#29083=CARTESIAN_POINT('Ctrl Pts',(-5.57070135292674,17.4021716501991,-1.73233362790125));
#29084=CARTESIAN_POINT('Ctrl Pts',(-3.0933954413352,16.0236820718031,-3.90312782094782E-15));
#29085=CARTESIAN_POINT('Ctrl Pts',(-4.32161737629064,17.101457730593,-7.08979370270738E-13));
#29086=CARTESIAN_POINT('Ctrl Pts',(-4.98189659816054,17.7388522667007,-1.35167343337454));
#29087=CARTESIAN_POINT('Ctrl Pts',(-2.57755123502756,16.6150404676675,-3.90312782094782E-15));
#29088=CARTESIAN_POINT('Ctrl Pts',(-3.58858852668275,17.4969722081568,-3.68628738645072E-15));
#29089=CARTESIAN_POINT('Ctrl Pts',(-4.2626133877862,18.0849267018164,-1.00000000000002));
#29090=CARTESIAN_POINT('Origin',(-2.57755123502967,16.6150404676651,-3.));
#29091=CARTESIAN_POINT('Ctrl Pts',(-2.65026635075671,16.5230910607405,-3.90312782094782E-15));
#29092=CARTESIAN_POINT('Ctrl Pts',(-3.93121150527454,17.4113360715034,-2.40519271556319E-14));
#29093=CARTESIAN_POINT('Ctrl Pts',(-4.67780976387663,17.9221915162604,-1.26686881256096));
#29094=CARTESIAN_POINT('Ctrl Pts',(-2.58982177419273,16.6081406317741,-3.90312782094782E-15));
#29095=CARTESIAN_POINT('Ctrl Pts',(-3.58403517709281,17.502457154976,-7.58581112797788E-16));
#29096=CARTESIAN_POINT('Ctrl Pts',(-4.25643072887683,18.1092948431411,-0.98033117164757));
#29097=CARTESIAN_POINT('Ctrl Pts',(-2.520036855148,16.6804128460974,-3.90312782094782E-15));
#29098=CARTESIAN_POINT('Ctrl Pts',(-3.3837893047036,17.5440516973813,6.73959394317873E-15));
#29099=CARTESIAN_POINT('Ctrl Pts',(-4.0035673109207,18.1650097251003,-0.848906689568997));
#29100=CARTESIAN_POINT('Ctrl Pts',(-2.4014699111082,16.7894204758251,-3.90312782094782E-15));
#29101=CARTESIAN_POINT('Ctrl Pts',(-3.10682864280438,17.6014533498079,-1.0760287253188E-14));
#29102=CARTESIAN_POINT('Ctrl Pts',(-3.6520440245868,18.2296067372679,-0.681757726600342));
#29103=CARTESIAN_POINT('Ctrl Pts',(-2.35467715083726,16.8290896112472,-3.90312782094782E-15));
#29104=CARTESIAN_POINT('Ctrl Pts',(-3.01282991317201,17.6202437200552,9.82896428929409E-15));
#29105=CARTESIAN_POINT('Ctrl Pts',(-3.53255699009597,18.2454983024002,-0.630757807690744));
#29106=CARTESIAN_POINT('Ctrl Pts',(-2.21130584963072,16.9438587854014,-3.90312782094782E-15));
#29107=CARTESIAN_POINT('Ctrl Pts',(-2.74722464793154,17.672188586077,-2.97020675421629E-14));
#29108=CARTESIAN_POINT('Ctrl Pts',(-3.19434763009571,18.2819216705659,-0.495821710441106));
#29109=CARTESIAN_POINT('Ctrl Pts',(-2.11176395525848,17.0147626015738,-3.90312782094782E-15));
#29110=CARTESIAN_POINT('Ctrl Pts',(-2.58832028065808,17.7015695819063,-7.00728626402298E-14));
#29111=CARTESIAN_POINT('Ctrl Pts',(-2.99607057193134,18.2908999426481,-0.430151713361074));
#29112=CARTESIAN_POINT('Ctrl Pts',(-1.90750673615457,17.1492444573458,-3.90312782094782E-15));
#29113=CARTESIAN_POINT('Ctrl Pts',(-2.28363197198743,17.7549714543992,6.25362877129781E-14));
#29114=CARTESIAN_POINT('Ctrl Pts',(-2.61932017222916,18.2973683425155,-0.318623830938357));
#29115=CARTESIAN_POINT('Ctrl Pts',(-1.8027279134725,17.2127325814031,-3.90312782094782E-15));
#29116=CARTESIAN_POINT('Ctrl Pts',(-2.13794849055309,17.7789387893463,-1.6446554081392E-13));
#29117=CARTESIAN_POINT('Ctrl Pts',(-2.44212041430075,18.2940957945633,-0.273827531969986));
#29118=CARTESIAN_POINT('Ctrl Pts',(-1.58907728513264,17.3339130080377,-3.90312782094782E-15));
#29119=CARTESIAN_POINT('Ctrl Pts',(-1.85327321501476,17.8227171794114,1.55159105695241E-13));
#29120=CARTESIAN_POINT('Ctrl Pts',(-2.09962638137778,18.2799878268482,-0.197417694137515));
#29121=CARTESIAN_POINT('Ctrl Pts',(-1.48001425485894,17.3916684380896,-3.90312782094782E-15));
#29122=CARTESIAN_POINT('Ctrl Pts',(-1.71380729714811,17.8426075850251,-1.06713969348454E-13));
#29123=CARTESIAN_POINT('Ctrl Pts',(-1.93430002680081,18.2690099523279,-0.165946208717278));
#29124=CARTESIAN_POINT('Ctrl Pts',(-1.14923719088923,17.5568620321569,-3.90312782094782E-15));
#29125=CARTESIAN_POINT('Ctrl Pts',(-1.30369857493165,17.8965847239158,2.13313069839087E-13));
#29126=CARTESIAN_POINT('Ctrl Pts',(-1.45222631610225,18.2281607599565,-0.0863400919308878));
#29127=CARTESIAN_POINT('Ctrl Pts',(-0.923960370814179,17.6563936138833,
-3.90312782094782E-15));
#29128=CARTESIAN_POINT('Ctrl Pts',(-1.03778172221478,17.9255569355276,-4.02138859125459E-12));
#29129=CARTESIAN_POINT('Ctrl Pts',(-1.14890106782272,18.1905780578673,-0.0526204014144626));
#29130=CARTESIAN_POINT('Ctrl Pts',(-0.466309887646034,17.8396525797112,
-3.90312782094782E-15));
#29131=CARTESIAN_POINT('Ctrl Pts',(-0.514033028281307,17.971454564463,3.99686269630224E-12));
#29132=CARTESIAN_POINT('Ctrl Pts',(-0.560899725435443,18.1034285976806,
-0.0092688435986574));
#29133=CARTESIAN_POINT('Ctrl Pts',(-0.233960073391672,17.9230862029248,
-3.90312782094782E-15));
#29134=CARTESIAN_POINT('Ctrl Pts',(-0.255450344254625,17.9882387163068,
-4.24790311669457E-15));
#29135=CARTESIAN_POINT('Ctrl Pts',(-0.276905092784516,18.0534927742982,
-4.59293432271516E-15));
#29136=CARTESIAN_POINT('Ctrl Pts',(1.00908127238944E-13,18.,-3.25260651745651E-15));
#29137=CARTESIAN_POINT('Ctrl Pts',(1.00908127238944E-13,18.,-3.25260651745651E-15));
#29138=CARTESIAN_POINT('Ctrl Pts',(1.00908127238944E-13,18.,-3.25260651745651E-15));
#32879=UNCERTAINTY_MEASURE_WITH_UNIT(LENGTH_MEASURE(0.01),#32904,
'DISTANCE_ACCURACY_VALUE',
'Maximum model space distance between geometric entities at asserted c
onnectivities');
#32886=UNCERTAINTY_MEASURE_WITH_UNIT(LENGTH_MEASURE(0.01),#32904,
'DISTANCE_ACCURACY_VALUE',
'Maximum model space distance between geometric entities at asserted c
onnectivities');
#32896=(
GEOMETRIC_REPRESENTATION_CONTEXT(3)
GLOBAL_UNCERTAINTY_ASSIGNED_CONTEXT((#32879))
GLOBAL_UNIT_ASSIGNED_CONTEXT((#32904,#32906,#32907))
REPRESENTATION_CONTEXT('','3D')
);
#32903=(
GEOMETRIC_REPRESENTATION_CONTEXT(3)
GLOBAL_UNCERTAINTY_ASSIGNED_CONTEXT((#32886))
GLOBAL_UNIT_ASSIGNED_CONTEXT((#32904,#32906,#32907))
REPRESENTATION_CONTEXT('','3D')
);
#32904=(
LENGTH_UNIT()
NAMED_UNIT(*)
SI_UNIT(.MILLI.,.METRE.)
);
#32906=(
NAMED_UNIT(*)
PLANE_ANGLE_UNIT()
SI_UNIT($,.RADIAN.)
);
#32907=(
NAMED_UNIT(*)
SI_UNIT($,.STERADIAN.)
SOLID_ANGLE_UNIT()
);
#32917=SHAPE_DEFINITION_REPRESENTATION(#32933,#33021);
#32933=PRODUCT_DEFINITION_SHAPE('',$,#33038);
#33021=SHAPE_REPRESENTATION('',(#16374),#32896);
#33028=PRODUCT_DEFINITION_CONTEXT('part definition',#33078,'design');
#33038=PRODUCT_DEFINITION('Eye Bolt','Eye Bolt',#33054,#33028);
#33054=PRODUCT_DEFINITION_FORMATION('',$,#33089);
#33078=APPLICATION_CONTEXT(
'Core Data for Automotive Mechanical Design Process');
#33079=PRODUCT_CONTEXT('part definition',#33078,'mechanical');
#33089=PRODUCT('Eye Bolt','Eye Bolt',$,(#33079));
#33098=PRESENTATION_STYLE_ASSIGNMENT((#33104));
#33104=SURFACE_STYLE_USAGE(.BOTH.,#33110);
#33110=SURFACE_SIDE_STYLE('',(#33116));
#33116=SURFACE_STYLE_FILL_AREA(#33122);
#33122=FILL_AREA_STYLE('Opaque(227,224,212)',(#33128));
#33128=FILL_AREA_STYLE_COLOUR('Opaque(227,224,212)',#33134);
#33134=COLOUR_RGB('Opaque(227,224,212)',0.890196078431372,0.87843137254902,
0.831372549019608);
ENDSEC;
END-ISO-10303-21;
